ISO-10303-21;
HEADER;
/* Generated by software containing ST-Developer
 * from STEP Tools, Inc. (www.steptools.com) 
 */

FILE_DESCRIPTION(
/* description */ ('STEP AP214'),
/* implementation_level */ '2;1');

FILE_NAME(
/* name */ 'PRT-TQ-1012-02.step',
/* time_stamp */ '2026-10-07T12:49:37-07:00',
/* author */ (''),
/* organization */ (''),
/* preprocessor_version */ 'ST-DEVELOPER v20.2',
/* originating_system */ 'Autodesk Translation Framework v15.15.0.0',
/* authorisation */ '');

FILE_SCHEMA (('AUTOMOTIVE_DESIGN { 1 0 10303 214 3 1 1 }'));
ENDSEC;

DATA;
#10=MECHANICAL_DESIGN_GEOMETRIC_PRESENTATION_REPRESENTATION('',(#296),#33016);
#11=B_SPLINE_SURFACE_WITH_KNOTS('',1,3,((#22855,#22856,#22857,#22858,#22859,
#22860,#22861,#22862,#22863,#22864,#22865,#22866,#22867,#22868,#22869,#22870,
#22871,#22872,#22873,#22874,#22875,#22876,#22877,#22878,#22879,#22880,#22881,
#22882,#22883,#22884,#22885,#22886,#22887,#22888,#22889,#22890,#22891,#22892,
#22893,#22894,#22895,#22896,#22897,#22898,#22899,#22900,#22901,#22902,#22903,
#22904,#22905,#22906,#22907,#22908,#22909,#22910,#22911,#22912,#22913,#22914,
#22915,#22916,#22917,#22918,#22919,#22920,#22921,#22922,#22923,#22924,#22925,
#22926,#22927,#22928,#22929,#22930,#22931,#22932,#22933,#22934,#22935,#22936,
#22937,#22938,#22939,#22940,#22941,#22942,#22943,#22944,#22945,#22946,#22947,
#22948,#22949,#22950,#22951,#22952,#22953,#22954,#22955,#22956,#22957,#22958,
#22959,#22960,#22961,#22962,#22963,#22964,#22965,#22966,#22967,#22968,#22969,
#22970,#22971,#22972,#22973,#22974,#22975,#22976,#22977,#22978,#22979,#22980,
#22981,#22982,#22983,#22984,#22985,#22986,#22987,#22988,#22989,#22990,#22991,
#22992,#22993,#22994,#22995,#22996,#22997,#22998,#22999,#23000,#23001,#23002,
#23003,#23004,#23005,#23006,#23007,#23008,#23009,#23010,#23011,#23012,#23013,
#23014,#23015,#23016,#23017,#23018,#23019,#23020,#23021,#23022,#23023,#23024,
#23025,#23026,#23027,#23028,#23029,#23030,#23031,#23032,#23033,#23034,#23035,
#23036,#23037,#23038,#23039,#23040,#23041,#23042,#23043,#23044,#23045,#23046,
#23047,#23048,#23049,#23050,#23051,#23052,#23053,#23054,#23055,#23056,#23057,
#23058,#23059,#23060,#23061,#23062,#23063,#23064,#23065,#23066,#23067,#23068,
#23069,#23070,#23071,#23072,#23073,#23074,#23075,#23076,#23077,#23078,#23079,
#23080,#23081,#23082),(#23083,#23084,#23085,#23086,#23087,#23088,#23089,
#23090,#23091,#23092,#23093,#23094,#23095,#23096,#23097,#23098,#23099,#23100,
#23101,#23102,#23103,#23104,#23105,#23106,#23107,#23108,#23109,#23110,#23111,
#23112,#23113,#23114,#23115,#23116,#23117,#23118,#23119,#23120,#23121,#23122,
#23123,#23124,#23125,#23126,#23127,#23128,#23129,#23130,#23131,#23132,#23133,
#23134,#23135,#23136,#23137,#23138,#23139,#23140,#23141,#23142,#23143,#23144,
#23145,#23146,#23147,#23148,#23149,#23150,#23151,#23152,#23153,#23154,#23155,
#23156,#23157,#23158,#23159,#23160,#23161,#23162,#23163,#23164,#23165,#23166,
#23167,#23168,#23169,#23170,#23171,#23172,#23173,#23174,#23175,#23176,#23177,
#23178,#23179,#23180,#23181,#23182,#23183,#23184,#23185,#23186,#23187,#23188,
#23189,#23190,#23191,#23192,#23193,#23194,#23195,#23196,#23197,#23198,#23199,
#23200,#23201,#23202,#23203,#23204,#23205,#23206,#23207,#23208,#23209,#23210,
#23211,#23212,#23213,#23214,#23215,#23216,#23217,#23218,#23219,#23220,#23221,
#23222,#23223,#23224,#23225,#23226,#23227,#23228,#23229,#23230,#23231,#23232,
#23233,#23234,#23235,#23236,#23237,#23238,#23239,#23240,#23241,#23242,#23243,
#23244,#23245,#23246,#23247,#23248,#23249,#23250,#23251,#23252,#23253,#23254,
#23255,#23256,#23257,#23258,#23259,#23260,#23261,#23262,#23263,#23264,#23265,
#23266,#23267,#23268,#23269,#23270,#23271,#23272,#23273,#23274,#23275,#23276,
#23277,#23278,#23279,#23280,#23281,#23282,#23283,#23284,#23285,#23286,#23287,
#23288,#23289,#23290,#23291,#23292,#23293,#23294,#23295,#23296,#23297,#23298,
#23299,#23300,#23301,#23302,#23303,#23304,#23305,#23306,#23307,#23308,#23309,
#23310)),.UNSPECIFIED.,.F.,.T.,.F.,(2,2),(4,2,2,2,2,2,2,2,2,2,2,2,2,2,2,
2,2,2,2,2,2,2,2,2,2,2,2,2,2,2,2,2,2,2,2,2,2,2,2,2,2,2,2,2,2,2,2,2,2,2,2,
2,2,2,2,2,2,2,2,2,2,2,2,2,2,2,2,2,2,2,2,2,2,2,2,2,2,2,2,2,2,2,2,2,2,2,2,
2,2,2,2,2,2,2,2,2,2,2,2,2,2,2,2,2,2,2,2,2,2,2,2,2,2,4),(-3.44305291207021E-6,
1.00001612088686),(0.000602391914111579,0.000716155250734292,0.000829918587357007,
0.000943681923979721,0.00105744526060244,0.00128497193384786,0.00139873527047058,
0.00151249860709329,0.00156938027540465,0.00162626194371601,0.00174002528033872,
0.00196755195358415,0.00208131529020687,0.00219507862682958,0.00230884196345229,
0.00242260530007501,0.00253636863669772,0.00265013197332044,0.00287765864656587,
0.00299142198318858,0.0031051853198113,0.00321894865643401,0.00333271199305672,
0.00356023866630215,0.00378776533954758,0.00384464700785894,0.0039015286761703,
0.00401529201279301,0.00412905534941573,0.00424281868603844,0.00435658202266115,
0.00447034535928387,0.00458410869590658,0.0046978720325293,0.00481163536915201,
0.00492539870577473,0.00515292537902016,0.00526668871564287,0.00538045205226559,
0.00543733372057694,0.0054942153888883,0.00560797872551101,0.00583550539875644,
0.00594926873537916,0.00606303207200187,0.00617679540862459,0.0062905587452473,
0.00651808541849273,0.00674561209173816,0.00697313876498359,0.00720066543822902,
0.00731442877485173,0.00742819211147445,0.00754195544809716,0.00765571878471987,
0.00776948212134259,0.0078832454579653,0.00811077213121073,0.00822453546783345,
0.00833829880445616,0.00845206214107888,0.00856582547770159,0.00879335215094702,
0.00902087882419245,0.00913464216081516,0.00924840549743788,0.00936216883406059,
0.00947593217068331,0.00970345884392873,0.00981722218055145,0.00987410384886281,
0.00993098551717416,0.0100447488537969,0.0101585121904196,0.010386038863665,
0.0104998022002877,0.0106135655369105,0.0107273288735332,0.0108410922101559,
0.0109548555467786,0.0110686188834013,0.011182382220024,0.0112961455566467,
0.0114099088932695,0.0115236722298922,0.0116374355665149,0.0117511989031376,
0.011978725576383,0.0120924889130057,0.0122062522496285,0.0122631339179398,
0.0123200155862512,0.0124337789228739,0.0126613055961193,0.0128888322693647,
0.0130025956059875,0.0131163589426102,0.0132301222792329,0.0133438856158556,
0.013571412289101,0.0136851756257237,0.0137420572940351,0.0137989389623465,
0.0139127022989692,0.0140264656355919,0.0142539923088373,0.0144815189820827,
0.0145384006503941,0.0145952823187055,0.0147090456553282,0.0148228089919509,
0.0149365723285736,0.0150503356651963,0.015164099001819),.UNSPECIFIED.);
#12=B_SPLINE_SURFACE_WITH_KNOTS('',1,3,((#23313,#23314,#23315,#23316,#23317,
#23318,#23319,#23320,#23321,#23322,#23323,#23324,#23325,#23326,#23327,#23328,
#23329,#23330,#23331,#23332,#23333,#23334,#23335,#23336,#23337,#23338,#23339,
#23340,#23341,#23342,#23343,#23344,#23345,#23346,#23347,#23348,#23349,#23350,
#23351,#23352,#23353,#23354,#23355,#23356,#23357,#23358,#23359,#23360,#23361,
#23362,#23363,#23364,#23365,#23366,#23367,#23368,#23369,#23370,#23371,#23372,
#23373,#23374,#23375,#23376,#23377,#23378,#23379,#23380,#23381,#23382,#23383,
#23384,#23385,#23386,#23387,#23388,#23389,#23390,#23391,#23392,#23393,#23394,
#23395,#23396,#23397,#23398,#23399,#23400,#23401,#23402,#23403,#23404,#23405,
#23406,#23407,#23408,#23409,#23410,#23411,#23412,#23413,#23414,#23415,#23416,
#23417,#23418,#23419,#23420,#23421,#23422,#23423,#23424,#23425,#23426,#23427,
#23428,#23429,#23430,#23431,#23432,#23433,#23434,#23435,#23436,#23437,#23438,
#23439,#23440,#23441,#23442,#23443,#23444,#23445,#23446,#23447,#23448,#23449,
#23450,#23451,#23452,#23453,#23454,#23455,#23456,#23457,#23458,#23459,#23460,
#23461,#23462,#23463,#23464,#23465,#23466,#23467,#23468,#23469,#23470,#23471,
#23472,#23473,#23474,#23475,#23476,#23477,#23478,#23479,#23480,#23481,#23482,
#23483,#23484,#23485,#23486,#23487,#23488,#23489,#23490,#23491,#23492,#23493,
#23494,#23495,#23496,#23497,#23498,#23499,#23500,#23501,#23502,#23503,#23504,
#23505,#23506,#23507,#23508,#23509,#23510,#23511,#23512,#23513,#23514,#23515,
#23516,#23517,#23518,#23519,#23520,#23521,#23522,#23523,#23524,#23525,#23526,
#23527,#23528,#23529,#23530,#23531,#23532,#23533,#23534,#23535,#23536,#23537,
#23538),(#23539,#23540,#23541,#23542,#23543,#23544,#23545,#23546,#23547,
#23548,#23549,#23550,#23551,#23552,#23553,#23554,#23555,#23556,#23557,#23558,
#23559,#23560,#23561,#23562,#23563,#23564,#23565,#23566,#23567,#23568,#23569,
#23570,#23571,#23572,#23573,#23574,#23575,#23576,#23577,#23578,#23579,#23580,
#23581,#23582,#23583,#23584,#23585,#23586,#23587,#23588,#23589,#23590,#23591,
#23592,#23593,#23594,#23595,#23596,#23597,#23598,#23599,#23600,#23601,#23602,
#23603,#23604,#23605,#23606,#23607,#23608,#23609,#23610,#23611,#23612,#23613,
#23614,#23615,#23616,#23617,#23618,#23619,#23620,#23621,#23622,#23623,#23624,
#23625,#23626,#23627,#23628,#23629,#23630,#23631,#23632,#23633,#23634,#23635,
#23636,#23637,#23638,#23639,#23640,#23641,#23642,#23643,#23644,#23645,#23646,
#23647,#23648,#23649,#23650,#23651,#23652,#23653,#23654,#23655,#23656,#23657,
#23658,#23659,#23660,#23661,#23662,#23663,#23664,#23665,#23666,#23667,#23668,
#23669,#23670,#23671,#23672,#23673,#23674,#23675,#23676,#23677,#23678,#23679,
#23680,#23681,#23682,#23683,#23684,#23685,#23686,#23687,#23688,#23689,#23690,
#23691,#23692,#23693,#23694,#23695,#23696,#23697,#23698,#23699,#23700,#23701,
#23702,#23703,#23704,#23705,#23706,#23707,#23708,#23709,#23710,#23711,#23712,
#23713,#23714,#23715,#23716,#23717,#23718,#23719,#23720,#23721,#23722,#23723,
#23724,#23725,#23726,#23727,#23728,#23729,#23730,#23731,#23732,#23733,#23734,
#23735,#23736,#23737,#23738,#23739,#23740,#23741,#23742,#23743,#23744,#23745,
#23746,#23747,#23748,#23749,#23750,#23751,#23752,#23753,#23754,#23755,#23756,
#23757,#23758,#23759,#23760,#23761,#23762,#23763,#23764)),.UNSPECIFIED.,
 .F.,.T.,.F.,(2,2),(4,2,2,2,2,2,2,2,2,2,2,2,2,2,2,2,2,2,2,2,2,2,2,2,2,2,
2,2,2,2,2,2,2,2,2,2,2,2,2,2,2,2,2,2,2,2,2,2,2,2,2,2,2,2,2,2,2,2,2,2,2,2,
2,2,2,2,2,2,2,2,2,2,2,2,2,2,2,2,2,2,2,2,2,2,2,2,2,2,2,2,2,2,2,2,2,2,2,2,
2,2,2,2,2,2,2,2,2,2,2,2,2,2,4),(-7.24489232955387E-6,1.00002207748051),
(0.000580381745839097,0.000694149846669441,0.000751033897084613,0.000807917947499785,
0.00092168604833013,0.00103545414916048,0.00126299035082116,0.00137675845165151,
0.00149052655248185,0.0016042946533122,0.00171806275414254,0.00183183085497289,
0.00194559895580323,0.00205936705663358,0.00217313515746392,0.00228690325829427,
0.00234378730870944,0.00240067135912461,0.0026282075607853,0.00285574376244599,
0.00296951186327634,0.00308327996410668,0.00319704806493703,0.00331081616576737,
0.00353835236742806,0.00365212046825841,0.00376588856908875,0.00387965666991909,
0.00399342477074944,0.00410719287157978,0.00422096097241013,0.00444849717407082,
0.00456226527490116,0.00461914932531634,0.00467603337573151,0.00478980147656185,
0.0049035695773922,0.00513110577905289,0.00524487387988323,0.00535864198071358,
0.00547241008154392,0.00558617818237427,0.00569994628320461,0.00581371438403496,
0.0059274824848653,0.00604125058569565,0.00615501868652599,0.00621190273694116,
0.00626878678735633,0.00649632298901703,0.00672385919067771,0.00683762729150806,
0.0069513953923384,0.00706516349316875,0.00717893159399909,0.00740646779565978,
0.00752023589649013,0.00763400399732047,0.00774777209815082,0.00786154019898116,
0.00808907640064185,0.00820284450147219,0.00831661260230254,0.00837349665271771,
0.00843038070313289,0.00854414880396323,0.00877168500562392,0.00888545310645426,
0.00899922120728461,0.00911298930811495,0.0092267574089453,0.00934052550977564,
0.00945429361060599,0.00968182981226668,0.00979559791309702,0.00990936601392737,
0.0100231341147577,0.0101369022155881,0.0103644384172487,0.0105919746189094,
0.0106488586693246,0.0107057427197398,0.0108195108205701,0.0109332789214005,
0.0110470470222308,0.0112745832238915,0.0113883513247218,0.011445235375137,
0.0115021194255522,0.0116158875263825,0.0117296556272129,0.0119571918288736,
0.0120709599297039,0.0121847280305343,0.0122984961313646,0.012412264232195,
0.0125260323330253,0.0126398004338556,0.012753568534686,0.0128673366355163,
0.0129811047363467,0.013094872837177,0.0133224090388377,0.0135499452404984,
0.0137774814421591,0.0140050176438198,0.0142325538454805,0.0144600900471412,
0.0145738581479715,0.0146876262488018,0.0148013943496322,0.0149151624504625,
0.0151426986521232),.UNSPECIFIED.);
#242=SHAPE_REPRESENTATION_RELATIONSHIP('SRR','None',#33136,#269);
#269=ADVANCED_BREP_SHAPE_REPRESENTATION('',(#327),#32997);
#296=STYLED_ITEM('',(#33284),#327);
#327=MANIFOLD_SOLID_BREP('Body1',#9951);
#355=CONICAL_SURFACE('',#10763,9.2,0.785398163397462);
#356=CONICAL_SURFACE('',#10764,9.70000000000007,0.785398163397452);
#357=CONICAL_SURFACE('',#10765,10.6,0.785398163397424);
#358=CONICAL_SURFACE('',#10766,11.1,0.785398163397478);
#388=TOROIDAL_SURFACE('',#10729,11.375,0.8);
#389=TOROIDAL_SURFACE('',#10731,11.375,0.8);
#439=(
BOUNDED_SURFACE()
B_SPLINE_SURFACE(3,3,((#22265,#22266,#22267,#22268),(#22269,#22270,#22271,
#22272),(#22273,#22274,#22275,#22276),(#22277,#22278,#22279,#22280),(#22281,
#22282,#22283,#22284),(#22285,#22286,#22287,#22288),(#22289,#22290,#22291,
#22292)),.UNSPECIFIED.,.T.,.F.,.F.)
B_SPLINE_SURFACE_WITH_KNOTS((4,3,4),(4,4),(0.,0.5,1.),(-1.90675276406229E-6,
0.0446764713368579),.UNSPECIFIED.)
GEOMETRIC_REPRESENTATION_ITEM()
RATIONAL_B_SPLINE_SURFACE(((1.,1.,1.,1.),(0.333333333333333,0.333333333333333,
0.333333333333333,0.333333333333333),(0.333333333333333,0.333333333333333,
0.333333333333333,0.333333333333333),(1.,1.,1.,1.),(0.333333333333333,0.333333333333333,
0.333333333333333,0.333333333333333),(0.333333333333333,0.333333333333333,
0.333333333333333,0.333333333333333),(1.,1.,1.,1.)))
REPRESENTATION_ITEM('')
SURFACE()
);
#440=(
BOUNDED_SURFACE()
B_SPLINE_SURFACE(3,3,((#22296,#22297,#22298,#22299),(#22300,#22301,#22302,
#22303),(#22304,#22305,#22306,#22307),(#22308,#22309,#22310,#22311),(#22312,
#22313,#22314,#22315),(#22316,#22317,#22318,#22319),(#22320,#22321,#22322,
#22323)),.UNSPECIFIED.,.T.,.F.,.F.)
B_SPLINE_SURFACE_WITH_KNOTS((4,3,4),(4,4),(0.,0.5,1.),(0.955323528663142,
1.00000238460506),.UNSPECIFIED.)
GEOMETRIC_REPRESENTATION_ITEM()
RATIONAL_B_SPLINE_SURFACE(((1.,1.,1.,0.999999999999999),(0.333333333333333,
0.333333333333333,0.333333333333333,0.333333333333333),(0.333333333333333,
0.333333333333333,0.333333333333333,0.333333333333333),(1.,1.,1.,0.999999999999999),
(0.333333333333333,0.333333333333333,0.333333333333333,0.333333333333333),
(0.333333333333333,0.333333333333333,0.333333333333333,0.333333333333333),
(1.,1.,1.,0.999999999999999)))
REPRESENTATION_ITEM('')
SURFACE()
);
#441=(
BOUNDED_SURFACE()
B_SPLINE_SURFACE(3,3,((#22324,#22325,#22326,#22327),(#22328,#22329,#22330,
#22331),(#22332,#22333,#22334,#22335),(#22336,#22337,#22338,#22339),(#22340,
#22341,#22342,#22343),(#22344,#22345,#22346,#22347),(#22348,#22349,#22350,
#22351)),.UNSPECIFIED.,.T.,.F.,.F.)
B_SPLINE_SURFACE_WITH_KNOTS((4,3,4),(4,4),(0.,0.5,1.),(-1.90675276411689E-6,
0.044676471336858),.UNSPECIFIED.)
GEOMETRIC_REPRESENTATION_ITEM()
RATIONAL_B_SPLINE_SURFACE(((0.999999999999999,1.,1.,1.),(0.333333333333333,
0.333333333333333,0.333333333333333,0.333333333333333),(0.333333333333333,
0.333333333333333,0.333333333333333,0.333333333333333),(0.999999999999999,
1.,1.,1.),(0.333333333333333,0.333333333333333,0.333333333333333,0.333333333333333),
(0.333333333333333,0.333333333333333,0.333333333333333,0.333333333333333),
(0.999999999999999,1.,1.,1.)))
REPRESENTATION_ITEM('')
SURFACE()
);
#442=(
BOUNDED_SURFACE()
B_SPLINE_SURFACE(3,3,((#22355,#22356,#22357,#22358),(#22359,#22360,#22361,
#22362),(#22363,#22364,#22365,#22366),(#22367,#22368,#22369,#22370),(#22371,
#22372,#22373,#22374),(#22375,#22376,#22377,#22378),(#22379,#22380,#22381,
#22382)),.UNSPECIFIED.,.T.,.F.,.F.)
B_SPLINE_SURFACE_WITH_KNOTS((4,3,4),(4,4),(0.,0.5,1.),(0.955323528663142,
1.00000238460506),.UNSPECIFIED.)
GEOMETRIC_REPRESENTATION_ITEM()
RATIONAL_B_SPLINE_SURFACE(((1.,1.,1.,1.),(0.333333333333333,0.333333333333333,
0.333333333333333,0.333333333333333),(0.333333333333333,0.333333333333333,
0.333333333333333,0.333333333333333),(1.,1.,1.,1.),(0.333333333333333,0.333333333333333,
0.333333333333333,0.333333333333333),(0.333333333333333,0.333333333333333,
0.333333333333333,0.333333333333333),(1.,1.,1.,1.)))
REPRESENTATION_ITEM('')
SURFACE()
);
#443=(
BOUNDED_SURFACE()
B_SPLINE_SURFACE(3,3,((#22383,#22384,#22385,#22386),(#22387,#22388,#22389,
#22390),(#22391,#22392,#22393,#22394),(#22395,#22396,#22397,#22398),(#22399,
#22400,#22401,#22402),(#22403,#22404,#22405,#22406),(#22407,#22408,#22409,
#22410)),.UNSPECIFIED.,.T.,.F.,.F.)
B_SPLINE_SURFACE_WITH_KNOTS((4,3,4),(4,4),(0.,0.5,1.),(-1.90675276402769E-6,
0.044676471336858),.UNSPECIFIED.)
GEOMETRIC_REPRESENTATION_ITEM()
RATIONAL_B_SPLINE_SURFACE(((1.,1.,1.,1.),(0.333333333333334,0.333333333333333,
0.333333333333333,0.333333333333333),(0.333333333333334,0.333333333333333,
0.333333333333333,0.333333333333333),(1.,1.,1.,1.),(0.333333333333334,0.333333333333333,
0.333333333333333,0.333333333333333),(0.333333333333334,0.333333333333333,
0.333333333333333,0.333333333333333),(1.,1.,1.,1.)))
REPRESENTATION_ITEM('')
SURFACE()
);
#444=(
BOUNDED_SURFACE()
B_SPLINE_SURFACE(3,3,((#22414,#22415,#22416,#22417),(#22418,#22419,#22420,
#22421),(#22422,#22423,#22424,#22425),(#22426,#22427,#22428,#22429),(#22430,
#22431,#22432,#22433),(#22434,#22435,#22436,#22437),(#22438,#22439,#22440,
#22441)),.UNSPECIFIED.,.T.,.F.,.F.)
B_SPLINE_SURFACE_WITH_KNOTS((4,3,4),(4,4),(0.,0.5,1.),(0.955323528663142,
1.00000238460506),.UNSPECIFIED.)
GEOMETRIC_REPRESENTATION_ITEM()
RATIONAL_B_SPLINE_SURFACE(((1.,1.,1.,1.),(0.333333333333333,0.333333333333333,
0.333333333333333,0.333333333333333),(0.333333333333333,0.333333333333333,
0.333333333333333,0.333333333333333),(1.,1.,1.,1.),(0.333333333333333,0.333333333333333,
0.333333333333333,0.333333333333333),(0.333333333333333,0.333333333333333,
0.333333333333333,0.333333333333333),(1.,1.,1.,1.)))
REPRESENTATION_ITEM('')
SURFACE()
);
#445=(
BOUNDED_SURFACE()
B_SPLINE_SURFACE(3,3,((#22442,#22443,#22444,#22445),(#22446,#22447,#22448,
#22449),(#22450,#22451,#22452,#22453),(#22454,#22455,#22456,#22457),(#22458,
#22459,#22460,#22461),(#22462,#22463,#22464,#22465),(#22466,#22467,#22468,
#22469)),.UNSPECIFIED.,.T.,.F.,.F.)
B_SPLINE_SURFACE_WITH_KNOTS((4,3,4),(4,4),(0.,0.5,1.),(-1.90675276440842E-6,
0.0446764713368579),.UNSPECIFIED.)
GEOMETRIC_REPRESENTATION_ITEM()
RATIONAL_B_SPLINE_SURFACE(((1.,1.,1.,1.),(0.333333333333333,0.333333333333333,
0.333333333333333,0.333333333333333),(0.333333333333333,0.333333333333333,
0.333333333333333,0.333333333333333),(1.,1.,1.,1.),(0.333333333333333,0.333333333333333,
0.333333333333333,0.333333333333333),(0.333333333333333,0.333333333333333,
0.333333333333333,0.333333333333333),(1.,1.,1.,1.)))
REPRESENTATION_ITEM('')
SURFACE()
);
#446=(
BOUNDED_SURFACE()
B_SPLINE_SURFACE(3,3,((#22473,#22474,#22475,#22476),(#22477,#22478,#22479,
#22480),(#22481,#22482,#22483,#22484),(#22485,#22486,#22487,#22488),(#22489,
#22490,#22491,#22492),(#22493,#22494,#22495,#22496),(#22497,#22498,#22499,
#22500)),.UNSPECIFIED.,.T.,.F.,.F.)
B_SPLINE_SURFACE_WITH_KNOTS((4,3,4),(4,4),(0.,0.5,1.),(0.955323528663142,
1.00000238460506),.UNSPECIFIED.)
GEOMETRIC_REPRESENTATION_ITEM()
RATIONAL_B_SPLINE_SURFACE(((1.,1.,1.,1.),(0.333333333333333,0.333333333333333,
0.333333333333333,0.333333333333333),(0.333333333333333,0.333333333333333,
0.333333333333333,0.333333333333333),(1.,1.,1.,1.),(0.333333333333333,0.333333333333333,
0.333333333333333,0.333333333333333),(0.333333333333333,0.333333333333333,
0.333333333333333,0.333333333333333),(1.,1.,1.,1.)))
REPRESENTATION_ITEM('')
SURFACE()
);
#447=(
BOUNDED_SURFACE()
B_SPLINE_SURFACE(3,3,((#22501,#22502,#22503,#22504),(#22505,#22506,#22507,
#22508),(#22509,#22510,#22511,#22512),(#22513,#22514,#22515,#22516),(#22517,
#22518,#22519,#22520),(#22521,#22522,#22523,#22524),(#22525,#22526,#22527,
#22528)),.UNSPECIFIED.,.T.,.F.,.F.)
B_SPLINE_SURFACE_WITH_KNOTS((4,3,4),(4,4),(0.,0.5,1.),(-1.90675276415042E-6,
0.0446764713368579),.UNSPECIFIED.)
GEOMETRIC_REPRESENTATION_ITEM()
RATIONAL_B_SPLINE_SURFACE(((1.,1.,1.,1.),(0.333333333333333,0.333333333333333,
0.333333333333333,0.333333333333333),(0.333333333333333,0.333333333333333,
0.333333333333333,0.333333333333333),(1.,1.,1.,1.),(0.333333333333333,0.333333333333333,
0.333333333333333,0.333333333333333),(0.333333333333333,0.333333333333333,
0.333333333333333,0.333333333333333),(1.,1.,1.,1.)))
REPRESENTATION_ITEM('')
SURFACE()
);
#448=(
BOUNDED_SURFACE()
B_SPLINE_SURFACE(3,3,((#22532,#22533,#22534,#22535),(#22536,#22537,#22538,
#22539),(#22540,#22541,#22542,#22543),(#22544,#22545,#22546,#22547),(#22548,
#22549,#22550,#22551),(#22552,#22553,#22554,#22555),(#22556,#22557,#22558,
#22559)),.UNSPECIFIED.,.T.,.F.,.F.)
B_SPLINE_SURFACE_WITH_KNOTS((4,3,4),(4,4),(0.,0.5,1.),(0.955323528663142,
1.00000238460506),.UNSPECIFIED.)
GEOMETRIC_REPRESENTATION_ITEM()
RATIONAL_B_SPLINE_SURFACE(((1.,1.,1.,1.),(0.333333333333333,0.333333333333333,
0.333333333333333,0.333333333333333),(0.333333333333333,0.333333333333333,
0.333333333333333,0.333333333333333),(1.,1.,1.,1.),(0.333333333333333,0.333333333333333,
0.333333333333333,0.333333333333333),(0.333333333333333,0.333333333333333,
0.333333333333333,0.333333333333333),(1.,1.,1.,1.)))
REPRESENTATION_ITEM('')
SURFACE()
);
#449=(
BOUNDED_SURFACE()
B_SPLINE_SURFACE(3,3,((#22560,#22561,#22562,#22563),(#22564,#22565,#22566,
#22567),(#22568,#22569,#22570,#22571),(#22572,#22573,#22574,#22575),(#22576,
#22577,#22578,#22579),(#22580,#22581,#22582,#22583),(#22584,#22585,#22586,
#22587)),.UNSPECIFIED.,.T.,.F.,.F.)
B_SPLINE_SURFACE_WITH_KNOTS((4,3,4),(4,4),(0.,0.5,1.),(-1.90675276405256E-6,
0.0446764713368579),.UNSPECIFIED.)
GEOMETRIC_REPRESENTATION_ITEM()
RATIONAL_B_SPLINE_SURFACE(((1.,1.,1.,1.),(0.333333333333333,0.333333333333333,
0.333333333333333,0.333333333333333),(0.333333333333333,0.333333333333333,
0.333333333333333,0.333333333333333),(1.,1.,1.,1.),(0.333333333333333,0.333333333333333,
0.333333333333333,0.333333333333333),(0.333333333333333,0.333333333333333,
0.333333333333333,0.333333333333333),(1.,1.,1.,1.)))
REPRESENTATION_ITEM('')
SURFACE()
);
#450=(
BOUNDED_SURFACE()
B_SPLINE_SURFACE(3,3,((#22591,#22592,#22593,#22594),(#22595,#22596,#22597,
#22598),(#22599,#22600,#22601,#22602),(#22603,#22604,#22605,#22606),(#22607,
#22608,#22609,#22610),(#22611,#22612,#22613,#22614),(#22615,#22616,#22617,
#22618)),.UNSPECIFIED.,.T.,.F.,.F.)
B_SPLINE_SURFACE_WITH_KNOTS((4,3,4),(4,4),(0.,0.5,1.),(0.955323528663142,
1.00000238460506),.UNSPECIFIED.)
GEOMETRIC_REPRESENTATION_ITEM()
RATIONAL_B_SPLINE_SURFACE(((1.,1.,1.,0.999999999999999),(0.333333333333333,
0.333333333333333,0.333333333333333,0.333333333333333),(0.333333333333333,
0.333333333333333,0.333333333333333,0.333333333333333),(1.,1.,1.,0.999999999999999),
(0.333333333333333,0.333333333333333,0.333333333333333,0.333333333333333),
(0.333333333333333,0.333333333333333,0.333333333333333,0.333333333333333),
(1.,1.,1.,0.999999999999999)))
REPRESENTATION_ITEM('')
SURFACE()
);
#451=(
BOUNDED_SURFACE()
B_SPLINE_SURFACE(3,3,((#22619,#22620,#22621,#22622),(#22623,#22624,#22625,
#22626),(#22627,#22628,#22629,#22630),(#22631,#22632,#22633,#22634),(#22635,
#22636,#22637,#22638),(#22639,#22640,#22641,#22642),(#22643,#22644,#22645,
#22646)),.UNSPECIFIED.,.T.,.F.,.F.)
B_SPLINE_SURFACE_WITH_KNOTS((4,3,4),(4,4),(0.,0.5,1.),(-1.90675276426259E-6,
0.0446764713368579),.UNSPECIFIED.)
GEOMETRIC_REPRESENTATION_ITEM()
RATIONAL_B_SPLINE_SURFACE(((1.,1.,1.,1.),(0.333333333333333,0.333333333333333,
0.333333333333333,0.333333333333333),(0.333333333333333,0.333333333333333,
0.333333333333333,0.333333333333333),(1.,1.,1.,1.),(0.333333333333333,0.333333333333333,
0.333333333333333,0.333333333333333),(0.333333333333333,0.333333333333333,
0.333333333333333,0.333333333333333),(1.,1.,1.,1.)))
REPRESENTATION_ITEM('')
SURFACE()
);
#452=(
BOUNDED_SURFACE()
B_SPLINE_SURFACE(3,3,((#22650,#22651,#22652,#22653),(#22654,#22655,#22656,
#22657),(#22658,#22659,#22660,#22661),(#22662,#22663,#22664,#22665),(#22666,
#22667,#22668,#22669),(#22670,#22671,#22672,#22673),(#22674,#22675,#22676,
#22677)),.UNSPECIFIED.,.T.,.F.,.F.)
B_SPLINE_SURFACE_WITH_KNOTS((4,3,4),(4,4),(0.,0.5,1.),(0.955323528663142,
1.00000238460506),.UNSPECIFIED.)
GEOMETRIC_REPRESENTATION_ITEM()
RATIONAL_B_SPLINE_SURFACE(((1.,1.,1.,1.),(0.333333333333333,0.333333333333333,
0.333333333333333,0.333333333333333),(0.333333333333333,0.333333333333333,
0.333333333333333,0.333333333333333),(1.,1.,1.,1.),(0.333333333333333,0.333333333333333,
0.333333333333333,0.333333333333333),(0.333333333333333,0.333333333333333,
0.333333333333333,0.333333333333333),(1.,1.,1.,1.)))
REPRESENTATION_ITEM('')
SURFACE()
);
#453=(
BOUNDED_SURFACE()
B_SPLINE_SURFACE(3,3,((#22678,#22679,#22680,#22681),(#22682,#22683,#22684,
#22685),(#22686,#22687,#22688,#22689),(#22690,#22691,#22692,#22693),(#22694,
#22695,#22696,#22697),(#22698,#22699,#22700,#22701),(#22702,#22703,#22704,
#22705)),.UNSPECIFIED.,.T.,.F.,.F.)
B_SPLINE_SURFACE_WITH_KNOTS((4,3,4),(4,4),(0.,0.5,1.),(-1.90675276424112E-6,
0.0446764713368579),.UNSPECIFIED.)
GEOMETRIC_REPRESENTATION_ITEM()
RATIONAL_B_SPLINE_SURFACE(((1.,1.,1.,1.),(0.333333333333333,0.333333333333333,
0.333333333333333,0.333333333333333),(0.333333333333333,0.333333333333333,
0.333333333333333,0.333333333333333),(1.,1.,1.,1.),(0.333333333333333,0.333333333333333,
0.333333333333333,0.333333333333333),(0.333333333333333,0.333333333333333,
0.333333333333333,0.333333333333333),(1.,1.,1.,1.)))
REPRESENTATION_ITEM('')
SURFACE()
);
#454=(
BOUNDED_SURFACE()
B_SPLINE_SURFACE(3,3,((#22709,#22710,#22711,#22712),(#22713,#22714,#22715,
#22716),(#22717,#22718,#22719,#22720),(#22721,#22722,#22723,#22724),(#22725,
#22726,#22727,#22728),(#22729,#22730,#22731,#22732),(#22733,#22734,#22735,
#22736)),.UNSPECIFIED.,.T.,.F.,.F.)
B_SPLINE_SURFACE_WITH_KNOTS((4,3,4),(4,4),(0.,0.5,1.),(0.955323528663142,
1.00000238460506),.UNSPECIFIED.)
GEOMETRIC_REPRESENTATION_ITEM()
RATIONAL_B_SPLINE_SURFACE(((1.,1.,1.,0.999999999999999),(0.333333333333333,
0.333333333333333,0.333333333333333,0.333333333333333),(0.333333333333333,
0.333333333333333,0.333333333333333,0.333333333333333),(1.,1.,1.,0.999999999999999),
(0.333333333333333,0.333333333333333,0.333333333333333,0.333333333333333),
(0.333333333333333,0.333333333333333,0.333333333333333,0.333333333333333),
(1.,1.,1.,0.999999999999999)))
REPRESENTATION_ITEM('')
SURFACE()
);
#455=(
BOUNDED_SURFACE()
B_SPLINE_SURFACE(3,3,((#22737,#22738,#22739,#22740),(#22741,#22742,#22743,
#22744),(#22745,#22746,#22747,#22748),(#22749,#22750,#22751,#22752),(#22753,
#22754,#22755,#22756),(#22757,#22758,#22759,#22760),(#22761,#22762,#22763,
#22764)),.UNSPECIFIED.,.T.,.F.,.F.)
B_SPLINE_SURFACE_WITH_KNOTS((4,3,4),(4,4),(0.,0.5,1.),(-1.90675276443097E-6,
0.0446764713368579),.UNSPECIFIED.)
GEOMETRIC_REPRESENTATION_ITEM()
RATIONAL_B_SPLINE_SURFACE(((1.,1.,1.,1.),(0.333333333333333,0.333333333333333,
0.333333333333333,0.333333333333333),(0.333333333333333,0.333333333333333,
0.333333333333333,0.333333333333333),(1.,1.,1.,1.),(0.333333333333333,0.333333333333333,
0.333333333333333,0.333333333333333),(0.333333333333333,0.333333333333333,
0.333333333333333,0.333333333333333),(1.,1.,1.,1.)))
REPRESENTATION_ITEM('')
SURFACE()
);
#456=(
BOUNDED_SURFACE()
B_SPLINE_SURFACE(3,3,((#22768,#22769,#22770,#22771),(#22772,#22773,#22774,
#22775),(#22776,#22777,#22778,#22779),(#22780,#22781,#22782,#22783),(#22784,
#22785,#22786,#22787),(#22788,#22789,#22790,#22791),(#22792,#22793,#22794,
#22795)),.UNSPECIFIED.,.T.,.F.,.F.)
B_SPLINE_SURFACE_WITH_KNOTS((4,3,4),(4,4),(0.,0.5,1.),(0.955323528663142,
1.00000238460506),.UNSPECIFIED.)
GEOMETRIC_REPRESENTATION_ITEM()
RATIONAL_B_SPLINE_SURFACE(((1.,1.,1.,1.),(0.333333333333333,0.333333333333333,
0.333333333333333,0.333333333333333),(0.333333333333333,0.333333333333333,
0.333333333333333,0.333333333333333),(1.,1.,1.,1.),(0.333333333333333,0.333333333333333,
0.333333333333333,0.333333333333333),(0.333333333333333,0.333333333333333,
0.333333333333333,0.333333333333333),(1.,1.,1.,1.)))
REPRESENTATION_ITEM('')
SURFACE()
);
#457=(
BOUNDED_SURFACE()
B_SPLINE_SURFACE(3,3,((#22796,#22797,#22798,#22799),(#22800,#22801,#22802,
#22803),(#22804,#22805,#22806,#22807),(#22808,#22809,#22810,#22811),(#22812,
#22813,#22814,#22815),(#22816,#22817,#22818,#22819),(#22820,#22821,#22822,
#22823)),.UNSPECIFIED.,.T.,.F.,.F.)
B_SPLINE_SURFACE_WITH_KNOTS((4,3,4),(4,4),(0.,0.5,1.),(-1.90675276401703E-6,
0.0446764713368579),.UNSPECIFIED.)
GEOMETRIC_REPRESENTATION_ITEM()
RATIONAL_B_SPLINE_SURFACE(((0.999999999999999,1.,1.,1.),(0.333333333333333,
0.333333333333333,0.333333333333333,0.333333333333333),(0.333333333333333,
0.333333333333333,0.333333333333333,0.333333333333333),(0.999999999999999,
1.,1.,1.),(0.333333333333333,0.333333333333333,0.333333333333333,0.333333333333333),
(0.333333333333333,0.333333333333333,0.333333333333333,0.333333333333333),
(0.999999999999999,1.,1.,1.)))
REPRESENTATION_ITEM('')
SURFACE()
);
#458=(
BOUNDED_SURFACE()
B_SPLINE_SURFACE(3,3,((#22827,#22828,#22829,#22830),(#22831,#22832,#22833,
#22834),(#22835,#22836,#22837,#22838),(#22839,#22840,#22841,#22842),(#22843,
#22844,#22845,#22846),(#22847,#22848,#22849,#22850),(#22851,#22852,#22853,
#22854)),.UNSPECIFIED.,.T.,.F.,.F.)
B_SPLINE_SURFACE_WITH_KNOTS((4,3,4),(4,4),(0.,0.5,1.),(0.955323528663142,
1.00000238460506),.UNSPECIFIED.)
GEOMETRIC_REPRESENTATION_ITEM()
RATIONAL_B_SPLINE_SURFACE(((1.,1.,1.,1.),(0.333333333333333,0.333333333333333,
0.333333333333333,0.333333333333333),(0.333333333333333,0.333333333333333,
0.333333333333333,0.333333333333333),(1.,1.,1.,1.),(0.333333333333333,0.333333333333333,
0.333333333333333,0.333333333333333),(0.333333333333333,0.333333333333333,
0.333333333333333,0.333333333333333),(1.,1.,1.,1.)))
REPRESENTATION_ITEM('')
SURFACE()
);
#496=FACE_BOUND('',#1849,.T.);
#497=FACE_BOUND('',#1850,.T.);
#498=FACE_BOUND('',#1851,.T.);
#499=FACE_BOUND('',#1852,.T.);
#500=FACE_BOUND('',#1853,.T.);
#501=FACE_BOUND('',#1854,.T.);
#502=FACE_BOUND('',#1855,.T.);
#503=FACE_BOUND('',#1856,.T.);
#504=FACE_BOUND('',#1857,.T.);
#505=FACE_BOUND('',#1859,.T.);
#506=FACE_BOUND('',#1861,.T.);
#507=FACE_BOUND('',#1863,.T.);
#508=FACE_BOUND('',#1865,.T.);
#509=FACE_BOUND('',#1867,.T.);
#510=FACE_BOUND('',#1868,.T.);
#581=B_SPLINE_CURVE_WITH_KNOTS('',3,(#21100,#21101,#21102,#21103,#21104,
#21105,#21106,#21107,#21108,#21109,#21110,#21111,#21112,#21113,#21114,#21115,
#21116,#21117),.UNSPECIFIED.,.F.,.F.,(4,2,2,2,2,2,2,2,4),(0.,0.0591297066253043,
0.101286062949422,0.137517711401243,0.179810134914136,0.212974667045344,
0.229441128614405,0.242688203236853,0.242937404635999),.UNSPECIFIED.);
#582=B_SPLINE_CURVE_WITH_KNOTS('',3,(#21121,#21122,#21123,#21124,#21125,
#21126,#21127,#21128,#21129,#21130,#21131,#21132,#21133,#21134,#21135,#21136),
 .UNSPECIFIED.,.F.,.F.,(4,2,2,2,2,2,2,4),(0.242619551178519,0.255524854267213,
0.271696804230175,0.303396718536254,0.343221718357041,0.379813718288485,
0.420371936847968,0.486941959854264),.UNSPECIFIED.);
#583=B_SPLINE_CURVE_WITH_KNOTS('',3,(#21141,#21142,#21143,#21144,#21145,
#21146,#21147,#21148,#21149,#21150,#21151,#21152,#21153,#21154,#21155,#21156,
#21157,#21158),.UNSPECIFIED.,.F.,.F.,(4,2,2,2,2,2,2,2,4),(0.,0.0625576155549603,
0.103705894629019,0.140114223826818,0.180905683903664,0.212584741865507,
0.229068999283201,0.242305782037659,0.242619551178519),.UNSPECIFIED.);
#584=B_SPLINE_CURVE_WITH_KNOTS('',3,(#21161,#21162,#21163,#21164,#21165,
#21166,#21167,#21168,#21169,#21170,#21171,#21172,#21173,#21174,#21175,#21176),
 .UNSPECIFIED.,.F.,.F.,(4,2,2,2,2,2,2,4),(0.242937404635999,0.255921391403813,
0.272139917047041,0.304029069944799,0.344156916496348,0.380728183501685,
0.421482205148501,0.485707929360947),.UNSPECIFIED.);
#585=B_SPLINE_CURVE_WITH_KNOTS('',3,(#21179,#21180,#21181,#21182,#21183,
#21184,#21185,#21186,#21187,#21188,#21189,#21190,#21191,#21192,#21193,#21194,
#21195,#21196,#21197,#21198,#21199,#21200,#21201,#21202,#21203,#21204,#21205,
#21206,#21207,#21208),.UNSPECIFIED.,.F.,.F.,(4,2,2,2,2,2,2,2,2,2,2,2,2,
2,4),(0.,0.0591297066251443,0.10128606294921,0.137517711400911,0.179810134913968,
0.212974667045338,0.22944112861441,0.242688203236827,0.255921391403934,
0.272139917047388,0.304029069945497,0.3441569164974,0.380728183503124,0.421482205150273,
0.485707929363829),.UNSPECIFIED.);
#586=B_SPLINE_CURVE_WITH_KNOTS('',3,(#21212,#21213,#21214,#21215,#21216,
#21217,#21218,#21219,#21220,#21221,#21222,#21223,#21224,#21225,#21226,#21227,
#21228,#21229,#21230,#21231,#21232,#21233,#21234,#21235,#21236,#21237,#21238,
#21239,#21240,#21241),.UNSPECIFIED.,.F.,.F.,(4,2,2,2,2,2,2,2,2,2,2,2,2,
2,4),(0.,0.0625576155550425,0.103705894629037,0.140114223826745,0.180905683903574,
0.212584741865456,0.229068999283225,0.242305782037766,0.255524854267145,
0.271696804229871,0.303396718535534,0.343221718355779,0.379813718286607,
0.420371936845398,0.486941959850739),.UNSPECIFIED.);
#587=B_SPLINE_CURVE_WITH_KNOTS('',3,(#21245,#21246,#21247,#21248,#21249,
#21250,#21251,#21252,#21253,#21254,#21255,#21256,#21257,#21258,#21259,#21260,
#21261,#21262,#21263,#21264,#21265,#21266,#21267,#21268,#21269,#21270,#21271,
#21272,#21273,#21274),.UNSPECIFIED.,.F.,.F.,(4,2,2,2,2,2,2,2,2,2,2,2,2,
2,4),(0.,0.0591297066252864,0.101286062949393,0.137517711401177,0.179810134914117,
0.212974667045378,0.229441128614418,0.242688203236773,0.255921391403745,
0.272139917047061,0.304029069945025,0.344156916496804,0.380728183502349,
0.421482205149371,0.48570792936228),.UNSPECIFIED.);
#588=B_SPLINE_CURVE_WITH_KNOTS('',3,(#21278,#21279,#21280,#21281,#21282,
#21283,#21284,#21285,#21286,#21287,#21288,#21289,#21290,#21291,#21292,#21293,
#21294,#21295,#21296,#21297,#21298,#21299,#21300,#21301,#21302,#21303,#21304,
#21305,#21306,#21307),.UNSPECIFIED.,.F.,.F.,(4,2,2,2,2,2,2,2,2,2,2,2,2,
2,4),(0.,0.0625576155549716,0.103705894629009,0.140114223826776,0.180905683903617,
0.212584741865472,0.22906899928318,0.242305782037708,0.255524854267209,
0.271696804230295,0.303396718536698,0.343221718357867,0.379813718289666,
0.420371936849526,0.486941959856497),.UNSPECIFIED.);
#589=B_SPLINE_CURVE_WITH_KNOTS('',3,(#21311,#21312,#21313,#21314,#21315,
#21316,#21317,#21318,#21319,#21320,#21321,#21322,#21323,#21324,#21325,#21326,
#21327,#21328,#21329,#21330,#21331,#21332,#21333,#21334,#21335,#21336,#21337,
#21338,#21339,#21340),.UNSPECIFIED.,.F.,.F.,(4,2,2,2,2,2,2,2,2,2,2,2,2,
2,4),(0.,0.0591297066254632,0.101286062949567,0.137517711401381,0.179810134914222,
0.212974667045435,0.229441128614477,0.242688203236797,0.255921391403683,
0.272139917046899,0.304029069944637,0.344156916496141,0.380728183501339,
0.421482205148018,0.485707929360225),.UNSPECIFIED.);
#590=B_SPLINE_CURVE_WITH_KNOTS('',3,(#21344,#21345,#21346,#21347,#21348,
#21349,#21350,#21351,#21352,#21353,#21354,#21355,#21356,#21357,#21358,#21359,
#21360,#21361,#21362,#21363,#21364,#21365,#21366,#21367,#21368,#21369,#21370,
#21371,#21372,#21373),.UNSPECIFIED.,.F.,.F.,(4,2,2,2,2,2,2,2,2,2,2,2,2,
2,4),(0.,0.0625576155549251,0.103705894629016,0.140114223826815,0.180905683903673,
0.212584741865495,0.229068999283176,0.242305782037738,0.255524854267565,
0.271696804230953,0.303396718537859,0.343221718359601,0.379813718291938,
0.420371936852435,0.486941959860366),.UNSPECIFIED.);
#591=B_SPLINE_CURVE_WITH_KNOTS('',3,(#21377,#21378,#21379,#21380,#21381,
#21382,#21383,#21384,#21385,#21386,#21387,#21388,#21389,#21390,#21391,#21392,
#21393,#21394,#21395,#21396,#21397,#21398,#21399,#21400,#21401,#21402,#21403,
#21404,#21405,#21406),.UNSPECIFIED.,.F.,.F.,(4,2,2,2,2,2,2,2,2,2,2,2,2,
2,4),(0.,0.0591297066254656,0.101286062949478,0.137517711401217,0.179810134914112,
0.212974667045368,0.229441128614476,0.242688203236961,0.255921391404029,
0.272139917047424,0.30402906994545,0.344156916497263,0.38072818350272,0.421482205149666,
0.485707929362617),.UNSPECIFIED.);
#592=B_SPLINE_CURVE_WITH_KNOTS('',3,(#21410,#21411,#21412,#21413,#21414,
#21415,#21416,#21417,#21418,#21419,#21420,#21421,#21422,#21423,#21424,#21425,
#21426,#21427,#21428,#21429,#21430,#21431,#21432,#21433,#21434,#21435,#21436,
#21437,#21438,#21439),.UNSPECIFIED.,.F.,.F.,(4,2,2,2,2,2,2,2,2,2,2,2,2,
2,4),(0.,0.0625576155549631,0.103705894628963,0.140114223826657,0.18090568390353,
0.212584741865409,0.229068999283161,0.242305782037703,0.255524854267285,
0.271696804230179,0.303396718536041,0.343221718356524,0.379813718287668,
0.420371936846778,0.486941959852788),.UNSPECIFIED.);
#593=B_SPLINE_CURVE_WITH_KNOTS('',3,(#21443,#21444,#21445,#21446,#21447,
#21448,#21449,#21450,#21451,#21452,#21453,#21454,#21455,#21456,#21457,#21458,
#21459,#21460,#21461,#21462,#21463,#21464,#21465,#21466,#21467,#21468,#21469,
#21470,#21471,#21472),.UNSPECIFIED.,.F.,.F.,(4,2,2,2,2,2,2,2,2,2,2,2,2,
2,4),(0.,0.059129706625303,0.101286062949409,0.137517711401222,0.179810134914118,
0.212974667045327,0.229441128614365,0.242688203236767,0.255921391403782,
0.272139917047142,0.304029069945151,0.344156916497017,0.38072818350263,
0.421482205149739,0.48570792936266),.UNSPECIFIED.);
#594=B_SPLINE_CURVE_WITH_KNOTS('',3,(#21476,#21477,#21478,#21479,#21480,
#21481,#21482,#21483,#21484,#21485,#21486,#21487,#21488,#21489,#21490,#21491,
#21492,#21493,#21494,#21495,#21496,#21497,#21498,#21499,#21500,#21501,#21502,
#21503,#21504,#21505),.UNSPECIFIED.,.F.,.F.,(4,2,2,2,2,2,2,2,2,2,2,2,2,
2,4),(0.,0.0625576155549589,0.103705894629042,0.140114223826835,0.180905683903654,
0.212584741865466,0.229068999283114,0.242305782037558,0.255524854267162,
0.271696804230271,0.303396718536633,0.34322171835775,0.379813718289504,
0.420371936849334,0.486941959856202),.UNSPECIFIED.);
#595=B_SPLINE_CURVE_WITH_KNOTS('',3,(#21509,#21510,#21511,#21512,#21513,
#21514,#21515,#21516,#21517,#21518,#21519,#21520,#21521,#21522,#21523,#21524,
#21525,#21526,#21527,#21528,#21529,#21530,#21531,#21532,#21533,#21534,#21535,
#21536,#21537,#21538),.UNSPECIFIED.,.F.,.F.,(4,2,2,2,2,2,2,2,2,2,2,2,2,
2,4),(0.,0.0591297066253938,0.101286062949474,0.137517711401263,0.179810134914156,
0.212974667045388,0.229441128614457,0.242688203236794,0.255921391403719,
0.272139917047063,0.304029069945052,0.344156916496837,0.380728183502336,
0.421482205149336,0.485707929362192),.UNSPECIFIED.);
#596=B_SPLINE_CURVE_WITH_KNOTS('',3,(#21542,#21543,#21544,#21545,#21546,
#21547,#21548,#21549,#21550,#21551,#21552,#21553,#21554,#21555,#21556,#21557,
#21558,#21559,#21560,#21561,#21562,#21563,#21564,#21565,#21566,#21567,#21568,
#21569,#21570,#21571),.UNSPECIFIED.,.F.,.F.,(4,2,2,2,2,2,2,2,2,2,2,2,2,
2,4),(0.,0.0625576155548974,0.103705894628924,0.140114223826715,0.180905683903631,
0.212584741865498,0.229068999283233,0.242305782037817,0.255524854267415,
0.271696804230564,0.303396718537098,0.343221718358438,0.379813718290417,
0.420371936850418,0.486941959857704),.UNSPECIFIED.);
#597=B_SPLINE_CURVE_WITH_KNOTS('',3,(#21575,#21576,#21577,#21578,#21579,
#21580,#21581,#21582,#21583,#21584,#21585,#21586,#21587,#21588,#21589,#21590,
#21591,#21592,#21593,#21594,#21595,#21596,#21597,#21598,#21599,#21600,#21601,
#21602,#21603,#21604),.UNSPECIFIED.,.F.,.F.,(4,2,2,2,2,2,2,2,2,2,2,2,2,
2,4),(0.,0.0591297066250036,0.101286062949091,0.137517711400804,0.179810134913944,
0.21297466704533,0.229441128614477,0.242688203236995,0.255921391404044,
0.272139917047368,0.304029069945175,0.344156916496678,0.380728183502119,
0.421482205148957,0.485707929362086),.UNSPECIFIED.);
#598=B_SPLINE_CURVE_WITH_KNOTS('',3,(#21608,#21609,#21610,#21611,#21612,
#21613,#21614,#21615,#21616,#21617,#21618,#21619,#21620,#21621,#21622,#21623,
#21624,#21625,#21626,#21627,#21628,#21629,#21630,#21631,#21632,#21633,#21634,
#21635,#21636,#21637),.UNSPECIFIED.,.F.,.F.,(4,2,2,2,2,2,2,2,2,2,2,2,2,
2,4),(0.,0.0625576155550406,0.103705894629032,0.140114223826711,0.18090568390349,
0.21258474186536,0.229068999283064,0.242305782037584,0.255524854267104,
0.271696804230055,0.303396718536132,0.343221718356878,0.379813718288151,
0.420371936847442,0.486941959853629),.UNSPECIFIED.);
#599=B_SPLINE_CURVE_WITH_KNOTS('',3,(#21641,#21642,#21643,#21644,#21645,
#21646,#21647,#21648,#21649,#21650,#21651,#21652,#21653,#21654,#21655,#21656,
#21657,#21658,#21659,#21660,#21661,#21662,#21663,#21664,#21665,#21666,#21667,
#21668,#21669,#21670),.UNSPECIFIED.,.F.,.F.,(4,2,2,2,2,2,2,2,2,2,2,2,2,
2,4),(0.,0.0591297066253794,0.10128606294941,0.137517711401119,0.179810134914014,
0.212974667045288,0.229441128614387,0.242688203236939,0.255921391404106,
0.272139917047586,0.304029069945836,0.344156916497933,0.380728183503669,
0.421482205150903,0.485707929364375),.UNSPECIFIED.);
#600=B_SPLINE_CURVE_WITH_KNOTS('',3,(#21674,#21675,#21676,#21677,#21678,
#21679,#21680,#21681,#21682,#21683,#21684,#21685,#21686,#21687,#21688,#21689,
#21690,#21691,#21692,#21693,#21694,#21695,#21696,#21697,#21698,#21699,#21700,
#21701,#21702,#21703),.UNSPECIFIED.,.F.,.F.,(4,2,2,2,2,2,2,2,2,2,2,2,2,
2,4),(0.,0.062557615554957,0.103705894628953,0.140114223826674,0.180905683903591,
0.212584741865488,0.229068999283227,0.242305782037741,0.255524854267291,
0.271696804230317,0.303396718536427,0.3432217183572,0.379813718288632,0.420371936848053,
0.486941959854542),.UNSPECIFIED.);
#601=B_SPLINE_CURVE_WITH_KNOTS('',3,(#21707,#21708,#21709,#21710,#21711,
#21712,#21713,#21714,#21715,#21716,#21717,#21718,#21719,#21720,#21721,#21722,
#21723,#21724,#21725,#21726,#21727,#21728,#21729,#21730,#21731,#21732,#21733,
#21734,#21735,#21736),.UNSPECIFIED.,.F.,.F.,(4,2,2,2,2,2,2,2,2,2,2,2,2,
2,4),(0.,0.0591297066254563,0.101286062949547,0.137517711401359,0.179810134914195,
0.212974667045375,0.229441128614446,0.24268820323693,0.255921391404018,
0.272139917047466,0.304029069945651,0.34415691649772,0.380728183503433,
0.421482205150684,0.485707929363767),.UNSPECIFIED.);
#602=B_SPLINE_CURVE_WITH_KNOTS('',3,(#21740,#21741,#21742,#21743,#21744,
#21745,#21746,#21747,#21748,#21749,#21750,#21751,#21752,#21753,#21754,#21755,
#21756,#21757,#21758,#21759,#21760,#21761,#21762,#21763,#21764,#21765,#21766,
#21767,#21768,#21769),.UNSPECIFIED.,.F.,.F.,(4,2,2,2,2,2,2,2,2,2,2,2,2,
2,4),(0.,0.0625576155549561,0.103705894629025,0.140114223826833,0.18090568390366,
0.212584741865487,0.229068999283183,0.242305782037646,0.25552485426716,
0.271696804230063,0.303396718535982,0.343221718356607,0.379813718287887,
0.420371936847143,0.486941959853062),.UNSPECIFIED.);
#603=B_SPLINE_CURVE_WITH_KNOTS('',3,(#21777,#21778,#21779,#21780,#21781,
#21782,#21783,#21784,#21785,#21786),.UNSPECIFIED.,.F.,.F.,(4,2,2,2,4),(-0.46979780856301,
-0.352361341367453,-0.234924874171897,-0.117462437085949,0.),
 .UNSPECIFIED.);
#604=B_SPLINE_CURVE_WITH_KNOTS('',3,(#21788,#21789,#21790,#21791,#21792,
#21793,#21794,#21795,#21796,#21797),.UNSPECIFIED.,.F.,.F.,(4,2,2,2,4),(0.,
0.117462437085949,0.234924874171897,0.352361341367453,0.46979780856301),
 .UNSPECIFIED.);
#605=B_SPLINE_CURVE_WITH_KNOTS('',3,(#21802,#21803,#21804,#21805,#21806,
#21807,#21808,#21809,#21810,#21811),.UNSPECIFIED.,.F.,.F.,(4,2,2,2,4),(0.46979780856301,
0.587234275758566,0.704670742954122,0.822133180040071,0.939595617126019),
 .UNSPECIFIED.);
#606=B_SPLINE_CURVE_WITH_KNOTS('',3,(#21812,#21813,#21814,#21815,#21816,
#21817,#21818,#21819,#21820,#21821),.UNSPECIFIED.,.F.,.F.,(4,2,2,2,4),(-0.939595617126019,
-0.822133180040071,-0.704670742954122,-0.587234275758566,-0.46979780856301),
 .UNSPECIFIED.);
#607=B_SPLINE_CURVE_WITH_KNOTS('',3,(#21824,#21825,#21826,#21827,#21828,
#21829,#21830,#21831,#21832,#21833),.UNSPECIFIED.,.F.,.F.,(4,2,2,2,4),(-0.46979780856301,
-0.352361341367453,-0.234924874171897,-0.117462437085949,0.),
 .UNSPECIFIED.);
#608=B_SPLINE_CURVE_WITH_KNOTS('',3,(#21834,#21835,#21836,#21837,#21838,
#21839,#21840,#21841,#21842,#21843,#21844,#21845,#21846,#21847,#21848,#21849,
#21850,#21851,#21852,#21853,#21854,#21855,#21856,#21857,#21858,#21859),
 .UNSPECIFIED.,.F.,.F.,(4,2,2,2,2,2,2,2,2,2,2,2,4),(0.,0.117462437085949,
0.234924874171897,0.352361341367453,0.46979780856301,0.587234275758566,
0.704670742954122,0.822133180040071,0.939595617126019,1.05705805421197,
1.17452049129792,1.29195695849347,1.40939342568903),.UNSPECIFIED.);
#609=B_SPLINE_CURVE_WITH_KNOTS('',3,(#21868,#21869,#21870,#21871,#21872,
#21873,#21874,#21875,#21876,#21877,#21878,#21879,#21880,#21881,#21882,#21883,
#21884,#21885,#21886,#21887,#21888,#21889,#21890),.UNSPECIFIED.,.F.,.F.,
(4,2,2,2,3,2,2,2,2,2,4),(-0.353056606424783,-0.270966220923752,-0.175803528294806,
-0.0859129119745955,0.,0.0556570980636411,0.111652355987737,0.20499419097358,
0.299846488870027,0.394527300690664,0.396042374825994),.UNSPECIFIED.);
#610=B_SPLINE_CURVE_WITH_KNOTS('',3,(#21895,#21896,#21897,#21898,#21899,
#21900,#21901,#21902,#21903,#21904,#21905,#21906),.UNSPECIFIED.,.F.,.F.,
(4,2,2,2,2,4),(0.396042374825994,0.490876853267616,0.585866484025814,0.675498135386537,
0.761377359963428,0.770847053721237),.UNSPECIFIED.);
#611=B_SPLINE_CURVE_WITH_KNOTS('',3,(#21907,#21908,#21909,#21910,#21911,
#21912,#21913,#21914,#21915,#21916,#21917,#21918),.UNSPECIFIED.,.F.,.F.,
(4,2,2,2,2,4),(-0.727854718895878,-0.649817772706759,-0.557871466640106,
-0.462969650386807,-0.367340921859025,-0.353056606424783),.UNSPECIFIED.);
#612=B_SPLINE_CURVE_WITH_KNOTS('',3,(#21920,#21921,#21922,#21923,#21924,
#21925,#21926,#21927,#21928,#21929,#21930,#21931,#21932,#21933,#21934,#21935,
#21936,#21937,#21938,#21939,#21940,#21941,#21942,#21943,#21944,#21945,#21946,
#21947,#21948,#21949,#21950,#21951,#21952,#21953,#21954,#21955,#21956,#21957,
#21958),.UNSPECIFIED.,.T.,.F.,(4,2,2,2,2,2,2,2,2,3,2,2,2,2,2,2,2,2,4),(-0.7577515844171,
-0.736832386346907,-0.640706303106354,-0.54687575262776,-0.458462079703312,
-0.372641160637091,-0.283889834493717,-0.19079436895225,-0.096117228806511,
0.,0.0612173298619945,0.121966896291198,0.214605744640411,0.30206903695819,
0.387916805853724,0.477547309412777,0.571760843278307,0.667059100969111,
0.740952092944516),.UNSPECIFIED.);
#613=B_SPLINE_CURVE_WITH_KNOTS('',3,(#21976,#21977,#21978,#21979,#21980,
#21981,#21982,#21983,#21984,#21985),.UNSPECIFIED.,.F.,.F.,(4,2,2,2,4),(0.302390904078212,
0.377985652694416,0.453580401310619,0.529181104733521,0.604781808156423),
 .UNSPECIFIED.);
#614=B_SPLINE_CURVE_WITH_KNOTS('',3,(#21987,#21988,#21989,#21990,#21991,
#21992,#21993,#21994,#21995,#21996),.UNSPECIFIED.,.F.,.F.,(4,2,2,2,4),(0.604781808156423,
0.680382511579325,0.755983215002227,0.831577963618431,0.907172712234635),
 .UNSPECIFIED.);
#615=B_SPLINE_CURVE_WITH_KNOTS('',3,(#22000,#22001,#22002,#22003,#22004,
#22005,#22006,#22007,#22008,#22009),.UNSPECIFIED.,.F.,.F.,(4,2,2,2,4),(0.47110500506321,
0.588852659623554,0.706600314183898,0.824405162155159,0.942210010126421),
 .UNSPECIFIED.);
#616=B_SPLINE_CURVE_WITH_KNOTS('',3,(#22011,#22012,#22013,#22014,#22015,
#22016,#22017,#22018,#22019,#22020),.UNSPECIFIED.,.F.,.F.,(4,2,2,2,4),(0.942210010126421,
1.06001485809768,1.17781970606894,1.29556736062929,1.41331501518963),
 .UNSPECIFIED.);
#617=B_SPLINE_CURVE_WITH_KNOTS('',3,(#22025,#22026,#22027,#22028,#22029,
#22030,#22031,#22032,#22033,#22034),.UNSPECIFIED.,.F.,.F.,(4,2,2,2,4),(1.41331501518963,
1.53106266974997,1.64881032431032,1.76661517228158,1.88442002025284),
 .UNSPECIFIED.);
#618=B_SPLINE_CURVE_WITH_KNOTS('',3,(#22035,#22036,#22037,#22038,#22039,
#22040,#22041,#22042,#22043,#22044),.UNSPECIFIED.,.F.,.F.,(4,2,2,2,4),(0.,
0.117804847971262,0.235609695942523,0.353357350502867,0.47110500506321),
 .UNSPECIFIED.);
#619=B_SPLINE_CURVE_WITH_KNOTS('',3,(#22046,#22047,#22048,#22049,#22050,
#22051,#22052,#22053,#22054,#22055),.UNSPECIFIED.,.F.,.F.,(4,2,2,2,4),(0.907172712234635,
0.982767460850839,1.05836220946704,1.13396291288994,1.20956361631285),
 .UNSPECIFIED.);
#620=B_SPLINE_CURVE_WITH_KNOTS('',3,(#22056,#22057,#22058,#22059,#22060,
#22061,#22062,#22063,#22064,#22065),.UNSPECIFIED.,.F.,.F.,(4,2,2,2,4),(0.,
0.0756007034229019,0.151201406845804,0.226796155462008,0.302390904078212),
 .UNSPECIFIED.);
#621=B_SPLINE_CURVE_WITH_KNOTS('',3,(#22069,#22070,#22071,#22072,#22073,
#22074,#22075,#22076,#22077,#22078,#22079,#22080,#22081,#22082,#22083,#22084,
#22085,#22086,#22087,#22088,#22089,#22090,#22091,#22092,#22093,#22094,#22095),
 .UNSPECIFIED.,.F.,.F.,(4,2,2,2,3,2,2,2,2,2,2,2,4),(0.907172712234635,0.982767460850839,
1.05836220946704,1.13396291288994,1.20956361631285,1.28516431973575,1.36076502315865,
1.43635977177485,1.51195452039106,1.58754926900726,1.66314401762347,1.73874472104637,
1.81434542446927),.UNSPECIFIED.);
#622=B_SPLINE_CURVE_WITH_KNOTS('',3,(#22096,#22097,#22098,#22099,#22100,
#22101,#22102,#22103,#22104,#22105),.UNSPECIFIED.,.F.,.F.,(4,2,2,2,4),(1.81434542446927,
1.88994612789217,1.96554683131507,2.04114157993128,2.11673632854748),
 .UNSPECIFIED.);
#623=B_SPLINE_CURVE_WITH_KNOTS('',3,(#22108,#22109,#22110,#22111,#22112,
#22113,#22114,#22115,#22116,#22117,#22118,#22119,#22120,#22121,#22122,#22123,
#22124,#22125,#22126,#22127,#22128,#22129,#22130,#22131,#22132,#22133,#22134),
 .UNSPECIFIED.,.F.,.F.,(4,2,2,2,3,2,2,2,2,2,2,2,4),(1.41331501518963,1.53106266974997,
1.64881032431032,1.76661517228158,1.88442002025284,2.0022248682241,2.12002971619536,
2.23777737075571,2.35552502531605,2.4732726798764,2.59102033443674,2.708825182408,
2.82663003037926),.UNSPECIFIED.);
#624=B_SPLINE_CURVE_WITH_KNOTS('',3,(#22135,#22136,#22137,#22138,#22139,
#22140,#22141,#22142,#22143,#22144),.UNSPECIFIED.,.F.,.F.,(4,2,2,2,4),(2.82663003037926,
2.94443487835052,3.06223972632179,3.17998738088213,3.29773503544247),
 .UNSPECIFIED.);
#625=B_SPLINE_CURVE_WITH_KNOTS('',3,(#22152,#22153,#22154,#22155,#22156,
#22157,#22158,#22159,#22160,#22161,#22162,#22163,#22164,#22165,#22166,#22167,
#22168,#22169,#22170,#22171,#22172,#22173,#22174,#22175,#22176,#22177,#22178,
#22179,#22180,#22181,#22182,#22183,#22184,#22185,#22186,#22187,#22188),
 .UNSPECIFIED.,.F.,.F.,(4,2,2,2,2,2,2,2,2,2,3,2,2,2,2,2,2,4),(0.66709016003974,
0.694276778086138,0.770594476757215,0.84906692863503,0.927850026287074,
0.965860761886542,1.00385889129356,1.07985135515414,1.15830200911339,1.21149927946789,
1.26460940023701,1.3023609951576,1.34039955079445,1.37852748721988,1.41681863761144,
1.49590023217333,1.57485124143574,1.61563645580579),.UNSPECIFIED.);
#626=B_SPLINE_CURVE_WITH_KNOTS('',3,(#22190,#22191,#22192,#22193,#22194,
#22195,#22196,#22197,#22198,#22199,#22200,#22201,#22202,#22203,#22204,#22205),
 .UNSPECIFIED.,.F.,.F.,(4,2,2,2,2,2,2,4),(1.61563645580579,1.65065033370949,
1.72635516248862,1.80489182430705,1.84434548324305,1.88293297920974,1.92132794397062,
1.93169956027675),.UNSPECIFIED.);
#627=B_SPLINE_CURVE_WITH_KNOTS('',3,(#22210,#22211,#22212,#22213,#22214,
#22215,#22216,#22217,#22218,#22219,#22220,#22221,#22222,#22223,#22224,#22225,
#22226,#22227,#22228,#22229),.UNSPECIFIED.,.F.,.F.,(4,2,2,2,2,2,2,2,2,4),
(1.26878286228387,1.3415697328015,1.4185184514642,1.49730235790989,1.57510611204151,
1.6512168301348,1.7286733175368,1.80824177624455,1.84722443352035,1.90183587401007),
 .UNSPECIFIED.);
#628=B_SPLINE_CURVE_WITH_KNOTS('',3,(#22230,#22231,#22232,#22233,#22234,
#22235,#22236,#22237,#22238,#22239,#22240,#22241,#22242,#22243,#22244,#22245,
#22246,#22247,#22248,#22249,#22250,#22251,#22252,#22253,#22254,#22255,#22256,
#22257,#22258,#22259,#22260),.UNSPECIFIED.,.F.,.F.,(4,2,2,2,2,2,2,2,2,2,
2,2,2,3,4),(0.636510547675982,0.658871161538065,0.696960874037515,0.735081814971663,
0.813573460248337,0.833402362698247,0.872507027375637,0.911354700684223,
0.98788468247215,1.02607483553733,1.06428112645553,1.14327310095656,1.20431912927923,
1.26532532633409,1.26878286228387),.UNSPECIFIED.);
#629=B_SPLINE_CURVE_WITH_KNOTS('',1,(#23311,#23312),.UNSPECIFIED.,.F.,.F.,
(2,2),(-0.999999999999999,-7.62951798228629E-16),.UNSPECIFIED.);
#630=B_SPLINE_CURVE_WITH_KNOTS('',1,(#23765,#23766),.UNSPECIFIED.,.F.,.F.,
(2,2),(-1.,3.41544860156615E-16),.UNSPECIFIED.);
#898=PLANE('',#10715);
#899=PLANE('',#10718);
#1270=FACE_OUTER_BOUND('',#1848,.T.);
#1271=FACE_OUTER_BOUND('',#1858,.T.);
#1272=FACE_OUTER_BOUND('',#1860,.T.);
#1273=FACE_OUTER_BOUND('',#1862,.T.);
#1274=FACE_OUTER_BOUND('',#1864,.T.);
#1275=FACE_OUTER_BOUND('',#1866,.T.);
#1276=FACE_OUTER_BOUND('',#1869,.T.);
#1277=FACE_OUTER_BOUND('',#1870,.T.);
#1278=FACE_OUTER_BOUND('',#1871,.T.);
#1279=FACE_OUTER_BOUND('',#1872,.T.);
#1280=FACE_OUTER_BOUND('',#1873,.T.);
#1281=FACE_OUTER_BOUND('',#1874,.T.);
#1282=FACE_OUTER_BOUND('',#1875,.T.);
#1283=FACE_OUTER_BOUND('',#1876,.T.);
#1284=FACE_OUTER_BOUND('',#1877,.T.);
#1285=FACE_OUTER_BOUND('',#1878,.T.);
#1286=FACE_OUTER_BOUND('',#1879,.T.);
#1287=FACE_OUTER_BOUND('',#1880,.T.);
#1288=FACE_OUTER_BOUND('',#1881,.T.);
#1289=FACE_OUTER_BOUND('',#1882,.T.);
#1290=FACE_OUTER_BOUND('',#1883,.T.);
#1291=FACE_OUTER_BOUND('',#1884,.T.);
#1292=FACE_OUTER_BOUND('',#1885,.T.);
#1293=FACE_OUTER_BOUND('',#1886,.T.);
#1294=FACE_OUTER_BOUND('',#1887,.T.);
#1295=FACE_OUTER_BOUND('',#1888,.T.);
#1296=FACE_OUTER_BOUND('',#1889,.T.);
#1297=FACE_OUTER_BOUND('',#1890,.T.);
#1298=FACE_OUTER_BOUND('',#1891,.T.);
#1299=FACE_OUTER_BOUND('',#1892,.T.);
#1300=FACE_OUTER_BOUND('',#1893,.T.);
#1301=FACE_OUTER_BOUND('',#1894,.T.);
#1302=FACE_OUTER_BOUND('',#1895,.T.);
#1303=FACE_OUTER_BOUND('',#1896,.T.);
#1304=FACE_OUTER_BOUND('',#1897,.T.);
#1305=FACE_OUTER_BOUND('',#1898,.T.);
#1306=FACE_OUTER_BOUND('',#1899,.T.);
#1307=FACE_OUTER_BOUND('',#1900,.T.);
#1308=FACE_OUTER_BOUND('',#1901,.T.);
#1309=FACE_OUTER_BOUND('',#1902,.T.);
#1310=FACE_OUTER_BOUND('',#1903,.T.);
#1311=FACE_OUTER_BOUND('',#1904,.T.);
#1312=FACE_OUTER_BOUND('',#1905,.T.);
#1313=FACE_OUTER_BOUND('',#1906,.T.);
#1314=FACE_OUTER_BOUND('',#1907,.T.);
#1315=FACE_OUTER_BOUND('',#1908,.T.);
#1316=FACE_OUTER_BOUND('',#1909,.T.);
#1317=FACE_OUTER_BOUND('',#1910,.T.);
#1848=EDGE_LOOP('',(#7728,#7729,#7730,#7731,#7732,#7733,#7734,#7735,#7736,
#7737,#7738,#7739));
#1849=EDGE_LOOP('',(#7740,#7741,#7742,#7743));
#1850=EDGE_LOOP('',(#7744,#7745,#7746,#7747));
#1851=EDGE_LOOP('',(#7748,#7749,#7750,#7751));
#1852=EDGE_LOOP('',(#7752,#7753,#7754,#7755));
#1853=EDGE_LOOP('',(#7756,#7757,#7758,#7759));
#1854=EDGE_LOOP('',(#7760,#7761,#7762,#7763));
#1855=EDGE_LOOP('',(#7764,#7765,#7766,#7767));
#1856=EDGE_LOOP('',(#7768,#7769,#7770,#7771));
#1857=EDGE_LOOP('',(#7772,#7773,#7774,#7775));
#1858=EDGE_LOOP('',(#7776,#7777,#7778,#7779,#7780,#7781,#7782,#7783,#7784,
#7785));
#1859=EDGE_LOOP('',(#7786,#7787));
#1860=EDGE_LOOP('',(#7788,#7789,#7790,#7791,#7792,#7793,#7794,#7795,#7796,
#7797));
#1861=EDGE_LOOP('',(#7798));
#1862=EDGE_LOOP('',(#7799));
#1863=EDGE_LOOP('',(#7800));
#1864=EDGE_LOOP('',(#7801));
#1865=EDGE_LOOP('',(#7802));
#1866=EDGE_LOOP('',(#7803,#7804,#7805,#7806,#7807,#7808,#7809,#7810,#7811,
#7812,#7813,#7814,#7815,#7816,#7817,#7818,#7819));
#1867=EDGE_LOOP('',(#7820,#7821));
#1868=EDGE_LOOP('',(#7822,#7823));
#1869=EDGE_LOOP('',(#7824,#7825,#7826,#7827,#7828,#7829,#7830,#7831));
#1870=EDGE_LOOP('',(#7832,#7833,#7834,#7835,#7836,#7837,#7838,#7839));
#1871=EDGE_LOOP('',(#7840,#7841,#7842,#7843,#7844,#7845,#7846,#7847));
#1872=EDGE_LOOP('',(#7848,#7849,#7850,#7851,#7852,#7853));
#1873=EDGE_LOOP('',(#7854,#7855,#7856,#7857));
#1874=EDGE_LOOP('',(#7858,#7859,#7860,#7861));
#1875=EDGE_LOOP('',(#7862,#7863));
#1876=EDGE_LOOP('',(#7864,#7865,#7866,#7867));
#1877=EDGE_LOOP('',(#7868,#7869));
#1878=EDGE_LOOP('',(#7870,#7871));
#1879=EDGE_LOOP('',(#7872,#7873,#7874,#7875));
#1880=EDGE_LOOP('',(#7876,#7877));
#1881=EDGE_LOOP('',(#7878,#7879));
#1882=EDGE_LOOP('',(#7880,#7881,#7882,#7883));
#1883=EDGE_LOOP('',(#7884,#7885));
#1884=EDGE_LOOP('',(#7886,#7887));
#1885=EDGE_LOOP('',(#7888,#7889,#7890,#7891));
#1886=EDGE_LOOP('',(#7892,#7893));
#1887=EDGE_LOOP('',(#7894,#7895));
#1888=EDGE_LOOP('',(#7896,#7897,#7898,#7899));
#1889=EDGE_LOOP('',(#7900,#7901));
#1890=EDGE_LOOP('',(#7902,#7903,#7904));
#1891=EDGE_LOOP('',(#7905,#7906,#7907,#7908));
#1892=EDGE_LOOP('',(#7909,#7910,#7911));
#1893=EDGE_LOOP('',(#7912,#7913));
#1894=EDGE_LOOP('',(#7914,#7915,#7916,#7917));
#1895=EDGE_LOOP('',(#7918,#7919));
#1896=EDGE_LOOP('',(#7920,#7921));
#1897=EDGE_LOOP('',(#7922,#7923,#7924,#7925));
#1898=EDGE_LOOP('',(#7926,#7927));
#1899=EDGE_LOOP('',(#7928,#7929));
#1900=EDGE_LOOP('',(#7930,#7931,#7932,#7933));
#1901=EDGE_LOOP('',(#7934,#7935));
#1902=EDGE_LOOP('',(#7936,#7937));
#1903=EDGE_LOOP('',(#7938,#7939,#7940,#7941));
#1904=EDGE_LOOP('',(#7942,#7943));
#1905=EDGE_LOOP('',(#7944,#7945,#7946,#7947,#7948,#7949,#7950));
#1906=EDGE_LOOP('',(#7951,#7952,#7953,#7954,#7955));
#1907=EDGE_LOOP('',(#7956,#7957,#7958,#7959));
#1908=EDGE_LOOP('',(#7960,#7961,#7962,#7963,#7964));
#1909=EDGE_LOOP('',(#7965,#7966,#7967,#7968));
#1910=EDGE_LOOP('',(#7969,#7970,#7971,#7972,#7973));
#2398=CIRCLE('',#10706,11.1);
#2399=CIRCLE('',#10707,11.1);
#2400=CIRCLE('',#10709,11.1);
#2401=CIRCLE('',#10710,11.1);
#2402=CIRCLE('',#10712,11.1);
#2403=CIRCLE('',#10713,11.1);
#2404=CIRCLE('',#10714,11.1);
#2405=CIRCLE('',#10716,10.6);
#2406=CIRCLE('',#10717,9.69998799999997);
#2407=CIRCLE('',#10719,10.6);
#2408=CIRCLE('',#10720,9.70000000000007);
#2409=CIRCLE('',#10722,9.2);
#2410=CIRCLE('',#10723,9.2);
#2411=CIRCLE('',#10724,9.2);
#2412=CIRCLE('',#10730,0.8);
#2413=CIRCLE('',#10732,0.8);
#2414=CIRCLE('',#10733,1.865);
#2415=CIRCLE('',#10735,1.865);
#2416=CIRCLE('',#10736,1.865);
#2417=CIRCLE('',#10738,1.865);
#2418=CIRCLE('',#10739,1.865);
#2419=CIRCLE('',#10741,1.865);
#2420=CIRCLE('',#10742,1.865);
#2421=CIRCLE('',#10744,1.865);
#2422=CIRCLE('',#10745,1.865);
#2423=CIRCLE('',#10747,1.865);
#2424=CIRCLE('',#10748,1.865);
#2425=CIRCLE('',#10750,1.865);
#2426=CIRCLE('',#10751,1.865);
#2427=CIRCLE('',#10753,1.865);
#2428=CIRCLE('',#10754,1.865);
#2429=CIRCLE('',#10756,1.865);
#2430=CIRCLE('',#10757,1.865);
#2431=CIRCLE('',#10759,1.865);
#2432=CIRCLE('',#10760,1.865);
#2433=CIRCLE('',#10762,1.865);
#3014=LINE('',#21098,#3764);
#3015=LINE('',#21119,#3765);
#3016=LINE('',#21138,#3766);
#3017=LINE('',#21160,#3767);
#3018=LINE('',#21210,#3768);
#3019=LINE('',#21242,#3769);
#3020=LINE('',#21276,#3770);
#3021=LINE('',#21308,#3771);
#3022=LINE('',#21342,#3772);
#3023=LINE('',#21374,#3773);
#3024=LINE('',#21408,#3774);
#3025=LINE('',#21440,#3775);
#3026=LINE('',#21474,#3776);
#3027=LINE('',#21506,#3777);
#3028=LINE('',#21540,#3778);
#3029=LINE('',#21572,#3779);
#3030=LINE('',#21606,#3780);
#3031=LINE('',#21638,#3781);
#3032=LINE('',#21672,#3782);
#3033=LINE('',#21704,#3783);
#3034=LINE('',#21738,#3784);
#3035=LINE('',#21770,#3785);
#3036=LINE('',#21775,#3786);
#3037=LINE('',#21799,#3787);
#3038=LINE('',#21866,#3788);
#3039=LINE('',#21892,#3789);
#3040=LINE('',#21974,#3790);
#3041=LINE('',#21998,#3791);
#3042=LINE('',#22022,#3792);
#3043=LINE('',#22146,#3793);
#3044=LINE('',#22148,#3794);
#3045=LINE('',#22189,#3795);
#3046=LINE('',#22208,#3796);
#3047=LINE('',#23768,#3797);
#3048=LINE('',#23770,#3798);
#3049=LINE('',#23772,#3799);
#3050=LINE('',#23774,#3800);
#3764=VECTOR('',#12527,11.1);
#3765=VECTOR('',#12528,1000.);
#3766=VECTOR('',#12529,11.1);
#3767=VECTOR('',#12532,1000.);
#3768=VECTOR('',#12533,1000.);
#3769=VECTOR('',#12534,1000.);
#3770=VECTOR('',#12535,1000.);
#3771=VECTOR('',#12536,1000.);
#3772=VECTOR('',#12537,1000.);
#3773=VECTOR('',#12538,1000.);
#3774=VECTOR('',#12539,1000.);
#3775=VECTOR('',#12540,1000.);
#3776=VECTOR('',#12541,1000.);
#3777=VECTOR('',#12542,1000.);
#3778=VECTOR('',#12543,1000.);
#3779=VECTOR('',#12544,1000.);
#3780=VECTOR('',#12545,1000.);
#3781=VECTOR('',#12546,1000.);
#3782=VECTOR('',#12547,1000.);
#3783=VECTOR('',#12548,1000.);
#3784=VECTOR('',#12549,1000.);
#3785=VECTOR('',#12550,1000.);
#3786=VECTOR('',#12555,11.1);
#3787=VECTOR('',#12556,11.1);
#3788=VECTOR('',#12565,11.1);
#3789=VECTOR('',#12566,11.1);
#3790=VECTOR('',#12585,9.2);
#3791=VECTOR('',#12586,9.2);
#3792=VECTOR('',#12587,9.2);
#3793=VECTOR('',#12594,3.09999999999999);
#3794=VECTOR('',#12597,3.09999999999999);
#3795=VECTOR('',#12600,2.);
#3796=VECTOR('',#12603,2.);
#3797=VECTOR('',#12674,9.2);
#3798=VECTOR('',#12677,9.70000000000007);
#3799=VECTOR('',#12680,10.6);
#3800=VECTOR('',#12683,11.1);
#4526=VERTEX_POINT('',#21095);
#4527=VERTEX_POINT('',#21097);
#4528=VERTEX_POINT('',#21099);
#4529=VERTEX_POINT('',#21118);
#4530=VERTEX_POINT('',#21120);
#4531=VERTEX_POINT('',#21137);
#4532=VERTEX_POINT('',#21140);
#4533=VERTEX_POINT('',#21159);
#4534=VERTEX_POINT('',#21177);
#4535=VERTEX_POINT('',#21178);
#4536=VERTEX_POINT('',#21209);
#4537=VERTEX_POINT('',#21211);
#4538=VERTEX_POINT('',#21243);
#4539=VERTEX_POINT('',#21244);
#4540=VERTEX_POINT('',#21275);
#4541=VERTEX_POINT('',#21277);
#4542=VERTEX_POINT('',#21309);
#4543=VERTEX_POINT('',#21310);
#4544=VERTEX_POINT('',#21341);
#4545=VERTEX_POINT('',#21343);
#4546=VERTEX_POINT('',#21375);
#4547=VERTEX_POINT('',#21376);
#4548=VERTEX_POINT('',#21407);
#4549=VERTEX_POINT('',#21409);
#4550=VERTEX_POINT('',#21441);
#4551=VERTEX_POINT('',#21442);
#4552=VERTEX_POINT('',#21473);
#4553=VERTEX_POINT('',#21475);
#4554=VERTEX_POINT('',#21507);
#4555=VERTEX_POINT('',#21508);
#4556=VERTEX_POINT('',#21539);
#4557=VERTEX_POINT('',#21541);
#4558=VERTEX_POINT('',#21573);
#4559=VERTEX_POINT('',#21574);
#4560=VERTEX_POINT('',#21605);
#4561=VERTEX_POINT('',#21607);
#4562=VERTEX_POINT('',#21639);
#4563=VERTEX_POINT('',#21640);
#4564=VERTEX_POINT('',#21671);
#4565=VERTEX_POINT('',#21673);
#4566=VERTEX_POINT('',#21705);
#4567=VERTEX_POINT('',#21706);
#4568=VERTEX_POINT('',#21737);
#4569=VERTEX_POINT('',#21739);
#4570=VERTEX_POINT('',#21772);
#4571=VERTEX_POINT('',#21774);
#4572=VERTEX_POINT('',#21776);
#4573=VERTEX_POINT('',#21787);
#4574=VERTEX_POINT('',#21798);
#4575=VERTEX_POINT('',#21801);
#4576=VERTEX_POINT('',#21822);
#4577=VERTEX_POINT('',#21823);
#4578=VERTEX_POINT('',#21861);
#4579=VERTEX_POINT('',#21862);
#4580=VERTEX_POINT('',#21865);
#4581=VERTEX_POINT('',#21867);
#4582=VERTEX_POINT('',#21891);
#4583=VERTEX_POINT('',#21894);
#4584=VERTEX_POINT('',#21919);
#4585=VERTEX_POINT('',#21960);
#4586=VERTEX_POINT('',#21962);
#4587=VERTEX_POINT('',#21965);
#4588=VERTEX_POINT('',#21967);
#4589=VERTEX_POINT('',#21970);
#4590=VERTEX_POINT('',#21971);
#4591=VERTEX_POINT('',#21973);
#4592=VERTEX_POINT('',#21975);
#4593=VERTEX_POINT('',#21986);
#4594=VERTEX_POINT('',#21997);
#4595=VERTEX_POINT('',#21999);
#4596=VERTEX_POINT('',#22010);
#4597=VERTEX_POINT('',#22021);
#4598=VERTEX_POINT('',#22024);
#4599=VERTEX_POINT('',#22045);
#4600=VERTEX_POINT('',#22067);
#4601=VERTEX_POINT('',#22068);
#4602=VERTEX_POINT('',#22106);
#4603=VERTEX_POINT('',#22107);
#4604=VERTEX_POINT('',#22150);
#4605=VERTEX_POINT('',#22151);
#4606=VERTEX_POINT('',#22207);
#4607=VERTEX_POINT('',#22209);
#5677=EDGE_CURVE('',#4526,#4526,#2398,.T.);
#5678=EDGE_CURVE('',#4526,#4527,#3014,.T.);
#5679=EDGE_CURVE('',#4528,#4527,#581,.T.);
#5680=EDGE_CURVE('',#4529,#4528,#3015,.T.);
#5681=EDGE_CURVE('',#4530,#4529,#582,.T.);
#5682=EDGE_CURVE('',#4530,#4531,#3016,.T.);
#5683=EDGE_CURVE('',#4531,#4531,#2399,.T.);
#5684=EDGE_CURVE('',#4532,#4530,#583,.T.);
#5685=EDGE_CURVE('',#4533,#4532,#3017,.T.);
#5686=EDGE_CURVE('',#4527,#4533,#584,.T.);
#5687=EDGE_CURVE('',#4534,#4535,#585,.T.);
#5688=EDGE_CURVE('',#4536,#4534,#3018,.T.);
#5689=EDGE_CURVE('',#4537,#4536,#586,.T.);
#5690=EDGE_CURVE('',#4535,#4537,#3019,.T.);
#5691=EDGE_CURVE('',#4538,#4539,#587,.T.);
#5692=EDGE_CURVE('',#4540,#4538,#3020,.T.);
#5693=EDGE_CURVE('',#4541,#4540,#588,.T.);
#5694=EDGE_CURVE('',#4539,#4541,#3021,.T.);
#5695=EDGE_CURVE('',#4542,#4543,#589,.T.);
#5696=EDGE_CURVE('',#4544,#4542,#3022,.T.);
#5697=EDGE_CURVE('',#4545,#4544,#590,.T.);
#5698=EDGE_CURVE('',#4543,#4545,#3023,.T.);
#5699=EDGE_CURVE('',#4546,#4547,#591,.T.);
#5700=EDGE_CURVE('',#4548,#4546,#3024,.T.);
#5701=EDGE_CURVE('',#4549,#4548,#592,.T.);
#5702=EDGE_CURVE('',#4547,#4549,#3025,.T.);
#5703=EDGE_CURVE('',#4550,#4551,#593,.T.);
#5704=EDGE_CURVE('',#4552,#4550,#3026,.T.);
#5705=EDGE_CURVE('',#4553,#4552,#594,.T.);
#5706=EDGE_CURVE('',#4551,#4553,#3027,.T.);
#5707=EDGE_CURVE('',#4554,#4555,#595,.T.);
#5708=EDGE_CURVE('',#4556,#4554,#3028,.T.);
#5709=EDGE_CURVE('',#4557,#4556,#596,.T.);
#5710=EDGE_CURVE('',#4555,#4557,#3029,.T.);
#5711=EDGE_CURVE('',#4558,#4559,#597,.T.);
#5712=EDGE_CURVE('',#4560,#4558,#3030,.T.);
#5713=EDGE_CURVE('',#4561,#4560,#598,.T.);
#5714=EDGE_CURVE('',#4559,#4561,#3031,.T.);
#5715=EDGE_CURVE('',#4562,#4563,#599,.T.);
#5716=EDGE_CURVE('',#4564,#4562,#3032,.T.);
#5717=EDGE_CURVE('',#4565,#4564,#600,.T.);
#5718=EDGE_CURVE('',#4563,#4565,#3033,.T.);
#5719=EDGE_CURVE('',#4566,#4567,#601,.T.);
#5720=EDGE_CURVE('',#4568,#4566,#3034,.T.);
#5721=EDGE_CURVE('',#4569,#4568,#602,.T.);
#5722=EDGE_CURVE('',#4567,#4569,#3035,.T.);
#5723=EDGE_CURVE('',#4570,#4570,#2400,.T.);
#5724=EDGE_CURVE('',#4570,#4571,#3036,.T.);
#5725=EDGE_CURVE('',#4571,#4572,#603,.T.);
#5726=EDGE_CURVE('',#4572,#4573,#604,.T.);
#5727=EDGE_CURVE('',#4573,#4574,#3037,.T.);
#5728=EDGE_CURVE('',#4574,#4574,#2401,.T.);
#5729=EDGE_CURVE('',#4573,#4575,#605,.T.);
#5730=EDGE_CURVE('',#4575,#4571,#606,.T.);
#5731=EDGE_CURVE('',#4576,#4577,#607,.T.);
#5732=EDGE_CURVE('',#4577,#4576,#608,.T.);
#5733=EDGE_CURVE('',#4578,#4579,#2402,.T.);
#5734=EDGE_CURVE('',#4579,#4578,#2403,.T.);
#5735=EDGE_CURVE('',#4578,#4580,#3038,.T.);
#5736=EDGE_CURVE('',#4580,#4581,#609,.T.);
#5737=EDGE_CURVE('',#4581,#4582,#3039,.T.);
#5738=EDGE_CURVE('',#4582,#4582,#2404,.T.);
#5739=EDGE_CURVE('',#4581,#4583,#610,.T.);
#5740=EDGE_CURVE('',#4583,#4580,#611,.T.);
#5741=EDGE_CURVE('',#4584,#4584,#612,.T.);
#5742=EDGE_CURVE('',#4585,#4585,#2405,.T.);
#5743=EDGE_CURVE('',#4586,#4586,#2406,.T.);
#5744=EDGE_CURVE('',#4587,#4587,#2407,.T.);
#5745=EDGE_CURVE('',#4588,#4588,#2408,.T.);
#5746=EDGE_CURVE('',#4589,#4590,#2409,.T.);
#5747=EDGE_CURVE('',#4590,#4591,#3040,.T.);
#5748=EDGE_CURVE('',#4591,#4592,#613,.T.);
#5749=EDGE_CURVE('',#4592,#4593,#614,.T.);
#5750=EDGE_CURVE('',#4593,#4594,#3041,.T.);
#5751=EDGE_CURVE('',#4594,#4595,#615,.T.);
#5752=EDGE_CURVE('',#4595,#4596,#616,.T.);
#5753=EDGE_CURVE('',#4596,#4597,#3042,.T.);
#5754=EDGE_CURVE('',#4597,#4597,#2410,.T.);
#5755=EDGE_CURVE('',#4596,#4598,#617,.T.);
#5756=EDGE_CURVE('',#4598,#4594,#618,.T.);
#5757=EDGE_CURVE('',#4593,#4599,#619,.T.);
#5758=EDGE_CURVE('',#4599,#4591,#620,.T.);
#5759=EDGE_CURVE('',#4590,#4589,#2411,.T.);
#5760=EDGE_CURVE('',#4600,#4601,#621,.T.);
#5761=EDGE_CURVE('',#4601,#4600,#622,.T.);
#5762=EDGE_CURVE('',#4602,#4603,#623,.T.);
#5763=EDGE_CURVE('',#4603,#4602,#624,.T.);
#5764=EDGE_CURVE('',#4577,#4595,#3043,.T.);
#5765=EDGE_CURVE('',#4603,#4572,#3044,.T.);
#5766=EDGE_CURVE('',#4604,#4605,#625,.T.);
#5767=EDGE_CURVE('',#4605,#4592,#3045,.T.);
#5768=EDGE_CURVE('',#4605,#4604,#626,.T.);
#5769=EDGE_CURVE('',#4601,#4606,#3046,.T.);
#5770=EDGE_CURVE('',#4606,#4607,#627,.T.);
#5771=EDGE_CURVE('',#4607,#4606,#628,.T.);
#5772=EDGE_CURVE('',#4582,#4526,#2412,.T.);
#5773=EDGE_CURVE('',#4531,#4570,#2413,.T.);
#5774=EDGE_CURVE('',#4550,#4551,#2414,.T.);
#5775=EDGE_CURVE('',#4552,#4553,#2415,.T.);
#5776=EDGE_CURVE('',#4554,#4555,#2416,.T.);
#5777=EDGE_CURVE('',#4556,#4557,#2417,.T.);
#5778=EDGE_CURVE('',#4546,#4547,#2418,.T.);
#5779=EDGE_CURVE('',#4548,#4549,#2419,.T.);
#5780=EDGE_CURVE('',#4558,#4559,#2420,.T.);
#5781=EDGE_CURVE('',#4560,#4561,#2421,.T.);
#5782=EDGE_CURVE('',#4542,#4543,#2422,.T.);
#5783=EDGE_CURVE('',#4544,#4545,#2423,.T.);
#5784=EDGE_CURVE('',#4528,#4533,#2424,.T.);
#5785=EDGE_CURVE('',#4529,#4532,#2425,.T.);
#5786=EDGE_CURVE('',#4538,#4539,#2426,.T.);
#5787=EDGE_CURVE('',#4540,#4541,#2427,.T.);
#5788=EDGE_CURVE('',#4562,#4563,#2428,.T.);
#5789=EDGE_CURVE('',#4564,#4565,#2429,.T.);
#5790=EDGE_CURVE('',#4534,#4535,#2430,.T.);
#5791=EDGE_CURVE('',#4536,#4537,#2431,.T.);
#5792=EDGE_CURVE('',#4566,#4567,#2432,.T.);
#5793=EDGE_CURVE('',#4568,#4569,#2433,.T.);
#5794=EDGE_CURVE('',#4607,#4583,#629,.T.);
#5795=EDGE_CURVE('',#4604,#4584,#630,.T.);
#5796=EDGE_CURVE('',#4597,#4586,#3047,.T.);
#5797=EDGE_CURVE('',#4589,#4588,#3048,.T.);
#5798=EDGE_CURVE('',#4574,#4585,#3049,.T.);
#5799=EDGE_CURVE('',#4579,#4587,#3050,.T.);
#7728=ORIENTED_EDGE('',*,*,#5677,.F.);
#7729=ORIENTED_EDGE('',*,*,#5678,.T.);
#7730=ORIENTED_EDGE('',*,*,#5679,.F.);
#7731=ORIENTED_EDGE('',*,*,#5680,.F.);
#7732=ORIENTED_EDGE('',*,*,#5681,.F.);
#7733=ORIENTED_EDGE('',*,*,#5682,.T.);
#7734=ORIENTED_EDGE('',*,*,#5683,.F.);
#7735=ORIENTED_EDGE('',*,*,#5682,.F.);
#7736=ORIENTED_EDGE('',*,*,#5684,.F.);
#7737=ORIENTED_EDGE('',*,*,#5685,.F.);
#7738=ORIENTED_EDGE('',*,*,#5686,.F.);
#7739=ORIENTED_EDGE('',*,*,#5678,.F.);
#7740=ORIENTED_EDGE('',*,*,#5687,.F.);
#7741=ORIENTED_EDGE('',*,*,#5688,.F.);
#7742=ORIENTED_EDGE('',*,*,#5689,.F.);
#7743=ORIENTED_EDGE('',*,*,#5690,.F.);
#7744=ORIENTED_EDGE('',*,*,#5691,.F.);
#7745=ORIENTED_EDGE('',*,*,#5692,.F.);
#7746=ORIENTED_EDGE('',*,*,#5693,.F.);
#7747=ORIENTED_EDGE('',*,*,#5694,.F.);
#7748=ORIENTED_EDGE('',*,*,#5695,.F.);
#7749=ORIENTED_EDGE('',*,*,#5696,.F.);
#7750=ORIENTED_EDGE('',*,*,#5697,.F.);
#7751=ORIENTED_EDGE('',*,*,#5698,.F.);
#7752=ORIENTED_EDGE('',*,*,#5699,.F.);
#7753=ORIENTED_EDGE('',*,*,#5700,.F.);
#7754=ORIENTED_EDGE('',*,*,#5701,.F.);
#7755=ORIENTED_EDGE('',*,*,#5702,.F.);
#7756=ORIENTED_EDGE('',*,*,#5703,.F.);
#7757=ORIENTED_EDGE('',*,*,#5704,.F.);
#7758=ORIENTED_EDGE('',*,*,#5705,.F.);
#7759=ORIENTED_EDGE('',*,*,#5706,.F.);
#7760=ORIENTED_EDGE('',*,*,#5707,.F.);
#7761=ORIENTED_EDGE('',*,*,#5708,.F.);
#7762=ORIENTED_EDGE('',*,*,#5709,.F.);
#7763=ORIENTED_EDGE('',*,*,#5710,.F.);
#7764=ORIENTED_EDGE('',*,*,#5711,.F.);
#7765=ORIENTED_EDGE('',*,*,#5712,.F.);
#7766=ORIENTED_EDGE('',*,*,#5713,.F.);
#7767=ORIENTED_EDGE('',*,*,#5714,.F.);
#7768=ORIENTED_EDGE('',*,*,#5715,.F.);
#7769=ORIENTED_EDGE('',*,*,#5716,.F.);
#7770=ORIENTED_EDGE('',*,*,#5717,.F.);
#7771=ORIENTED_EDGE('',*,*,#5718,.F.);
#7772=ORIENTED_EDGE('',*,*,#5719,.F.);
#7773=ORIENTED_EDGE('',*,*,#5720,.F.);
#7774=ORIENTED_EDGE('',*,*,#5721,.F.);
#7775=ORIENTED_EDGE('',*,*,#5722,.F.);
#7776=ORIENTED_EDGE('',*,*,#5723,.F.);
#7777=ORIENTED_EDGE('',*,*,#5724,.T.);
#7778=ORIENTED_EDGE('',*,*,#5725,.T.);
#7779=ORIENTED_EDGE('',*,*,#5726,.T.);
#7780=ORIENTED_EDGE('',*,*,#5727,.T.);
#7781=ORIENTED_EDGE('',*,*,#5728,.T.);
#7782=ORIENTED_EDGE('',*,*,#5727,.F.);
#7783=ORIENTED_EDGE('',*,*,#5729,.T.);
#7784=ORIENTED_EDGE('',*,*,#5730,.T.);
#7785=ORIENTED_EDGE('',*,*,#5724,.F.);
#7786=ORIENTED_EDGE('',*,*,#5731,.T.);
#7787=ORIENTED_EDGE('',*,*,#5732,.T.);
#7788=ORIENTED_EDGE('',*,*,#5733,.T.);
#7789=ORIENTED_EDGE('',*,*,#5734,.T.);
#7790=ORIENTED_EDGE('',*,*,#5735,.T.);
#7791=ORIENTED_EDGE('',*,*,#5736,.T.);
#7792=ORIENTED_EDGE('',*,*,#5737,.T.);
#7793=ORIENTED_EDGE('',*,*,#5738,.F.);
#7794=ORIENTED_EDGE('',*,*,#5737,.F.);
#7795=ORIENTED_EDGE('',*,*,#5739,.T.);
#7796=ORIENTED_EDGE('',*,*,#5740,.T.);
#7797=ORIENTED_EDGE('',*,*,#5735,.F.);
#7798=ORIENTED_EDGE('',*,*,#5741,.T.);
#7799=ORIENTED_EDGE('',*,*,#5742,.T.);
#7800=ORIENTED_EDGE('',*,*,#5743,.T.);
#7801=ORIENTED_EDGE('',*,*,#5744,.T.);
#7802=ORIENTED_EDGE('',*,*,#5745,.T.);
#7803=ORIENTED_EDGE('',*,*,#5746,.T.);
#7804=ORIENTED_EDGE('',*,*,#5747,.T.);
#7805=ORIENTED_EDGE('',*,*,#5748,.T.);
#7806=ORIENTED_EDGE('',*,*,#5749,.T.);
#7807=ORIENTED_EDGE('',*,*,#5750,.T.);
#7808=ORIENTED_EDGE('',*,*,#5751,.T.);
#7809=ORIENTED_EDGE('',*,*,#5752,.T.);
#7810=ORIENTED_EDGE('',*,*,#5753,.T.);
#7811=ORIENTED_EDGE('',*,*,#5754,.T.);
#7812=ORIENTED_EDGE('',*,*,#5753,.F.);
#7813=ORIENTED_EDGE('',*,*,#5755,.T.);
#7814=ORIENTED_EDGE('',*,*,#5756,.T.);
#7815=ORIENTED_EDGE('',*,*,#5750,.F.);
#7816=ORIENTED_EDGE('',*,*,#5757,.T.);
#7817=ORIENTED_EDGE('',*,*,#5758,.T.);
#7818=ORIENTED_EDGE('',*,*,#5747,.F.);
#7819=ORIENTED_EDGE('',*,*,#5759,.T.);
#7820=ORIENTED_EDGE('',*,*,#5760,.T.);
#7821=ORIENTED_EDGE('',*,*,#5761,.T.);
#7822=ORIENTED_EDGE('',*,*,#5762,.T.);
#7823=ORIENTED_EDGE('',*,*,#5763,.T.);
#7824=ORIENTED_EDGE('',*,*,#5731,.F.);
#7825=ORIENTED_EDGE('',*,*,#5732,.F.);
#7826=ORIENTED_EDGE('',*,*,#5764,.T.);
#7827=ORIENTED_EDGE('',*,*,#5751,.F.);
#7828=ORIENTED_EDGE('',*,*,#5756,.F.);
#7829=ORIENTED_EDGE('',*,*,#5755,.F.);
#7830=ORIENTED_EDGE('',*,*,#5752,.F.);
#7831=ORIENTED_EDGE('',*,*,#5764,.F.);
#7832=ORIENTED_EDGE('',*,*,#5762,.F.);
#7833=ORIENTED_EDGE('',*,*,#5763,.F.);
#7834=ORIENTED_EDGE('',*,*,#5765,.T.);
#7835=ORIENTED_EDGE('',*,*,#5725,.F.);
#7836=ORIENTED_EDGE('',*,*,#5730,.F.);
#7837=ORIENTED_EDGE('',*,*,#5729,.F.);
#7838=ORIENTED_EDGE('',*,*,#5726,.F.);
#7839=ORIENTED_EDGE('',*,*,#5765,.F.);
#7840=ORIENTED_EDGE('',*,*,#5766,.T.);
#7841=ORIENTED_EDGE('',*,*,#5767,.T.);
#7842=ORIENTED_EDGE('',*,*,#5748,.F.);
#7843=ORIENTED_EDGE('',*,*,#5758,.F.);
#7844=ORIENTED_EDGE('',*,*,#5757,.F.);
#7845=ORIENTED_EDGE('',*,*,#5749,.F.);
#7846=ORIENTED_EDGE('',*,*,#5767,.F.);
#7847=ORIENTED_EDGE('',*,*,#5768,.T.);
#7848=ORIENTED_EDGE('',*,*,#5760,.F.);
#7849=ORIENTED_EDGE('',*,*,#5761,.F.);
#7850=ORIENTED_EDGE('',*,*,#5769,.T.);
#7851=ORIENTED_EDGE('',*,*,#5770,.T.);
#7852=ORIENTED_EDGE('',*,*,#5771,.T.);
#7853=ORIENTED_EDGE('',*,*,#5769,.F.);
#7854=ORIENTED_EDGE('',*,*,#5738,.T.);
#7855=ORIENTED_EDGE('',*,*,#5772,.T.);
#7856=ORIENTED_EDGE('',*,*,#5677,.T.);
#7857=ORIENTED_EDGE('',*,*,#5772,.F.);
#7858=ORIENTED_EDGE('',*,*,#5683,.T.);
#7859=ORIENTED_EDGE('',*,*,#5773,.T.);
#7860=ORIENTED_EDGE('',*,*,#5723,.T.);
#7861=ORIENTED_EDGE('',*,*,#5773,.F.);
#7862=ORIENTED_EDGE('',*,*,#5774,.F.);
#7863=ORIENTED_EDGE('',*,*,#5703,.T.);
#7864=ORIENTED_EDGE('',*,*,#5704,.T.);
#7865=ORIENTED_EDGE('',*,*,#5774,.T.);
#7866=ORIENTED_EDGE('',*,*,#5706,.T.);
#7867=ORIENTED_EDGE('',*,*,#5775,.F.);
#7868=ORIENTED_EDGE('',*,*,#5775,.T.);
#7869=ORIENTED_EDGE('',*,*,#5705,.T.);
#7870=ORIENTED_EDGE('',*,*,#5776,.F.);
#7871=ORIENTED_EDGE('',*,*,#5707,.T.);
#7872=ORIENTED_EDGE('',*,*,#5708,.T.);
#7873=ORIENTED_EDGE('',*,*,#5776,.T.);
#7874=ORIENTED_EDGE('',*,*,#5710,.T.);
#7875=ORIENTED_EDGE('',*,*,#5777,.F.);
#7876=ORIENTED_EDGE('',*,*,#5777,.T.);
#7877=ORIENTED_EDGE('',*,*,#5709,.T.);
#7878=ORIENTED_EDGE('',*,*,#5778,.F.);
#7879=ORIENTED_EDGE('',*,*,#5699,.T.);
#7880=ORIENTED_EDGE('',*,*,#5700,.T.);
#7881=ORIENTED_EDGE('',*,*,#5778,.T.);
#7882=ORIENTED_EDGE('',*,*,#5702,.T.);
#7883=ORIENTED_EDGE('',*,*,#5779,.F.);
#7884=ORIENTED_EDGE('',*,*,#5779,.T.);
#7885=ORIENTED_EDGE('',*,*,#5701,.T.);
#7886=ORIENTED_EDGE('',*,*,#5780,.F.);
#7887=ORIENTED_EDGE('',*,*,#5711,.T.);
#7888=ORIENTED_EDGE('',*,*,#5712,.T.);
#7889=ORIENTED_EDGE('',*,*,#5780,.T.);
#7890=ORIENTED_EDGE('',*,*,#5714,.T.);
#7891=ORIENTED_EDGE('',*,*,#5781,.F.);
#7892=ORIENTED_EDGE('',*,*,#5781,.T.);
#7893=ORIENTED_EDGE('',*,*,#5713,.T.);
#7894=ORIENTED_EDGE('',*,*,#5782,.F.);
#7895=ORIENTED_EDGE('',*,*,#5695,.T.);
#7896=ORIENTED_EDGE('',*,*,#5696,.T.);
#7897=ORIENTED_EDGE('',*,*,#5782,.T.);
#7898=ORIENTED_EDGE('',*,*,#5698,.T.);
#7899=ORIENTED_EDGE('',*,*,#5783,.F.);
#7900=ORIENTED_EDGE('',*,*,#5783,.T.);
#7901=ORIENTED_EDGE('',*,*,#5697,.T.);
#7902=ORIENTED_EDGE('',*,*,#5784,.F.);
#7903=ORIENTED_EDGE('',*,*,#5679,.T.);
#7904=ORIENTED_EDGE('',*,*,#5686,.T.);
#7905=ORIENTED_EDGE('',*,*,#5680,.T.);
#7906=ORIENTED_EDGE('',*,*,#5784,.T.);
#7907=ORIENTED_EDGE('',*,*,#5685,.T.);
#7908=ORIENTED_EDGE('',*,*,#5785,.F.);
#7909=ORIENTED_EDGE('',*,*,#5785,.T.);
#7910=ORIENTED_EDGE('',*,*,#5684,.T.);
#7911=ORIENTED_EDGE('',*,*,#5681,.T.);
#7912=ORIENTED_EDGE('',*,*,#5786,.F.);
#7913=ORIENTED_EDGE('',*,*,#5691,.T.);
#7914=ORIENTED_EDGE('',*,*,#5692,.T.);
#7915=ORIENTED_EDGE('',*,*,#5786,.T.);
#7916=ORIENTED_EDGE('',*,*,#5694,.T.);
#7917=ORIENTED_EDGE('',*,*,#5787,.F.);
#7918=ORIENTED_EDGE('',*,*,#5787,.T.);
#7919=ORIENTED_EDGE('',*,*,#5693,.T.);
#7920=ORIENTED_EDGE('',*,*,#5788,.F.);
#7921=ORIENTED_EDGE('',*,*,#5715,.T.);
#7922=ORIENTED_EDGE('',*,*,#5716,.T.);
#7923=ORIENTED_EDGE('',*,*,#5788,.T.);
#7924=ORIENTED_EDGE('',*,*,#5718,.T.);
#7925=ORIENTED_EDGE('',*,*,#5789,.F.);
#7926=ORIENTED_EDGE('',*,*,#5789,.T.);
#7927=ORIENTED_EDGE('',*,*,#5717,.T.);
#7928=ORIENTED_EDGE('',*,*,#5790,.F.);
#7929=ORIENTED_EDGE('',*,*,#5687,.T.);
#7930=ORIENTED_EDGE('',*,*,#5688,.T.);
#7931=ORIENTED_EDGE('',*,*,#5790,.T.);
#7932=ORIENTED_EDGE('',*,*,#5690,.T.);
#7933=ORIENTED_EDGE('',*,*,#5791,.F.);
#7934=ORIENTED_EDGE('',*,*,#5791,.T.);
#7935=ORIENTED_EDGE('',*,*,#5689,.T.);
#7936=ORIENTED_EDGE('',*,*,#5792,.F.);
#7937=ORIENTED_EDGE('',*,*,#5719,.T.);
#7938=ORIENTED_EDGE('',*,*,#5720,.T.);
#7939=ORIENTED_EDGE('',*,*,#5792,.T.);
#7940=ORIENTED_EDGE('',*,*,#5722,.T.);
#7941=ORIENTED_EDGE('',*,*,#5793,.F.);
#7942=ORIENTED_EDGE('',*,*,#5793,.T.);
#7943=ORIENTED_EDGE('',*,*,#5721,.T.);
#7944=ORIENTED_EDGE('',*,*,#5771,.F.);
#7945=ORIENTED_EDGE('',*,*,#5794,.T.);
#7946=ORIENTED_EDGE('',*,*,#5739,.F.);
#7947=ORIENTED_EDGE('',*,*,#5736,.F.);
#7948=ORIENTED_EDGE('',*,*,#5740,.F.);
#7949=ORIENTED_EDGE('',*,*,#5794,.F.);
#7950=ORIENTED_EDGE('',*,*,#5770,.F.);
#7951=ORIENTED_EDGE('',*,*,#5766,.F.);
#7952=ORIENTED_EDGE('',*,*,#5795,.T.);
#7953=ORIENTED_EDGE('',*,*,#5741,.F.);
#7954=ORIENTED_EDGE('',*,*,#5795,.F.);
#7955=ORIENTED_EDGE('',*,*,#5768,.F.);
#7956=ORIENTED_EDGE('',*,*,#5754,.F.);
#7957=ORIENTED_EDGE('',*,*,#5796,.T.);
#7958=ORIENTED_EDGE('',*,*,#5743,.F.);
#7959=ORIENTED_EDGE('',*,*,#5796,.F.);
#7960=ORIENTED_EDGE('',*,*,#5746,.F.);
#7961=ORIENTED_EDGE('',*,*,#5797,.T.);
#7962=ORIENTED_EDGE('',*,*,#5745,.F.);
#7963=ORIENTED_EDGE('',*,*,#5797,.F.);
#7964=ORIENTED_EDGE('',*,*,#5759,.F.);
#7965=ORIENTED_EDGE('',*,*,#5728,.F.);
#7966=ORIENTED_EDGE('',*,*,#5798,.T.);
#7967=ORIENTED_EDGE('',*,*,#5742,.F.);
#7968=ORIENTED_EDGE('',*,*,#5798,.F.);
#7969=ORIENTED_EDGE('',*,*,#5733,.F.);
#7970=ORIENTED_EDGE('',*,*,#5734,.F.);
#7971=ORIENTED_EDGE('',*,*,#5799,.T.);
#7972=ORIENTED_EDGE('',*,*,#5744,.F.);
#7973=ORIENTED_EDGE('',*,*,#5799,.F.);
#9289=CYLINDRICAL_SURFACE('',#10705,11.1);
#9290=CYLINDRICAL_SURFACE('',#10708,11.1);
#9291=CYLINDRICAL_SURFACE('',#10711,11.1);
#9292=CYLINDRICAL_SURFACE('',#10721,9.2);
#9293=CYLINDRICAL_SURFACE('',#10725,3.09999999999999);
#9294=CYLINDRICAL_SURFACE('',#10726,3.09999999999999);
#9295=CYLINDRICAL_SURFACE('',#10727,2.);
#9296=CYLINDRICAL_SURFACE('',#10728,2.);
#9297=CYLINDRICAL_SURFACE('',#10734,1.865);
#9298=CYLINDRICAL_SURFACE('',#10737,1.865);
#9299=CYLINDRICAL_SURFACE('',#10740,1.865);
#9300=CYLINDRICAL_SURFACE('',#10743,1.865);
#9301=CYLINDRICAL_SURFACE('',#10746,1.865);
#9302=CYLINDRICAL_SURFACE('',#10749,1.865);
#9303=CYLINDRICAL_SURFACE('',#10752,1.865);
#9304=CYLINDRICAL_SURFACE('',#10755,1.865);
#9305=CYLINDRICAL_SURFACE('',#10758,1.865);
#9306=CYLINDRICAL_SURFACE('',#10761,1.865);
#9636=ADVANCED_FACE('',(#1270,#496,#497,#498,#499,#500,#501,#502,#503,#504),
#9289,.T.);
#9637=ADVANCED_FACE('',(#1271,#505),#9290,.T.);
#9638=ADVANCED_FACE('',(#1272,#506),#9291,.T.);
#9639=ADVANCED_FACE('',(#1273,#507),#898,.T.);
#9640=ADVANCED_FACE('',(#1274,#508),#899,.F.);
#9641=ADVANCED_FACE('',(#1275,#509,#510),#9292,.F.);
#9642=ADVANCED_FACE('',(#1276),#9293,.F.);
#9643=ADVANCED_FACE('',(#1277),#9294,.F.);
#9644=ADVANCED_FACE('',(#1278),#9295,.F.);
#9645=ADVANCED_FACE('',(#1279),#9296,.F.);
#9646=ADVANCED_FACE('',(#1280),#388,.F.);
#9647=ADVANCED_FACE('',(#1281),#389,.F.);
#9648=ADVANCED_FACE('',(#1282),#439,.T.);
#9649=ADVANCED_FACE('',(#1283),#9297,.F.);
#9650=ADVANCED_FACE('',(#1284),#440,.T.);
#9651=ADVANCED_FACE('',(#1285),#441,.T.);
#9652=ADVANCED_FACE('',(#1286),#9298,.F.);
#9653=ADVANCED_FACE('',(#1287),#442,.T.);
#9654=ADVANCED_FACE('',(#1288),#443,.T.);
#9655=ADVANCED_FACE('',(#1289),#9299,.F.);
#9656=ADVANCED_FACE('',(#1290),#444,.T.);
#9657=ADVANCED_FACE('',(#1291),#445,.T.);
#9658=ADVANCED_FACE('',(#1292),#9300,.F.);
#9659=ADVANCED_FACE('',(#1293),#446,.T.);
#9660=ADVANCED_FACE('',(#1294),#447,.T.);
#9661=ADVANCED_FACE('',(#1295),#9301,.F.);
#9662=ADVANCED_FACE('',(#1296),#448,.T.);
#9663=ADVANCED_FACE('',(#1297),#449,.T.);
#9664=ADVANCED_FACE('',(#1298),#9302,.F.);
#9665=ADVANCED_FACE('',(#1299),#450,.T.);
#9666=ADVANCED_FACE('',(#1300),#451,.T.);
#9667=ADVANCED_FACE('',(#1301),#9303,.F.);
#9668=ADVANCED_FACE('',(#1302),#452,.T.);
#9669=ADVANCED_FACE('',(#1303),#453,.T.);
#9670=ADVANCED_FACE('',(#1304),#9304,.F.);
#9671=ADVANCED_FACE('',(#1305),#454,.T.);
#9672=ADVANCED_FACE('',(#1306),#455,.T.);
#9673=ADVANCED_FACE('',(#1307),#9305,.F.);
#9674=ADVANCED_FACE('',(#1308),#456,.T.);
#9675=ADVANCED_FACE('',(#1309),#457,.T.);
#9676=ADVANCED_FACE('',(#1310),#9306,.F.);
#9677=ADVANCED_FACE('',(#1311),#458,.T.);
#9678=ADVANCED_FACE('',(#1312),#11,.T.);
#9679=ADVANCED_FACE('',(#1313),#12,.T.);
#9680=ADVANCED_FACE('',(#1314),#355,.F.);
#9681=ADVANCED_FACE('',(#1315),#356,.F.);
#9682=ADVANCED_FACE('',(#1316),#357,.T.);
#9683=ADVANCED_FACE('',(#1317),#358,.T.);
#9951=CLOSED_SHELL('',(#9636,#9637,#9638,#9639,#9640,#9641,#9642,#9643,
#9644,#9645,#9646,#9647,#9648,#9649,#9650,#9651,#9652,#9653,#9654,#9655,
#9656,#9657,#9658,#9659,#9660,#9661,#9662,#9663,#9664,#9665,#9666,#9667,
#9668,#9669,#9670,#9671,#9672,#9673,#9674,#9675,#9676,#9677,#9678,#9679,
#9680,#9681,#9682,#9683));
#10704=AXIS2_PLACEMENT_3D('',#21093,#12521,#12522);
#10705=AXIS2_PLACEMENT_3D('',#21094,#12523,#12524);
#10706=AXIS2_PLACEMENT_3D('',#21096,#12525,#12526);
#10707=AXIS2_PLACEMENT_3D('',#21139,#12530,#12531);
#10708=AXIS2_PLACEMENT_3D('',#21771,#12551,#12552);
#10709=AXIS2_PLACEMENT_3D('',#21773,#12553,#12554);
#10710=AXIS2_PLACEMENT_3D('',#21800,#12557,#12558);
#10711=AXIS2_PLACEMENT_3D('',#21860,#12559,#12560);
#10712=AXIS2_PLACEMENT_3D('',#21863,#12561,#12562);
#10713=AXIS2_PLACEMENT_3D('',#21864,#12563,#12564);
#10714=AXIS2_PLACEMENT_3D('',#21893,#12567,#12568);
#10715=AXIS2_PLACEMENT_3D('',#21959,#12569,#12570);
#10716=AXIS2_PLACEMENT_3D('',#21961,#12571,#12572);
#10717=AXIS2_PLACEMENT_3D('',#21963,#12573,#12574);
#10718=AXIS2_PLACEMENT_3D('',#21964,#12575,#12576);
#10719=AXIS2_PLACEMENT_3D('',#21966,#12577,#12578);
#10720=AXIS2_PLACEMENT_3D('',#21968,#12579,#12580);
#10721=AXIS2_PLACEMENT_3D('',#21969,#12581,#12582);
#10722=AXIS2_PLACEMENT_3D('',#21972,#12583,#12584);
#10723=AXIS2_PLACEMENT_3D('',#22023,#12588,#12589);
#10724=AXIS2_PLACEMENT_3D('',#22066,#12590,#12591);
#10725=AXIS2_PLACEMENT_3D('',#22145,#12592,#12593);
#10726=AXIS2_PLACEMENT_3D('',#22147,#12595,#12596);
#10727=AXIS2_PLACEMENT_3D('',#22149,#12598,#12599);
#10728=AXIS2_PLACEMENT_3D('',#22206,#12601,#12602);
#10729=AXIS2_PLACEMENT_3D('',#22261,#12604,#12605);
#10730=AXIS2_PLACEMENT_3D('',#22262,#12606,#12607);
#10731=AXIS2_PLACEMENT_3D('',#22263,#12608,#12609);
#10732=AXIS2_PLACEMENT_3D('',#22264,#12610,#12611);
#10733=AXIS2_PLACEMENT_3D('',#22293,#12612,#12613);
#10734=AXIS2_PLACEMENT_3D('',#22294,#12614,#12615);
#10735=AXIS2_PLACEMENT_3D('',#22295,#12616,#12617);
#10736=AXIS2_PLACEMENT_3D('',#22352,#12618,#12619);
#10737=AXIS2_PLACEMENT_3D('',#22353,#12620,#12621);
#10738=AXIS2_PLACEMENT_3D('',#22354,#12622,#12623);
#10739=AXIS2_PLACEMENT_3D('',#22411,#12624,#12625);
#10740=AXIS2_PLACEMENT_3D('',#22412,#12626,#12627);
#10741=AXIS2_PLACEMENT_3D('',#22413,#12628,#12629);
#10742=AXIS2_PLACEMENT_3D('',#22470,#12630,#12631);
#10743=AXIS2_PLACEMENT_3D('',#22471,#12632,#12633);
#10744=AXIS2_PLACEMENT_3D('',#22472,#12634,#12635);
#10745=AXIS2_PLACEMENT_3D('',#22529,#12636,#12637);
#10746=AXIS2_PLACEMENT_3D('',#22530,#12638,#12639);
#10747=AXIS2_PLACEMENT_3D('',#22531,#12640,#12641);
#10748=AXIS2_PLACEMENT_3D('',#22588,#12642,#12643);
#10749=AXIS2_PLACEMENT_3D('',#22589,#12644,#12645);
#10750=AXIS2_PLACEMENT_3D('',#22590,#12646,#12647);
#10751=AXIS2_PLACEMENT_3D('',#22647,#12648,#12649);
#10752=AXIS2_PLACEMENT_3D('',#22648,#12650,#12651);
#10753=AXIS2_PLACEMENT_3D('',#22649,#12652,#12653);
#10754=AXIS2_PLACEMENT_3D('',#22706,#12654,#12655);
#10755=AXIS2_PLACEMENT_3D('',#22707,#12656,#12657);
#10756=AXIS2_PLACEMENT_3D('',#22708,#12658,#12659);
#10757=AXIS2_PLACEMENT_3D('',#22765,#12660,#12661);
#10758=AXIS2_PLACEMENT_3D('',#22766,#12662,#12663);
#10759=AXIS2_PLACEMENT_3D('',#22767,#12664,#12665);
#10760=AXIS2_PLACEMENT_3D('',#22824,#12666,#12667);
#10761=AXIS2_PLACEMENT_3D('',#22825,#12668,#12669);
#10762=AXIS2_PLACEMENT_3D('',#22826,#12670,#12671);
#10763=AXIS2_PLACEMENT_3D('',#23767,#12672,#12673);
#10764=AXIS2_PLACEMENT_3D('',#23769,#12675,#12676);
#10765=AXIS2_PLACEMENT_3D('',#23771,#12678,#12679);
#10766=AXIS2_PLACEMENT_3D('',#23773,#12681,#12682);
#12521=DIRECTION('axis',(0.,0.,1.));
#12522=DIRECTION('refdir',(1.,0.,0.));
#12523=DIRECTION('center_axis',(0.,-1.,0.));
#12524=DIRECTION('ref_axis',(0.,0.,-1.));
#12525=DIRECTION('center_axis',(0.,-1.,0.));
#12526=DIRECTION('ref_axis',(0.,0.,-1.));
#12527=DIRECTION('',(0.,1.,0.));
#12528=DIRECTION('',(0.,-1.,-4.68844182696434E-17));
#12529=DIRECTION('',(0.,1.,0.));
#12530=DIRECTION('center_axis',(0.,1.,0.));
#12531=DIRECTION('ref_axis',(0.,0.,1.));
#12532=DIRECTION('',(0.,1.,4.68844182696434E-17));
#12533=DIRECTION('',(4.45897315080518E-17,-1.,1.44880820167036E-17));
#12534=DIRECTION('',(-4.45897315080518E-17,1.,-1.44880820167036E-17));
#12535=DIRECTION('',(2.75579696212085E-17,-1.,-3.79302911515246E-17));
#12536=DIRECTION('',(-2.75579696212085E-17,1.,3.79302911515246E-17));
#12537=DIRECTION('',(-2.7557969621208E-17,-1.,-3.7930291151525E-17));
#12538=DIRECTION('',(2.7557969621208E-17,1.,3.7930291151525E-17));
#12539=DIRECTION('',(-4.4589731508052E-17,-1.,1.4488082016703E-17));
#12540=DIRECTION('',(4.4589731508052E-17,1.,-1.4488082016703E-17));
#12541=DIRECTION('',(0.,-1.,4.68844182696434E-17));
#12542=DIRECTION('',(0.,1.,-4.68844182696434E-17));
#12543=DIRECTION('',(-2.75579696212083E-17,-1.,3.79302911515248E-17));
#12544=DIRECTION('',(2.75579696212083E-17,1.,-3.79302911515248E-17));
#12545=DIRECTION('',(-4.45897315080519E-17,-1.,-1.44880820167033E-17));
#12546=DIRECTION('',(4.45897315080519E-17,1.,1.44880820167033E-17));
#12547=DIRECTION('',(4.45897315080521E-17,-1.,-1.44880820167027E-17));
#12548=DIRECTION('',(-4.45897315080521E-17,1.,1.44880820167027E-17));
#12549=DIRECTION('',(2.75579696212077E-17,-1.,3.79302911515252E-17));
#12550=DIRECTION('',(-2.75579696212077E-17,1.,-3.79302911515252E-17));
#12551=DIRECTION('center_axis',(0.,-1.,0.));
#12552=DIRECTION('ref_axis',(0.,0.,-1.));
#12553=DIRECTION('center_axis',(0.,-1.,0.));
#12554=DIRECTION('ref_axis',(0.,0.,-1.));
#12555=DIRECTION('',(0.,1.,0.));
#12556=DIRECTION('',(0.,1.,0.));
#12557=DIRECTION('center_axis',(0.,-1.,0.));
#12558=DIRECTION('ref_axis',(0.,0.,1.));
#12559=DIRECTION('center_axis',(0.,-1.,0.));
#12560=DIRECTION('ref_axis',(0.,0.,-1.));
#12561=DIRECTION('center_axis',(0.,1.,0.));
#12562=DIRECTION('ref_axis',(0.,0.,1.));
#12563=DIRECTION('center_axis',(0.,1.,0.));
#12564=DIRECTION('ref_axis',(0.,0.,1.));
#12565=DIRECTION('',(0.,1.,0.));
#12566=DIRECTION('',(0.,1.,0.));
#12567=DIRECTION('center_axis',(0.,1.,0.));
#12568=DIRECTION('ref_axis',(0.,0.,1.));
#12569=DIRECTION('center_axis',(0.,1.,0.));
#12570=DIRECTION('ref_axis',(0.,0.,1.));
#12571=DIRECTION('center_axis',(0.,1.,0.));
#12572=DIRECTION('ref_axis',(0.,0.,1.));
#12573=DIRECTION('center_axis',(0.,-1.,0.));
#12574=DIRECTION('ref_axis',(0.,0.,1.));
#12575=DIRECTION('center_axis',(0.,1.,0.));
#12576=DIRECTION('ref_axis',(0.,0.,1.));
#12577=DIRECTION('center_axis',(0.,-1.,0.));
#12578=DIRECTION('ref_axis',(0.,0.,1.));
#12579=DIRECTION('center_axis',(0.,1.,0.));
#12580=DIRECTION('ref_axis',(0.,0.,1.));
#12581=DIRECTION('center_axis',(0.,1.,0.));
#12582=DIRECTION('ref_axis',(0.,0.,1.));
#12583=DIRECTION('center_axis',(0.,-1.,0.));
#12584=DIRECTION('ref_axis',(0.,0.,1.));
#12585=DIRECTION('',(0.,1.,0.));
#12586=DIRECTION('',(0.,1.,0.));
#12587=DIRECTION('',(0.,1.,0.));
#12588=DIRECTION('center_axis',(0.,1.,0.));
#12589=DIRECTION('ref_axis',(0.,0.,1.));
#12590=DIRECTION('center_axis',(0.,-1.,0.));
#12591=DIRECTION('ref_axis',(0.,0.,1.));
#12592=DIRECTION('center_axis',(0.,0.,1.));
#12593=DIRECTION('ref_axis',(1.,0.,0.));
#12594=DIRECTION('',(0.,0.,1.));
#12595=DIRECTION('center_axis',(0.,0.,1.));
#12596=DIRECTION('ref_axis',(1.,0.,0.));
#12597=DIRECTION('',(0.,0.,1.));
#12598=DIRECTION('center_axis',(0.,0.,1.));
#12599=DIRECTION('ref_axis',(1.,0.,0.));
#12600=DIRECTION('',(0.,0.,1.));
#12601=DIRECTION('center_axis',(0.,0.,1.));
#12602=DIRECTION('ref_axis',(1.,0.,0.));
#12603=DIRECTION('',(0.,0.,1.));
#12604=DIRECTION('center_axis',(0.,-1.,0.));
#12605=DIRECTION('ref_axis',(0.,0.,-1.));
#12606=DIRECTION('center_axis',(1.,0.,1.22464679914735E-16));
#12607=DIRECTION('ref_axis',(-1.22464679914735E-16,0.,1.));
#12608=DIRECTION('center_axis',(0.,-1.,0.));
#12609=DIRECTION('ref_axis',(0.,0.,-1.));
#12610=DIRECTION('center_axis',(1.,0.,1.22464679914735E-16));
#12611=DIRECTION('ref_axis',(-1.22464679914735E-16,0.,1.));
#12612=DIRECTION('center_axis',(0.,-1.,0.));
#12613=DIRECTION('ref_axis',(0.,0.,-1.));
#12614=DIRECTION('center_axis',(0.,1.,-4.68844182696434E-17));
#12615=DIRECTION('ref_axis',(0.,4.68844182696434E-17,1.));
#12616=DIRECTION('center_axis',(0.,-1.,0.));
#12617=DIRECTION('ref_axis',(0.,0.,-1.));
#12618=DIRECTION('center_axis',(0.,-1.,0.));
#12619=DIRECTION('ref_axis',(0.587785252292474,0.,-0.809016994374947));
#12620=DIRECTION('center_axis',(2.75579696212083E-17,1.,-3.79302911515248E-17));
#12621=DIRECTION('ref_axis',(1.0452818112773E-33,3.79302911515248E-17,1.));
#12622=DIRECTION('center_axis',(0.,-1.,0.));
#12623=DIRECTION('ref_axis',(0.587785252292474,0.,-0.809016994374947));
#12624=DIRECTION('center_axis',(0.,-1.,0.));
#12625=DIRECTION('ref_axis',(0.951056516295154,0.,-0.309016994374945));
#12626=DIRECTION('center_axis',(4.4589731508052E-17,1.,-1.4488082016703E-17));
#12627=DIRECTION('ref_axis',(-1.,4.4589731508052E-17,-6.46019687191422E-34));
#12628=DIRECTION('center_axis',(0.,-1.,0.));
#12629=DIRECTION('ref_axis',(0.951056516295155,0.,-0.309016994374944));
#12630=DIRECTION('center_axis',(0.,-1.,0.));
#12631=DIRECTION('ref_axis',(0.951056516295152,0.,0.309016994374952));
#12632=DIRECTION('center_axis',(4.45897315080519E-17,1.,1.44880820167033E-17));
#12633=DIRECTION('ref_axis',(-1.,4.45897315080519E-17,6.46019687191434E-34));
#12634=DIRECTION('center_axis',(0.,-1.,0.));
#12635=DIRECTION('ref_axis',(0.951056516295152,0.,0.309016994374952));
#12636=DIRECTION('center_axis',(0.,-1.,0.));
#12637=DIRECTION('ref_axis',(0.587785252292469,0.,0.809016994374951));
#12638=DIRECTION('center_axis',(2.7557969621208E-17,1.,3.7930291151525E-17));
#12639=DIRECTION('ref_axis',(-0.587785252292469,4.68844182696434E-17,-0.80901699437495));
#12640=DIRECTION('center_axis',(0.,-1.,0.));
#12641=DIRECTION('ref_axis',(0.587785252292469,0.,0.809016994374951));
#12642=DIRECTION('center_axis',(0.,-1.,0.));
#12643=DIRECTION('ref_axis',(0.,0.,1.));
#12644=DIRECTION('center_axis',(0.,1.,4.68844182696434E-17));
#12645=DIRECTION('ref_axis',(-1.22464679914735E-16,4.68844182696434E-17,
-1.));
#12646=DIRECTION('center_axis',(0.,-1.,0.));
#12647=DIRECTION('ref_axis',(0.,0.,1.));
#12648=DIRECTION('center_axis',(0.,-1.,0.));
#12649=DIRECTION('ref_axis',(-0.587785252292481,0.,0.809016994374942));
#12650=DIRECTION('center_axis',(-2.75579696212085E-17,1.,3.79302911515246E-17));
#12651=DIRECTION('ref_axis',(0.58778525229248,4.68844182696434E-17,-0.809016994374942));
#12652=DIRECTION('center_axis',(0.,-1.,0.));
#12653=DIRECTION('ref_axis',(-0.587785252292481,0.,0.809016994374942));
#12654=DIRECTION('center_axis',(0.,-1.,0.));
#12655=DIRECTION('ref_axis',(-0.951056516295156,0.,0.309016994374938));
#12656=DIRECTION('center_axis',(-4.45897315080521E-17,1.,1.44880820167027E-17));
#12657=DIRECTION('ref_axis',(0.951056516295156,4.68844182696434E-17,-0.309016994374939));
#12658=DIRECTION('center_axis',(0.,-1.,0.));
#12659=DIRECTION('ref_axis',(-0.951056516295156,0.,0.309016994374938));
#12660=DIRECTION('center_axis',(0.,-1.,0.));
#12661=DIRECTION('ref_axis',(-0.95105651629515,0.,-0.309016994374958));
#12662=DIRECTION('center_axis',(-4.45897315080518E-17,1.,-1.44880820167036E-17));
#12663=DIRECTION('ref_axis',(0.95105651629515,4.68844182696434E-17,0.309016994374958));
#12664=DIRECTION('center_axis',(0.,-1.,0.));
#12665=DIRECTION('ref_axis',(-0.95105651629515,0.,-0.309016994374958));
#12666=DIRECTION('center_axis',(0.,-1.,0.));
#12667=DIRECTION('ref_axis',(-0.587785252292462,0.,-0.809016994374955));
#12668=DIRECTION('center_axis',(-2.75579696212077E-17,1.,-3.79302911515252E-17));
#12669=DIRECTION('ref_axis',(-1.04528181127729E-33,3.79302911515252E-17,
1.));
#12670=DIRECTION('center_axis',(0.,-1.,0.));
#12671=DIRECTION('ref_axis',(-0.587785252292462,0.,-0.809016994374955));
#12672=DIRECTION('center_axis',(0.,1.,0.));
#12673=DIRECTION('ref_axis',(0.,0.,1.));
#12674=DIRECTION('',(-8.65956056235505E-17,0.707106781186538,-0.707106781186557));
#12675=DIRECTION('center_axis',(0.,-1.,0.));
#12676=DIRECTION('ref_axis',(0.,0.,-1.));
#12677=DIRECTION('',(-8.65956056235496E-17,-0.707106781186545,0.70710678118655));
#12678=DIRECTION('center_axis',(0.,-1.,0.));
#12679=DIRECTION('ref_axis',(0.,0.,-1.));
#12680=DIRECTION('',(8.65956056235472E-17,0.707106781186565,-0.70710678118653));
#12681=DIRECTION('center_axis',(0.,1.,0.));
#12682=DIRECTION('ref_axis',(0.,0.,1.));
#12683=DIRECTION('',(8.65956056235519E-17,-0.707106781186527,0.707106781186568));
#21093=CARTESIAN_POINT('',(0.,0.,0.));
#21094=CARTESIAN_POINT('Origin',(0.,275.,0.));
#21095=CARTESIAN_POINT('',(-1.35935794705356E-15,13.9512489600659,11.1));
#21096=CARTESIAN_POINT('Origin',(0.,13.9512489600658,0.));
#21097=CARTESIAN_POINT('',(-9.5723472968307E-16,32.7351817276402,11.1));
#21098=CARTESIAN_POINT('',(-1.35935794705356E-15,275.,11.1));
#21099=CARTESIAN_POINT('',(-1.5009622134597,34.2419663837872,10.9980503923998));
#21100=CARTESIAN_POINT('Ctrl Pts',(-1.5009622134597,34.2419663837872,10.9980503923998));
#21101=CARTESIAN_POINT('Ctrl Pts',(-1.5009622134597,34.0448673617028,10.9980503923998));
#21102=CARTESIAN_POINT('Ctrl Pts',(-1.4771810723556,33.8362237308831,11.001402687493));
#21103=CARTESIAN_POINT('Ctrl Pts',(-1.38530410221155,33.5102351295637,11.0132837659748));
#21104=CARTESIAN_POINT('Ctrl Pts',(-1.33034819384694,33.3781157666075,11.0202692332752));
#21105=CARTESIAN_POINT('Ctrl Pts',(-1.18533576935023,33.1591718022942,11.036735456266));
#21106=CARTESIAN_POINT('Ctrl Pts',(-1.10400652085937,33.0725369802661,11.0453977168056));
#21107=CARTESIAN_POINT('Ctrl Pts',(-0.892079326680414,32.9165975969895,
11.0646884672856));
#21108=CARTESIAN_POINT('Ctrl Pts',(-0.763175852377866,32.858361072496,11.0745648140582));
#21109=CARTESIAN_POINT('Ctrl Pts',(-0.521393923343649,32.7862330357377,
11.0882585321735));
#21110=CARTESIAN_POINT('Ctrl Pts',(-0.410221375913272,32.7652602373854,
11.0929635501988));
#21111=CARTESIAN_POINT('Ctrl Pts',(-0.245516803362297,32.7459057253595,
11.0974190600975));
#21112=CARTESIAN_POINT('Ctrl Pts',(-0.190368819985243,32.741377542263,11.0985035405639));
#21113=CARTESIAN_POINT('Ctrl Pts',(-0.0911928932145138,32.7363522396234,
11.0997134708045));
#21114=CARTESIAN_POINT('Ctrl Pts',(-0.0467732754157406,32.7352238081385,
11.0999897520302));
#21115=CARTESIAN_POINT('Ctrl Pts',(-0.00166591943505573,32.735182112509,
11.0999999064775));
#21116=CARTESIAN_POINT('Ctrl Pts',(-0.000832984580003692,32.7351817276402,
11.1));
#21117=CARTESIAN_POINT('Ctrl Pts',(-5.55111512312578E-16,32.7351817276402,
11.1));
#21118=CARTESIAN_POINT('',(-1.5009622134597,71.2419663837872,10.9980503923998));
#21119=CARTESIAN_POINT('',(-1.5009622134597,52.7419663837872,10.9980503923998));
#21120=CARTESIAN_POINT('',(-2.62256926662081E-15,72.7487510399342,11.1));
#21121=CARTESIAN_POINT('Ctrl Pts',(-3.33066907387547E-15,72.7487510399342,
11.1));
#21122=CARTESIAN_POINT('Ctrl Pts',(-0.0431795099645684,72.7487510399342,
11.1));
#21123=CARTESIAN_POINT('Ctrl Pts',(-0.0864912359924271,72.7477167835041,
11.0997467925512));
#21124=CARTESIAN_POINT('Ctrl Pts',(-0.183646082354134,72.7430091857572,
11.0986122679057));
#21125=CARTESIAN_POINT('Ctrl Pts',(-0.237861556176835,72.7387110754265,
11.0975813610593));
#21126=CARTESIAN_POINT('Ctrl Pts',(-0.396947158377275,72.7206077607173,
11.093400647027));
#21127=CARTESIAN_POINT('Ctrl Pts',(-0.503286882970604,72.7013249659842,
11.0890555714104));
#21128=CARTESIAN_POINT('Ctrl Pts',(-0.733608402260413,72.6362267971513,
11.0764757024731));
#21129=CARTESIAN_POINT('Ctrl Pts',(-0.857006401108304,72.5843799091735,
11.0674274747807));
#21130=CARTESIAN_POINT('Ctrl Pts',(-1.0699564859103,72.4419884523097,11.0487859403242));
#21131=CARTESIAN_POINT('Ctrl Pts',(-1.15605156955383,72.358608719571,11.0398711384066));
#21132=CARTESIAN_POINT('Ctrl Pts',(-1.30730179997395,72.1488438578608,11.0230378127299));
#21133=CARTESIAN_POINT('Ctrl Pts',(-1.36488506375574,72.0245694303452,11.0158446286986));
#21134=CARTESIAN_POINT('Ctrl Pts',(-1.47430578438809,71.6831286857258,11.0018689838731));
#21135=CARTESIAN_POINT('Ctrl Pts',(-1.5009622134597,71.4507884295538,10.9980503923998));
#21136=CARTESIAN_POINT('Ctrl Pts',(-1.5009622134597,71.2419663837872,10.9980503923998));
#21137=CARTESIAN_POINT('',(0.,75.4487510399342,11.1));
#21138=CARTESIAN_POINT('',(-1.35935794705356E-15,275.,11.1));
#21139=CARTESIAN_POINT('Origin',(0.,75.4487510399342,0.));
#21140=CARTESIAN_POINT('',(1.5009622134597,71.2419663837872,10.9980503923998));
#21141=CARTESIAN_POINT('Ctrl Pts',(1.5009622134597,71.2419663837872,10.9980503923998));
#21142=CARTESIAN_POINT('Ctrl Pts',(1.5009622134597,71.4504917689704,10.9980503923998));
#21143=CARTESIAN_POINT('Ctrl Pts',(1.47434652131067,71.672803365615,11.0018223294187));
#21144=CARTESIAN_POINT('Ctrl Pts',(1.37309027919535,72.0047784777117,11.0148201900203));
#21145=CARTESIAN_POINT('Ctrl Pts',(1.31654601035472,72.1320608146007,11.0219331133145));
#21146=CARTESIAN_POINT('Ctrl Pts',(1.16784203699473,72.345327367031,11.0386176428475));
#21147=CARTESIAN_POINT('Ctrl Pts',(1.0837084064114,72.4299633960732,11.0474297365141));
#21148=CARTESIAN_POINT('Ctrl Pts',(0.871159298255555,72.5776598312476,11.0663360902504));
#21149=CARTESIAN_POINT('Ctrl Pts',(0.745523925005296,72.6320095746663,11.0757141514867));
#21150=CARTESIAN_POINT('Ctrl Pts',(0.512543745213089,72.6993182274867,11.088629433639));
#21151=CARTESIAN_POINT('Ctrl Pts',(0.406386833752675,72.7190769495851,11.0930577318951));
#21152=CARTESIAN_POINT('Ctrl Pts',(0.246410373793648,72.7379457354566,11.0973997874919));
#21153=CARTESIAN_POINT('Ctrl Pts',(0.191151023811988,72.7425013416222,11.0984906444422));
#21154=CARTESIAN_POINT('Ctrl Pts',(0.0918578103499711,72.7475581223538,
11.0997080150118));
#21155=CARTESIAN_POINT('Ctrl Pts',(0.0474310645609758,72.7486976181121,
11.0999869901433));
#21156=CARTESIAN_POINT('Ctrl Pts',(0.00209958546977268,72.7487504285997,
11.0999998514453));
#21157=CARTESIAN_POINT('Ctrl Pts',(0.00104983181341904,72.7487510399342,
11.1));
#21158=CARTESIAN_POINT('Ctrl Pts',(-3.33066907387547E-15,72.7487510399342,
11.1));
#21159=CARTESIAN_POINT('',(1.5009622134597,34.2419663837872,10.9980503923998));
#21160=CARTESIAN_POINT('',(1.5009622134597,52.7419663837872,10.9980503923998));
#21161=CARTESIAN_POINT('Ctrl Pts',(-5.55111512312578E-16,32.7351817276402,
11.1));
#21162=CARTESIAN_POINT('Ctrl Pts',(0.0434004817053344,32.7351817276402,
11.1));
#21163=CARTESIAN_POINT('Ctrl Pts',(0.0869359496621808,32.7362265936286,
11.0997441811035));
#21164=CARTESIAN_POINT('Ctrl Pts',(0.18441610004499,32.7409747471531,11.0986000062274));
#21165=CARTESIAN_POINT('Ctrl Pts',(0.238736148222327,32.7452987075796,11.0975630731579));
#21166=CARTESIAN_POINT('Ctrl Pts',(0.398446951974643,32.7635405469734,11.0933518720784));
#21167=CARTESIAN_POINT('Ctrl Pts',(0.505323294057922,32.7830083481295,11.0889673028681));
#21168=CARTESIAN_POINT('Ctrl Pts',(0.736910254577693,32.8488643339236,11.0762658297061));
#21169=CARTESIAN_POINT('Ctrl Pts',(0.860930452663077,32.9013952313581,11.0671267518481));
#21170=CARTESIAN_POINT('Ctrl Pts',(1.07377070841953,33.0452362980269,11.0484114414186));
#21171=CARTESIAN_POINT('Ctrl Pts',(1.15931674222104,33.1289571391808,11.0395252155594));
#21172=CARTESIAN_POINT('Ctrl Pts',(1.30985683194324,33.3396669565376,11.0227332589662));
#21173=CARTESIAN_POINT('Ctrl Pts',(1.36715456694082,33.4647551607029,11.0155618965373));
#21174=CARTESIAN_POINT('Ctrl Pts',(1.47298429182855,33.7994478579454,11.0020260798964));
#21175=CARTESIAN_POINT('Ctrl Pts',(1.5009622134597,34.0281657983113,10.9980503923998));
#21176=CARTESIAN_POINT('Ctrl Pts',(1.5009622134597,34.2419663837872,10.9980503923998));
#21177=CARTESIAN_POINT('',(-9.99594466036059,34.2419663837872,-4.82608437006737));
#21178=CARTESIAN_POINT('',(-10.923590324108,34.2419663837872,-1.97108458242009));
#21179=CARTESIAN_POINT('Ctrl Pts',(-9.99594466036059,34.2419663837872,-4.82608437006737));
#21180=CARTESIAN_POINT('Ctrl Pts',(-9.99594466036059,34.0448673617033,-4.82608437006737));
#21181=CARTESIAN_POINT('Ctrl Pts',(-10.0064816592001,33.8362237308843,-4.80450307700966));
#21182=CARTESIAN_POINT('Ctrl Pts',(-10.0461727814766,33.5102351295654,-4.72079434101999));
#21183=CARTESIAN_POINT('Ctrl Pts',(-10.0697986652978,33.3781157666092,-4.6706867943708));
#21184=CARTESIAN_POINT('Ctrl Pts',(-10.1302702775366,33.1591718022959,-4.53786012584765));
#21185=CARTESIAN_POINT('Ctrl Pts',(-10.1636406967919,33.0725369802679,-4.46318819982197));
#21186=CARTESIAN_POINT('Ctrl Pts',(-10.2474763953116,32.9165975969906,-4.26759463055083));
#21187=CARTESIAN_POINT('Ctrl Pts',(-10.2967027234606,32.8583610724967,-4.14805210033697));
#21188=CARTESIAN_POINT('Ctrl Pts',(-10.3844409483111,32.786233035738,-3.92233541281966));
#21189=CARTESIAN_POINT('Ctrl Pts',(-10.4232698928274,32.7652602373856,-3.81805796768108));
#21190=CARTESIAN_POINT('Ctrl Pts',(-10.4784038465197,32.7459057253596,-3.66279143896971));
#21191=CARTESIAN_POINT('Ctrl Pts',(-10.4964769128031,32.741377542263,-3.61067771291264));
#21192=CARTESIAN_POINT('Ctrl Pts',(-10.5282746716481,32.7363522396233,-3.51672969050312));
#21193=CARTESIAN_POINT('Ctrl Pts',(-10.5422638474917,32.7352238081385,-3.47456949913784));
#21194=CARTESIAN_POINT('Ctrl Pts',(-10.5696315831627,32.7351419995549,-3.39040474326441));
#21195=CARTESIAN_POINT('Ctrl Pts',(-10.5831009478896,32.7361860749744,-3.34812273992118));
#21196=CARTESIAN_POINT('Ctrl Pts',(-10.6123835666263,32.7409747471531,-3.25426588203641));
#21197=CARTESIAN_POINT('Ctrl Pts',(-10.6281832026957,32.7452987075796,-3.20228401631138));
#21198=CARTESIAN_POINT('Ctrl Pts',(-10.6735314650123,32.7635405469733,-3.04908868297999));
#21199=CARTESIAN_POINT('Ctrl Pts',(-10.702388097894,32.7830083481294,-2.94608833500493));
#21200=CARTESIAN_POINT('Ctrl Pts',(-10.7618725855528,32.8488643339231,-2.72191107605337));
#21201=CARTESIAN_POINT('Ctrl Pts',(-10.7915051548571,32.9013952313574,-2.60113672814137));
#21202=CARTESIAN_POINT('Ctrl Pts',(-10.8394770930345,33.0452362980253,-2.39293026699688));
#21203=CARTESIAN_POINT('Ctrl Pts',(-10.8574609682719,33.1289571391788,-2.30882515930038));
#21204=CARTESIAN_POINT('Ctrl Pts',(-10.8880103145914,33.339666956535,-2.16046402605025));
#21205=CARTESIAN_POINT('Ctrl Pts',(-10.8988959174762,33.4647551606998,-2.10375456894849));
#21206=CARTESIAN_POINT('Ctrl Pts',(-10.918725774357,33.7994478579428,-1.99892172210077));
#21207=CARTESIAN_POINT('Ctrl Pts',(-10.923590324108,34.0281657983102,-1.97108458242009));
#21208=CARTESIAN_POINT('Ctrl Pts',(-10.923590324108,34.2419663837872,-1.97108458242009));
#21209=CARTESIAN_POINT('',(-9.9959446603606,71.2419663837872,-4.82608437006737));
#21210=CARTESIAN_POINT('',(-9.99594466036059,52.7419663837872,-4.82608437006737));
#21211=CARTESIAN_POINT('',(-10.923590324108,71.2419663837872,-1.97108458242009));
#21212=CARTESIAN_POINT('Ctrl Pts',(-10.923590324108,71.2419663837872,-1.97108458242009));
#21213=CARTESIAN_POINT('Ctrl Pts',(-10.923590324108,71.4504917689707,-1.97108458242009));
#21214=CARTESIAN_POINT('Ctrl Pts',(-10.9189529481978,71.6728033656156,-1.99756320251462));
#21215=CARTESIAN_POINT('Ctrl Pts',(-10.9000247486206,72.0047784777124,-2.09788017121028));
#21216=CARTESIAN_POINT('Ctrl Pts',(-10.8893164006632,72.1320608146012,-2.15385498072772));
#21217=CARTESIAN_POINT('Ctrl Pts',(-10.8592322762978,72.345327367031,-2.30043666675911));
#21218=CARTESIAN_POINT('Ctrl Pts',(-10.8416143537529,72.4299633960731,-2.38317559106369));
#21219=CARTESIAN_POINT('Ctrl Pts',(-10.7939140781139,72.5776598312475,-2.59116419001395));
#21220=CARTESIAN_POINT('Ctrl Pts',(-10.764009678934,72.6320095746662,-2.7135485107171));
#21221=CARTESIAN_POINT('Ctrl Pts',(-10.7042980072763,72.6993182274866,-2.93911687054849));
#21222=CARTESIAN_POINT('Ctrl Pts',(-10.6757052794772,72.719076949585,-3.04144651236021));
#21223=CARTESIAN_POINT('Ctrl Pts',(-10.6303993749193,72.7379457354566,-3.19493493602834));
#21224=CARTESIAN_POINT('Ctrl Pts',(-10.6143607632876,72.7425013416222,-3.24782679425093));
#21225=CARTESIAN_POINT('Ctrl Pts',(-10.5848352611148,72.7475581223538,-3.34263644013226));
#21226=CARTESIAN_POINT('Ctrl Pts',(-10.571371962778,72.7486976181121,-3.38497499426931));
#21227=CARTESIAN_POINT('Ctrl Pts',(-10.5440464900604,72.7488007243628,-3.46915541003349));
#21228=CARTESIAN_POINT('Ctrl Pts',(-10.5300948669953,72.7477675826252,-3.51127515430947));
#21229=CARTESIAN_POINT('Ctrl Pts',(-10.4986577588269,72.7430091857572,-3.60431760807713));
#21230=CARTESIAN_POINT('Ctrl Pts',(-10.4809238053836,72.7387110754265,-3.65556102000506));
#21231=CARTESIAN_POINT('Ctrl Pts',(-10.42778755542,72.7206077607172,-3.80556850694213));
#21232=CARTESIAN_POINT('Ctrl Pts',(-10.3907943608645,72.7013249659841,-3.90536089275047));
#21233=CARTESIAN_POINT('Ctrl Pts',(-10.3076569309066,72.6362267971511,-4.12052228122571));
#21234=CARTESIAN_POINT('Ctrl Pts',(-10.2609194762829,72.5843799091732,-4.23508469600187));
#21235=CARTESIAN_POINT('Ctrl Pts',(-10.177385128307,72.4419884523094,-4.43185171084982));
#21236=CARTESIAN_POINT('Ctrl Pts',(-10.1423018038739,72.3586087195709,-4.51097817587566));
#21237=CARTESIAN_POINT('Ctrl Pts',(-10.0795534681954,72.1488438578611,-4.64962390940142));
#21238=CARTESIAN_POINT('Ctrl Pts',(-10.0549181365495,72.0245694303458,-4.70216603154109));
#21239=CARTESIAN_POINT('Ctrl Pts',(-10.0078136462567,71.6831286857266,-4.80191260915753));
#21240=CARTESIAN_POINT('Ctrl Pts',(-9.99594466036059,71.4507884295542,-4.82608437006737));
#21241=CARTESIAN_POINT('Ctrl Pts',(-9.99594466036059,71.2419663837872,-4.82608437006737));
#21242=CARTESIAN_POINT('',(-10.923590324108,52.7419663837872,-1.97108458242009));
#21243=CARTESIAN_POINT('',(-7.67879576322568,34.2419663837872,8.01536621912358));
#21244=CARTESIAN_POINT('',(-5.25018788601862,34.2419663837872,9.77985312576336));
#21245=CARTESIAN_POINT('Ctrl Pts',(-7.67879576322567,34.2419663837872,8.01536621912358));
#21246=CARTESIAN_POINT('Ctrl Pts',(-7.67879576322567,34.0448673617029,8.01536621912358));
#21247=CARTESIAN_POINT('Ctrl Pts',(-7.66152684554398,33.8362237308833,8.03205648684773));
#21248=CARTESIAN_POINT('Ctrl Pts',(-7.59418033801888,33.5102351295641,8.09567240932681));
#21249=CARTESIAN_POINT('Ctrl Pts',(-7.55382602887025,33.3781157666079,8.13362604354948));
#21250=CARTESIAN_POINT('Ctrl Pts',(-7.44618711609206,33.1591718022946,8.23218366230037));
#21251=CARTESIAN_POINT('Ctrl Pts',(-7.38548192092003,33.0725369802665,8.28699571112944));
#21252=CARTESIAN_POINT('Ctrl Pts',(-7.22536803789698,32.9165975969898,8.42716993540006));
#21253=CARTESIAN_POINT('Ctrl Pts',(-7.12688810753166,32.8583610724962,8.51092762894583));
#21254=CARTESIAN_POINT('Ctrl Pts',(-6.93933138356723,32.7862330357378,8.66412193177461));
#21255=CARTESIAN_POINT('Ctrl Pts',(-6.85215644359495,32.7652602373855,8.73327395515536));
#21256=CARTESIAN_POINT('Ctrl Pts',(-6.72152652835995,32.7459057253595,8.83368945711258));
#21257=CARTESIAN_POINT('Ctrl Pts',(-6.6775483142271,32.741377542263,8.86698199156256));
#21258=CARTESIAN_POINT('Ctrl Pts',(-6.5980244831879,32.7363522396233,8.92625499282794));
#21259=CARTESIAN_POINT('Ctrl Pts',(-6.56225065153487,32.7352238081385,8.95258770528945));
#21260=CARTESIAN_POINT('Ctrl Pts',(-6.49066230743893,32.7351419995549,9.00462430852795));
#21261=CARTESIAN_POINT('Ctrl Pts',(-6.45461199524146,32.7361860749744,9.03050029321104));
#21262=CARTESIAN_POINT('Ctrl Pts',(-6.37439764578071,32.7409747471531,9.08735308269973));
#21263=CARTESIAN_POINT('Ctrl Pts',(-6.32984230970417,32.7452987075796,9.11844270944687));
#21264=CARTESIAN_POINT('Ctrl Pts',(-6.19815827339437,32.7635405469734,9.20891143128421));
#21265=CARTESIAN_POINT('Ctrl Pts',(-6.10911631123291,32.7830083481295,9.26818457797555));
#21266=CARTESIAN_POINT('Ctrl Pts',(-5.91429278588986,32.8488643339235,9.39403227035053));
#21267=CARTESIAN_POINT('Ctrl Pts',(-5.8085865228086,32.901395231358,9.45953584447143));
#21268=CARTESIAN_POINT('Ctrl Pts',(-5.62539455535209,33.0452362980266,9.56949920370674));
#21269=CARTESIAN_POINT('Ctrl Pts',(-5.55096316769673,33.1289571391803,9.61259279303143));
#21270=CARTESIAN_POINT('Ctrl Pts',(-5.41930361233409,33.339666956537,9.6874930593962));
#21271=CARTESIAN_POINT('Ctrl Pts',(-5.36873354990731,33.4647551607023,9.71537006893975));
#21272=CARTESIAN_POINT('Ctrl Pts',(-5.27515935056375,33.7994478579448,9.76662451478779));
#21273=CARTESIAN_POINT('Ctrl Pts',(-5.25018788601862,34.0281657983111,9.77985312576336));
#21274=CARTESIAN_POINT('Ctrl Pts',(-5.25018788601862,34.2419663837872,9.77985312576336));
#21275=CARTESIAN_POINT('',(-7.67879576322568,71.2419663837872,8.01536621912358));
#21276=CARTESIAN_POINT('',(-7.67879576322568,52.7419663837872,8.01536621912358));
#21277=CARTESIAN_POINT('',(-5.25018788601862,71.2419663837872,9.77985312576336));
#21278=CARTESIAN_POINT('Ctrl Pts',(-5.25018788601862,71.2419663837872,9.77985312576336));
#21279=CARTESIAN_POINT('Ctrl Pts',(-5.25018788601862,71.4504917689704,9.77985312576336));
#21280=CARTESIAN_POINT('Ctrl Pts',(-5.27393752223651,71.6728033656151,9.76726037558861));
#21281=CARTESIAN_POINT('Ctrl Pts',(-5.36349549366727,72.0047784777118,9.71825893988788));
#21282=CARTESIAN_POINT('Ctrl Pts',(-5.41342163950681,72.1320608146007,9.69077752838638));
#21283=CARTESIAN_POINT('Ctrl Pts',(-5.54353260148699,72.3453273670309,9.61686959382355));
#21284=CARTESIAN_POINT('Ctrl Pts',(-5.61677775712631,72.4299633960731,9.57454622007711));
#21285=CARTESIAN_POINT('Ctrl Pts',(-5.79984647366443,72.5776598312476,9.46490855038957));
#21286=CARTESIAN_POINT('Ctrl Pts',(-5.90699991180841,72.6320095746663,9.39864894174127));
#21287=CARTESIAN_POINT('Ctrl Pts',(-6.10307624899109,72.6993182274867,9.27215531073132));
#21288=CARTESIAN_POINT('Ctrl Pts',(-6.19156188284057,72.719076949585,9.21334041229131));
#21289=CARTESIAN_POINT('Ctrl Pts',(-6.32353775389205,72.7379457354567,9.12282140518168));
#21290=CARTESIAN_POINT('Ctrl Pts',(-6.36888469675312,72.7425013416222,9.09122329602228));
#21291=CARTESIAN_POINT('Ctrl Pts',(-6.44993014633738,72.7475581223538,9.0338450829759));
#21292=CARTESIAN_POINT('Ctrl Pts',(-6.48603611615359,72.7486976181121,9.00795739261613));
#21293=CARTESIAN_POINT('Ctrl Pts',(-6.557652413661,72.7488007243628,8.95595614466297));
#21294=CARTESIAN_POINT('Ctrl Pts',(-6.59339938229302,72.7477675826252,8.9296716458541));
#21295=CARTESIAN_POINT('Ctrl Pts',(-6.67217341356312,72.7430091857572,8.87102147986425));
#21296=CARTESIAN_POINT('Ctrl Pts',(-6.71542870140254,72.7387110754264,8.83832040274711));
#21297=CARTESIAN_POINT('Ctrl Pts',(-6.8416742950901,72.7206077607173,8.74142996322145));
#21298=CARTESIAN_POINT('Ctrl Pts',(-6.92515096809606,72.7013249659843,8.67540980135677));
#21299=CARTESIAN_POINT('Ctrl Pts',(-7.10409072993496,72.6362267971512,8.52985288127507));
#21300=CARTESIAN_POINT('Ctrl Pts',(-7.19860339327767,72.5843799091734,8.45000118741782));
#21301=CARTESIAN_POINT('Ctrl Pts',(-7.35992641180236,72.4419884523097,8.3097509499203));
#21302=CARTESIAN_POINT('Ctrl Pts',(-7.42433880850778,72.358608719571,8.25193330320691));
#21303=CARTESIAN_POINT('Ctrl Pts',(-7.53680843474087,72.148843857861,8.14941220181591));
#21304=CARTESIAN_POINT('Ctrl Pts',(-7.57916622624129,72.0245694303456,8.1097462004612));
#21305=CARTESIAN_POINT('Ctrl Pts',(-7.65947477084994,71.6831286857259,8.03412378040701));
#21306=CARTESIAN_POINT('Ctrl Pts',(-7.67879576322567,71.4507884295537,8.01536621912358));
#21307=CARTESIAN_POINT('Ctrl Pts',(-7.67879576322567,71.2419663837872,8.01536621912358));
#21308=CARTESIAN_POINT('',(-5.25018788601862,52.7419663837872,9.77985312576336));
#21309=CARTESIAN_POINT('',(5.25018788601848,34.2419663837872,9.77985312576343));
#21310=CARTESIAN_POINT('',(7.67879576322556,34.2419663837872,8.01536621912369));
#21311=CARTESIAN_POINT('Ctrl Pts',(5.25018788601849,34.2419663837872,9.77985312576343));
#21312=CARTESIAN_POINT('Ctrl Pts',(5.25018788601848,34.0448673617023,9.77985312576343));
#21313=CARTESIAN_POINT('Ctrl Pts',(5.27139766293454,33.8362237308821,9.76858698544023));
#21314=CARTESIAN_POINT('Ctrl Pts',(5.35271121588598,33.5102351295624,9.72419505176733));
#21315=CARTESIAN_POINT('Ctrl Pts',(5.40127743435387,33.3781157666064,9.69754414106393));
#21316=CARTESIAN_POINT('Ctrl Pts',(5.5282735532022,33.1591718022934,9.6256294307783));
#21317=CARTESIAN_POINT('Ctrl Pts',(5.59916184636776,33.0725369802654,9.58483321392157));
#21318=CARTESIAN_POINT('Ctrl Pts',(5.78195336666647,32.9165975969892,9.47587207959607));
#21319=CARTESIAN_POINT('Ctrl Pts',(5.89204363899056,32.8583610724958,9.40809465081323));
#21320=CARTESIAN_POINT('Ctrl Pts',(6.09569829406898,32.7862330357376,9.27705724932768));
#21321=CARTESIAN_POINT('Ctrl Pts',(6.18840431445511,32.7652602373854,9.21551810502958));
#21322=CARTESIAN_POINT('Ctrl Pts',(6.32427199570975,32.7459057253595,9.12231176952585));
#21323=CARTESIAN_POINT('Ctrl Pts',(6.36952509309167,32.741377542263,9.09077396133064));
#21324=CARTESIAN_POINT('Ctrl Pts',(6.45047128243415,32.7363522396234,9.03345866831884));
#21325=CARTESIAN_POINT('Ctrl Pts',(6.48656990214692,32.7352238081385,9.00757298827111));
#21326=CARTESIAN_POINT('Ctrl Pts',(6.55818166766807,32.7351419995549,8.95556862185776));
#21327=CARTESIAN_POINT('Ctrl Pts',(6.59393135063794,32.7361860749744,8.92927885654121));
#21328=CARTESIAN_POINT('Ctrl Pts',(6.67278916372664,32.7409747471532,8.87055895491594));
#21329=CARTESIAN_POINT('Ctrl Pts',(6.71612551187153,32.7452987075796,8.83779153521818));
#21330=CARTESIAN_POINT('Ctrl Pts',(6.8428589844036,32.7635405469734,8.74050894690068));
#21331=CARTESIAN_POINT('Ctrl Pts',(6.92674657632628,32.7830083481296,8.67414141820088));
#21332=CARTESIAN_POINT('Ctrl Pts',(7.10663862445558,32.8488643339238,8.52774231054223));
#21333=CARTESIAN_POINT('Ctrl Pts',(7.20160125716803,32.9013952313585,8.44745139782109));
#21334=CARTESIAN_POINT('Ctrl Pts',(7.36279205769948,33.0452362980275,8.30720603020091));
#21335=CARTESIAN_POINT('Ctrl Pts',(7.42677706033756,33.1289571391813,8.24973422540444));
#21336=CARTESIAN_POINT('Ctrl Pts',(7.5386964868147,33.3396669565382,8.14766400253439));
#21337=CARTESIAN_POINT('Ctrl Pts',(7.58083610709228,33.4647551607036,8.10818348483534));
#21338=CARTESIAN_POINT('Ctrl Pts',(7.65849799963697,33.7994478579458,8.03502762759721));
#21339=CARTESIAN_POINT('Ctrl Pts',(7.67879576322556,34.0281657983116,8.01536621912369));
#21340=CARTESIAN_POINT('Ctrl Pts',(7.67879576322556,34.2419663837872,8.01536621912369));
#21341=CARTESIAN_POINT('',(5.25018788601848,71.2419663837872,9.77985312576343));
#21342=CARTESIAN_POINT('',(5.25018788601848,52.7419663837872,9.77985312576343));
#21343=CARTESIAN_POINT('',(7.67879576322556,71.2419663837872,8.01536621912369));
#21344=CARTESIAN_POINT('Ctrl Pts',(7.67879576322556,71.2419663837872,8.01536621912369));
#21345=CARTESIAN_POINT('Ctrl Pts',(7.67879576322556,71.4504917689703,8.01536621912369));
#21346=CARTESIAN_POINT('Ctrl Pts',(7.65948030491229,71.6728033656148,8.03406209159839));
#21347=CARTESIAN_POINT('Ctrl Pts',(7.58520223502748,72.0047784777117,8.10409450753346));
#21348=CARTESIAN_POINT('Ctrl Pts',(7.54363783201395,72.1320608146005,8.14308487068425));
#21349=CARTESIAN_POINT('Ctrl Pts',(7.43314071083581,72.3453273670306,8.24398894111778));
#21350=CARTESIAN_POINT('Ctrl Pts',(7.37025479259449,72.4299633960729,8.30057058192867));
#21351=CARTESIAN_POINT('Ctrl Pts',(7.20941182785805,72.5776598312474,8.44079937456493));
#21352=CARTESIAN_POINT('Ctrl Pts',(7.1132829618938,72.6320095746662,8.52223300504219));
#21353=CARTESIAN_POINT('Ctrl Pts',(6.93238944946754,72.6993182274866,8.66962400154893));
#21354=CARTESIAN_POINT('Ctrl Pts',(6.84910959243338,72.719076949585,8.7356040370796));
#21355=CARTESIAN_POINT('Ctrl Pts',(6.72223811387084,72.7379457354567,8.83314863772604));
#21356=CARTESIAN_POINT('Ctrl Pts',(6.67817355026518,72.7425013416222,8.86651179050775));
#21357=CARTESIAN_POINT('Ctrl Pts',(6.59855920561551,72.7475581223538,8.92585975051291));
#21358=CARTESIAN_POINT('Ctrl Pts',(6.56278119073521,72.7486976181121,8.95219883211764));
#21359=CARTESIAN_POINT('Ctrl Pts',(6.49119441200987,72.7488007243628,9.00424070918876));
#21360=CARTESIAN_POINT('Ctrl Pts',(6.45514994733567,72.7477675826252,9.03011573982332));
#21361=CARTESIAN_POINT('Ctrl Pts',(6.37502781041205,72.7430091857572,9.08691039756332));
#21362=CARTESIAN_POINT('Ctrl Pts',(6.33056061889071,72.7387110754265,9.11794343236385));
#21363=CARTESIAN_POINT('Ctrl Pts',(6.19940030109836,72.7206077607173,9.20806933448832));
#21364=CARTESIAN_POINT('Ctrl Pts',(6.11081568535757,72.7013249659843,9.26705901632157));
#21365=CARTESIAN_POINT('Ctrl Pts',(5.91708740064485,72.6362267971514,9.39226128088835));
#21366=CARTESIAN_POINT('Ctrl Pts',(5.81193790770809,72.5843799091737,9.45747263480139));
#21367=CARTESIAN_POINT('Ctrl Pts',(5.62870045111611,72.44198845231,9.56756023594587));
#21368=CARTESIAN_POINT('Ctrl Pts',(5.55380807622207,72.3586087195714,9.61095343015356));
#21369=CARTESIAN_POINT('Ctrl Pts',(5.42154968882926,72.1488438578613,9.68623763845605));
#21370=CARTESIAN_POINT('Ctrl Pts',(5.37073580234758,72.0245694303458,9.71426482356093));
#21371=CARTESIAN_POINT('Ctrl Pts',(5.27399790189939,71.6831286857264,9.7672741752727));
#21372=CARTESIAN_POINT('Ctrl Pts',(5.25018788601848,71.4507884295543,9.77985312576343));
#21373=CARTESIAN_POINT('Ctrl Pts',(5.25018788601848,71.2419663837872,9.77985312576343));
#21374=CARTESIAN_POINT('',(7.67879576322556,52.7419663837872,8.01536621912369));
#21375=CARTESIAN_POINT('',(10.923590324108,34.2419663837872,-1.97108458241993));
#21376=CARTESIAN_POINT('',(9.99594466036066,34.2419663837872,-4.82608437006722));
#21377=CARTESIAN_POINT('Ctrl Pts',(10.923590324108,34.2419663837872,-1.97108458241994));
#21378=CARTESIAN_POINT('Ctrl Pts',(10.923590324108,34.0448673617023,-1.97108458241993));
#21379=CARTESIAN_POINT('Ctrl Pts',(10.9194297694541,33.836223730882,-1.99473770778586));
#21380=CARTESIAN_POINT('Ctrl Pts',(10.9023378013986,33.5102351295626,-2.08578935410117));
#21381=CARTESIAN_POINT('Ctrl Pts',(10.8919990659681,33.3781157666067,-2.14021415696957));
#21382=CARTESIAN_POINT('Ctrl Pts',(10.8628480710774,33.1591718022937,-2.28321751096788));
#21383=CARTESIAN_POINT('Ctrl Pts',(10.8459542504861,33.0725369802659,-2.36324300842669));
#21384=CARTESIAN_POINT('Ctrl Pts',(10.7988117398629,32.9165975969896,-2.57075891716293));
#21385=CARTESIAN_POINT('Ctrl Pts',(10.7683713396248,32.8583610724961,-2.69640536536647));
#21386=CARTESIAN_POINT('Ctrl Pts',(10.7066801144663,32.7862330357377,-2.93058523611078));
#21387=CARTESIAN_POINT('Ctrl Pts',(10.6768006460545,32.7652602373855,-3.03777054230638));
#21388=CARTESIAN_POINT('Ctrl Pts',(10.6301415758076,32.7459057253595,-3.1957907275721));
#21389=CARTESIAN_POINT('Ctrl Pts',(10.6141313139529,32.741377542263,-3.24857469941767));
#21390=CARTESIAN_POINT('Ctrl Pts',(10.5846349791874,32.7363522396234,-3.34327049983937));
#21391=CARTESIAN_POINT('Ctrl Pts',(10.5711713214639,32.7352238081385,-3.38560144239239));
#21392=CARTESIAN_POINT('Ctrl Pts',(10.5438414824539,32.7351419995549,-3.46977851163795));
#21393=CARTESIAN_POINT('Ctrl Pts',(10.5298856894189,32.7361860749744,-3.51190246484306));
#21394=CARTESIAN_POINT('Ctrl Pts',(10.4984081487255,32.7409747471532,-3.60504614935238));
#21395=CARTESIAN_POINT('Ctrl Pts',(10.4806361487507,32.7452987075796,-3.65638715519652));
#21396=CARTESIAN_POINT('Ctrl Pts',(10.4272777059778,32.7635405469734,-3.80697982312781));
#21397=CARTESIAN_POINT('Ctrl Pts',(10.3900811268587,32.7830083481296,-3.90727035830519));
#21398=CARTESIAN_POINT('Ctrl Pts',(10.306437001565,32.8488643339237,-4.12359767513608));
#21399=CARTESIAN_POINT('Ctrl Pts',(10.259420873161,32.9013952313583,-4.23872376230644));
#21400=CARTESIAN_POINT('Ctrl Pts',(10.1758502991068,33.0452362980271,-4.43536352549553));
#21401=CARTESIAN_POINT('Ctrl Pts',(10.1409638178522,33.1289571391808,-4.51397664357904));
#21402=CARTESIAN_POINT('Ctrl Pts',(10.0784742720542,33.3396669565371,-4.65195977691635));
#21403=CARTESIAN_POINT('Ctrl Pts',(10.0539479272322,33.4647551607021,-4.70423708829116));
#21404=CARTESIAN_POINT('Ctrl Pts',(10.0083714171123,33.7994478579445,-4.8007043403884));
#21405=CARTESIAN_POINT('Ctrl Pts',(9.99594466036066,34.028165798311,-4.82608437006722));
#21406=CARTESIAN_POINT('Ctrl Pts',(9.99594466036066,34.2419663837872,-4.82608437006722));
#21407=CARTESIAN_POINT('',(10.923590324108,71.2419663837872,-1.97108458241994));
#21408=CARTESIAN_POINT('',(10.923590324108,52.7419663837872,-1.97108458241993));
#21409=CARTESIAN_POINT('',(9.99594466036066,71.2419663837872,-4.82608437006722));
#21410=CARTESIAN_POINT('Ctrl Pts',(9.99594466036066,71.2419663837872,-4.82608437006722));
#21411=CARTESIAN_POINT('Ctrl Pts',(9.99594466036066,71.4504917689704,-4.82608437006722));
#21412=CARTESIAN_POINT('Ctrl Pts',(10.0077566868326,71.6728033656151,-4.8019369352539));
#21413=CARTESIAN_POINT('Ctrl Pts',(10.0514082864556,72.0047784777116,-4.70965308619137));
#21414=CARTESIAN_POINT('Ctrl Pts',(10.0756462185105,72.1320608146004,-4.65807430502919));
#21415=CARTESIAN_POINT('Ctrl Pts',(10.1374662039433,72.3453273670303,-4.52180422533572));
#21416=CARTESIAN_POINT('Ctrl Pts',(10.1718457246956,72.4299633960724,-4.44451147442918));
#21417=CARTESIAN_POINT('Ctrl Pts',(10.2555080221753,72.5776598312471,-4.24820764469131));
#21418=CARTESIAN_POINT('Ctrl Pts',(10.3032505538534,72.632009574666,-4.13161928458072));
#21419=CARTESIAN_POINT('Ctrl Pts',(10.3875285520126,72.6993182274866,-3.91403300809339));
#21420=CARTESIAN_POINT('Ctrl Pts',(10.4245444036369,72.719076949585,-3.81444020511614));
#21421=CARTESIAN_POINT('Ctrl Pts',(10.4781093887338,72.7379457354566,-3.66363531938793));
#21422=CARTESIAN_POINT('Ctrl Pts',(10.4962229335872,72.7425013416222,-3.61141764783749));
#21423=CARTESIAN_POINT('Ctrl Pts',(10.5280640121862,72.7475581223538,-3.51736037834474));
#21424=CARTESIAN_POINT('Ctrl Pts',(10.5420579527565,72.7486976181121,-3.47519424032078));
#21425=CARTESIAN_POINT('Ctrl Pts',(10.5694311878667,72.7488007243628,-3.39102934349887));
#21426=CARTESIAN_POINT('Ctrl Pts',(10.5829014522237,72.7477675826252,-3.34875319629781));
#21427=CARTESIAN_POINT('Ctrl Pts',(10.612157279623,72.7430091857572,-3.25500200144585));
#21428=CARTESIAN_POINT('Ctrl Pts',(10.6279303317183,72.7387110754265,-3.20312145404741));
#21429=CARTESIAN_POINT('Ctrl Pts',(10.6731143910355,72.7206077607173,-3.05053014374117));
#21430=CARTESIAN_POINT('Ctrl Pts',(10.7018427606331,72.7013249659842,-2.94805235351826));
#21431=CARTESIAN_POINT('Ctrl Pts',(10.7610518579369,72.6362267971514,-2.7251161784661));
#21432=CARTESIAN_POINT('Ctrl Pts',(10.7905785607449,72.5843799091737,-2.6049616514383));
#21433=CARTESIAN_POINT('Ctrl Pts',(10.8386546030836,72.4419884523103,-2.39667353469379));
#21434=CARTESIAN_POINT('Ctrl Pts',(10.8567809666063,72.3586087195719,-2.31203741907974));
#21435=CARTESIAN_POINT('Ctrl Pts',(10.8875104141335,72.1488438578622,-2.16298811814181));
#21436=CARTESIAN_POINT('Ctrl Pts',(10.8984634966878,72.024569430347,-2.10600036378336));
#21437=CARTESIAN_POINT('Ctrl Pts',(10.9189847308192,71.6831286857275,-1.99761636264956));
#21438=CARTESIAN_POINT('Ctrl Pts',(10.923590324108,71.4507884295547,-1.97108458241993));
#21439=CARTESIAN_POINT('Ctrl Pts',(10.923590324108,71.2419663837872,-1.97108458241993));
#21440=CARTESIAN_POINT('',(9.99594466036066,52.7419663837872,-4.82608437006722));
#21441=CARTESIAN_POINT('',(1.5009622134597,34.2419663837872,-10.9980503923998));
#21442=CARTESIAN_POINT('',(-1.5009622134597,34.2419663837872,-10.9980503923998));
#21443=CARTESIAN_POINT('Ctrl Pts',(1.5009622134597,34.2419663837872,-10.9980503923998));
#21444=CARTESIAN_POINT('Ctrl Pts',(1.5009622134597,34.0448673617028,-10.9980503923998));
#21445=CARTESIAN_POINT('Ctrl Pts',(1.4771810723556,33.8362237308832,-11.001402687493));
#21446=CARTESIAN_POINT('Ctrl Pts',(1.38530410221158,33.5102351295638,-11.0132837659748));
#21447=CARTESIAN_POINT('Ctrl Pts',(1.33034819384697,33.3781157666076,-11.0202692332752));
#21448=CARTESIAN_POINT('Ctrl Pts',(1.18533576935023,33.1591718022941,-11.036735456266));
#21449=CARTESIAN_POINT('Ctrl Pts',(1.10400652085938,33.0725369802661,-11.0453977168056));
#21450=CARTESIAN_POINT('Ctrl Pts',(0.892079326680434,32.9165975969895,-11.0646884672856));
#21451=CARTESIAN_POINT('Ctrl Pts',(0.763175852377868,32.858361072496,-11.0745648140582));
#21452=CARTESIAN_POINT('Ctrl Pts',(0.521393923343685,32.7862330357377,-11.0882585321735));
#21453=CARTESIAN_POINT('Ctrl Pts',(0.410221375913344,32.7652602373854,-11.0929635501988));
#21454=CARTESIAN_POINT('Ctrl Pts',(0.245516803362354,32.7459057253595,-11.0974190600975));
#21455=CARTESIAN_POINT('Ctrl Pts',(0.190368819985358,32.741377542263,-11.0985035405639));
#21456=CARTESIAN_POINT('Ctrl Pts',(0.0911928932145149,32.7363522396234,
-11.0997134708045));
#21457=CARTESIAN_POINT('Ctrl Pts',(0.0467732754157406,32.7352238081385,
-11.0999897520302));
#21458=CARTESIAN_POINT('Ctrl Pts',(-0.0417292595203717,32.7351419995549,
-11.1000096754841));
#21459=CARTESIAN_POINT('Ctrl Pts',(-0.0861040969257631,32.7361860749744,
-11.0997539449887));
#21460=CARTESIAN_POINT('Ctrl Pts',(-0.184416100045005,32.7409747471531,
-11.0986000062274));
#21461=CARTESIAN_POINT('Ctrl Pts',(-0.238736148222333,32.7452987075796,
-11.0975630731579));
#21462=CARTESIAN_POINT('Ctrl Pts',(-0.398446951974606,32.7635405469734,
-11.0933518720784));
#21463=CARTESIAN_POINT('Ctrl Pts',(-0.505323294057916,32.7830083481295,
-11.0889673028681));
#21464=CARTESIAN_POINT('Ctrl Pts',(-0.736910254577724,32.8488643339236,
-11.0762658297061));
#21465=CARTESIAN_POINT('Ctrl Pts',(-0.860930452663105,32.9013952313582,
-11.0671267518481));
#21466=CARTESIAN_POINT('Ctrl Pts',(-1.07377070841952,33.0452362980269,-11.0484114414186));
#21467=CARTESIAN_POINT('Ctrl Pts',(-1.15931674222102,33.1289571391807,-11.0395252155594));
#21468=CARTESIAN_POINT('Ctrl Pts',(-1.30985683194327,33.3396669565376,-11.0227332589661));
#21469=CARTESIAN_POINT('Ctrl Pts',(-1.36715456694085,33.464755160703,-11.0155618965373));
#21470=CARTESIAN_POINT('Ctrl Pts',(-1.47298429182855,33.7994478579454,-11.0020260798964));
#21471=CARTESIAN_POINT('Ctrl Pts',(-1.5009622134597,34.0281657983114,-10.9980503923998));
#21472=CARTESIAN_POINT('Ctrl Pts',(-1.5009622134597,34.2419663837872,-10.9980503923998));
#21473=CARTESIAN_POINT('',(1.5009622134597,71.2419663837872,-10.9980503923998));
#21474=CARTESIAN_POINT('',(1.5009622134597,52.7419663837872,-10.9980503923998));
#21475=CARTESIAN_POINT('',(-1.5009622134597,71.2419663837872,-10.9980503923998));
#21476=CARTESIAN_POINT('Ctrl Pts',(-1.5009622134597,71.2419663837872,-10.9980503923998));
#21477=CARTESIAN_POINT('Ctrl Pts',(-1.5009622134597,71.4504917689704,-10.9980503923998));
#21478=CARTESIAN_POINT('Ctrl Pts',(-1.47434652131067,71.672803365615,-11.0018223294187));
#21479=CARTESIAN_POINT('Ctrl Pts',(-1.37309027919532,72.0047784777118,-11.0148201900203));
#21480=CARTESIAN_POINT('Ctrl Pts',(-1.31654601035469,72.1320608146007,-11.0219331133145));
#21481=CARTESIAN_POINT('Ctrl Pts',(-1.1678420369948,72.3453273670308,-11.0386176428475));
#21482=CARTESIAN_POINT('Ctrl Pts',(-1.08370840641146,72.4299633960732,-11.0474297365141));
#21483=CARTESIAN_POINT('Ctrl Pts',(-0.871159298255557,72.5776598312476,
-11.0663360902504));
#21484=CARTESIAN_POINT('Ctrl Pts',(-0.745523925005287,72.6320095746663,
-11.0757141514867));
#21485=CARTESIAN_POINT('Ctrl Pts',(-0.512543745213127,72.6993182274867,
-11.088629433639));
#21486=CARTESIAN_POINT('Ctrl Pts',(-0.40638683375279,72.7190769495851,-11.0930577318951));
#21487=CARTESIAN_POINT('Ctrl Pts',(-0.246410373793683,72.7379457354567,
-11.0973997874919));
#21488=CARTESIAN_POINT('Ctrl Pts',(-0.191151023812067,72.7425013416222,
-11.0984906444421));
#21489=CARTESIAN_POINT('Ctrl Pts',(-0.0918578103498296,72.7475581223538,
-11.0997080150118));
#21490=CARTESIAN_POINT('Ctrl Pts',(-0.047431064560685,72.7486976181121,
-11.0999869901433));
#21491=CARTESIAN_POINT('Ctrl Pts',(0.0410733038449227,72.7488007243628,
-11.1000121003192));
#21492=CARTESIAN_POINT('Ctrl Pts',(0.0854428497291022,72.7477675826252,
-11.0997590350702));
#21493=CARTESIAN_POINT('Ctrl Pts',(0.183646082354475,72.7430091857572,-11.0986122679057));
#21494=CARTESIAN_POINT('Ctrl Pts',(0.237861556176987,72.7387110754265,-11.0975813610593));
#21495=CARTESIAN_POINT('Ctrl Pts',(0.396947158376942,72.7206077607173,-11.093400647027));
#21496=CARTESIAN_POINT('Ctrl Pts',(0.503286882970486,72.7013249659843,-11.0890555714104));
#21497=CARTESIAN_POINT('Ctrl Pts',(0.733608402260471,72.6362267971513,-11.0764757024731));
#21498=CARTESIAN_POINT('Ctrl Pts',(0.857006401108316,72.5843799091735,-11.0674274747807));
#21499=CARTESIAN_POINT('Ctrl Pts',(1.0699564859103,72.4419884523097,-11.0487859403242));
#21500=CARTESIAN_POINT('Ctrl Pts',(1.15605156955383,72.358608719571,-11.0398711384066));
#21501=CARTESIAN_POINT('Ctrl Pts',(1.30730179997395,72.1488438578608,-11.0230378127299));
#21502=CARTESIAN_POINT('Ctrl Pts',(1.36488506375574,72.0245694303452,-11.0158446286986));
#21503=CARTESIAN_POINT('Ctrl Pts',(1.47430578438809,71.6831286857259,-11.0018689838731));
#21504=CARTESIAN_POINT('Ctrl Pts',(1.5009622134597,71.4507884295539,-10.9980503923998));
#21505=CARTESIAN_POINT('Ctrl Pts',(1.5009622134597,71.2419663837872,-10.9980503923998));
#21506=CARTESIAN_POINT('',(-1.5009622134597,52.7419663837872,-10.9980503923998));
#21507=CARTESIAN_POINT('',(7.67879576322562,34.2419663837872,-8.01536621912364));
#21508=CARTESIAN_POINT('',(5.25018788601855,34.2419663837872,-9.7798531257634));
#21509=CARTESIAN_POINT('Ctrl Pts',(7.67879576322562,34.2419663837872,-8.01536621912364));
#21510=CARTESIAN_POINT('Ctrl Pts',(7.67879576322562,34.0448673617025,-8.01536621912364));
#21511=CARTESIAN_POINT('Ctrl Pts',(7.66152684554386,33.8362237308826,-8.03205648684785));
#21512=CARTESIAN_POINT('Ctrl Pts',(7.59418033801855,33.5102351295631,-8.09567240932711));
#21513=CARTESIAN_POINT('Ctrl Pts',(7.55382602886988,33.3781157666071,-8.13362604354981));
#21514=CARTESIAN_POINT('Ctrl Pts',(7.44618711609161,33.1591718022939,-8.23218366230077));
#21515=CARTESIAN_POINT('Ctrl Pts',(7.38548192091953,33.072536980266,-8.2869957111299));
#21516=CARTESIAN_POINT('Ctrl Pts',(7.22536803789647,32.9165975969895,-8.42716993540051));
#21517=CARTESIAN_POINT('Ctrl Pts',(7.12688810753123,32.858361072496,-8.51092762894619));
#21518=CARTESIAN_POINT('Ctrl Pts',(6.93933138356694,32.7862330357377,-8.66412193177484));
#21519=CARTESIAN_POINT('Ctrl Pts',(6.8521564435947,32.7652602373854,-8.73327395515555));
#21520=CARTESIAN_POINT('Ctrl Pts',(6.72152652835974,32.7459057253595,-8.83368945711273));
#21521=CARTESIAN_POINT('Ctrl Pts',(6.67754831422682,32.741377542263,-8.86698199156276));
#21522=CARTESIAN_POINT('Ctrl Pts',(6.59802448318803,32.7363522396234,-8.92625499282784));
#21523=CARTESIAN_POINT('Ctrl Pts',(6.56225065153525,32.7352238081385,-8.95258770528917));
#21524=CARTESIAN_POINT('Ctrl Pts',(6.49066230743835,32.7351419995549,-9.00462430852837));
#21525=CARTESIAN_POINT('Ctrl Pts',(6.45461199524108,32.7361860749744,-9.03050029321131));
#21526=CARTESIAN_POINT('Ctrl Pts',(6.37439764578055,32.7409747471532,-9.08735308269985));
#21527=CARTESIAN_POINT('Ctrl Pts',(6.32984230970395,32.7452987075796,-9.11844270944702));
#21528=CARTESIAN_POINT('Ctrl Pts',(6.19815827339409,32.7635405469734,-9.20891143128439));
#21529=CARTESIAN_POINT('Ctrl Pts',(6.10911631123248,32.7830083481296,-9.26818457797584));
#21530=CARTESIAN_POINT('Ctrl Pts',(5.91429278588921,32.8488643339237,-9.39403227035094));
#21531=CARTESIAN_POINT('Ctrl Pts',(5.8085865228078,32.9013952313582,-9.45953584447193));
#21532=CARTESIAN_POINT('Ctrl Pts',(5.62539455535125,33.045236298027,-9.56949920370723));
#21533=CARTESIAN_POINT('Ctrl Pts',(5.55096316769597,33.1289571391809,-9.61259279303187));
#21534=CARTESIAN_POINT('Ctrl Pts',(5.41930361233357,33.3396669565375,-9.6874930593965));
#21535=CARTESIAN_POINT('Ctrl Pts',(5.36873354990689,33.4647551607027,-9.71537006893998));
#21536=CARTESIAN_POINT('Ctrl Pts',(5.27515935056357,33.7994478579451,-9.76662451478789));
#21537=CARTESIAN_POINT('Ctrl Pts',(5.25018788601855,34.0281657983112,-9.7798531257634));
#21538=CARTESIAN_POINT('Ctrl Pts',(5.25018788601855,34.2419663837872,-9.7798531257634));
#21539=CARTESIAN_POINT('',(7.67879576322562,71.2419663837872,-8.01536621912364));
#21540=CARTESIAN_POINT('',(7.67879576322562,52.7419663837872,-8.01536621912364));
#21541=CARTESIAN_POINT('',(5.25018788601855,71.2419663837872,-9.7798531257634));
#21542=CARTESIAN_POINT('Ctrl Pts',(5.25018788601855,71.2419663837872,-9.7798531257634));
#21543=CARTESIAN_POINT('Ctrl Pts',(5.25018788601855,71.4504917689702,-9.7798531257634));
#21544=CARTESIAN_POINT('Ctrl Pts',(5.27393752223632,71.6728033656147,-9.76726037558871));
#21545=CARTESIAN_POINT('Ctrl Pts',(5.36349549366685,72.0047784777112,-9.71825893988811));
#21546=CARTESIAN_POINT('Ctrl Pts',(5.4134216395063,72.1320608146002,-9.69077752838666));
#21547=CARTESIAN_POINT('Ctrl Pts',(5.54353260148639,72.3453273670305,-9.61686959382389));
#21548=CARTESIAN_POINT('Ctrl Pts',(5.61677775712566,72.4299633960727,-9.57454622007749));
#21549=CARTESIAN_POINT('Ctrl Pts',(5.79984647366373,72.5776598312473,-9.46490855038999));
#21550=CARTESIAN_POINT('Ctrl Pts',(5.90699991180771,72.6320095746661,-9.39864894174172));
#21551=CARTESIAN_POINT('Ctrl Pts',(6.10307624899076,72.6993182274866,-9.27215531073154));
#21552=CARTESIAN_POINT('Ctrl Pts',(6.19156188284038,72.719076949585,-9.21334041229143));
#21553=CARTESIAN_POINT('Ctrl Pts',(6.32353775389184,72.7379457354566,-9.12282140518183));
#21554=CARTESIAN_POINT('Ctrl Pts',(6.36888469675294,72.7425013416222,-9.09122329602241));
#21555=CARTESIAN_POINT('Ctrl Pts',(6.44993014633731,72.7475581223538,-9.03384508297595));
#21556=CARTESIAN_POINT('Ctrl Pts',(6.48603611615362,72.7486976181121,-9.00795739261611));
#21557=CARTESIAN_POINT('Ctrl Pts',(6.55765241366075,72.7488007243628,-8.95595614466315));
#21558=CARTESIAN_POINT('Ctrl Pts',(6.59339938229281,72.7477675826252,-8.92967164585425));
#21559=CARTESIAN_POINT('Ctrl Pts',(6.67217341356285,72.7430091857572,-8.87102147986445));
#21560=CARTESIAN_POINT('Ctrl Pts',(6.71542870140231,72.7387110754264,-8.83832040274729));
#21561=CARTESIAN_POINT('Ctrl Pts',(6.84167429508994,72.7206077607173,-8.74142996322158));
#21562=CARTESIAN_POINT('Ctrl Pts',(6.92515096809575,72.7013249659843,-8.67540980135703));
#21563=CARTESIAN_POINT('Ctrl Pts',(7.10409072993444,72.6362267971514,-8.52985288127551));
#21564=CARTESIAN_POINT('Ctrl Pts',(7.19860339327709,72.5843799091737,-8.45000118741832));
#21565=CARTESIAN_POINT('Ctrl Pts',(7.35992641180176,72.4419884523103,-8.30975094992083));
#21566=CARTESIAN_POINT('Ctrl Pts',(7.42433880850722,72.3586087195718,-8.2519333032074));
#21567=CARTESIAN_POINT('Ctrl Pts',(7.53680843474049,72.1488438578617,-8.14941220181626));
#21568=CARTESIAN_POINT('Ctrl Pts',(7.57916622624094,72.0245694303463,-8.10974620046152));
#21569=CARTESIAN_POINT('Ctrl Pts',(7.65947477084968,71.6831286857272,-8.03412378040726));
#21570=CARTESIAN_POINT('Ctrl Pts',(7.67879576322561,71.4507884295547,-8.01536621912364));
#21571=CARTESIAN_POINT('Ctrl Pts',(7.67879576322561,71.2419663837872,-8.01536621912364));
#21572=CARTESIAN_POINT('',(5.25018788601855,52.7419663837872,-9.7798531257634));
#21573=CARTESIAN_POINT('',(9.99594466036063,34.2419663837872,4.8260843700673));
#21574=CARTESIAN_POINT('',(10.923590324108,34.2419663837872,1.97108458242001));
#21575=CARTESIAN_POINT('Ctrl Pts',(9.99594466036063,34.2419663837872,4.82608437006729));
#21576=CARTESIAN_POINT('Ctrl Pts',(9.99594466036063,34.0448673617038,4.82608437006729));
#21577=CARTESIAN_POINT('Ctrl Pts',(10.0064816592001,33.8362237308852,4.80450307700971));
#21578=CARTESIAN_POINT('Ctrl Pts',(10.0461727814764,33.5102351295666,4.72079434102039));
#21579=CARTESIAN_POINT('Ctrl Pts',(10.0697986652976,33.3781157666103,4.67068679437128));
#21580=CARTESIAN_POINT('Ctrl Pts',(10.1302702775364,33.1591718022967,4.53786012584826));
#21581=CARTESIAN_POINT('Ctrl Pts',(10.1636406967916,33.0725369802687,4.46318819982269));
#21582=CARTESIAN_POINT('Ctrl Pts',(10.2474763953112,32.9165975969911,4.26759463055161));
#21583=CARTESIAN_POINT('Ctrl Pts',(10.2967027234602,32.858361072497,4.14805210033772));
#21584=CARTESIAN_POINT('Ctrl Pts',(10.384440948311,32.7862330357381,3.92233541281996));
#21585=CARTESIAN_POINT('Ctrl Pts',(10.4232698928273,32.7652602373856,3.81805796768124));
#21586=CARTESIAN_POINT('Ctrl Pts',(10.4784038465198,32.7459057253596,3.66279143896954));
#21587=CARTESIAN_POINT('Ctrl Pts',(10.4964769128032,32.741377542263,3.61067771291216));
#21588=CARTESIAN_POINT('Ctrl Pts',(10.528274671648,32.7363522396234,3.51672969050343));
#21589=CARTESIAN_POINT('Ctrl Pts',(10.5422638474915,32.7352238081385,3.47456949913845));
#21590=CARTESIAN_POINT('Ctrl Pts',(10.5696315831627,32.7351419995549,3.39040474326442));
#21591=CARTESIAN_POINT('Ctrl Pts',(10.5831009478896,32.7361860749744,3.34812273992123));
#21592=CARTESIAN_POINT('Ctrl Pts',(10.6123835666262,32.7409747471531,3.25426588203674));
#21593=CARTESIAN_POINT('Ctrl Pts',(10.6281832026956,32.7452987075795,3.20228401631163));
#21594=CARTESIAN_POINT('Ctrl Pts',(10.6735314650122,32.7635405469733,3.04908868298021));
#21595=CARTESIAN_POINT('Ctrl Pts',(10.7023880978939,32.7830083481293,2.94608833500536));
#21596=CARTESIAN_POINT('Ctrl Pts',(10.7618725855526,32.8488643339229,2.72191107605422));
#21597=CARTESIAN_POINT('Ctrl Pts',(10.7915051548569,32.901395231357,2.60113672814234));
#21598=CARTESIAN_POINT('Ctrl Pts',(10.8394770930343,33.0452362980247,2.39293026699778));
#21599=CARTESIAN_POINT('Ctrl Pts',(10.8574609682717,33.1289571391782,2.30882515930115));
#21600=CARTESIAN_POINT('Ctrl Pts',(10.8880103145913,33.3396669565342,2.16046402605085));
#21601=CARTESIAN_POINT('Ctrl Pts',(10.8988959174761,33.4647551606989,2.10375456894896));
#21602=CARTESIAN_POINT('Ctrl Pts',(10.918725774357,33.7994478579421,1.99892172210085));
#21603=CARTESIAN_POINT('Ctrl Pts',(10.923590324108,34.0281657983099,1.97108458242001));
#21604=CARTESIAN_POINT('Ctrl Pts',(10.923590324108,34.2419663837872,1.97108458242001));
#21605=CARTESIAN_POINT('',(9.99594466036063,71.2419663837872,4.82608437006729));
#21606=CARTESIAN_POINT('',(9.99594466036063,52.7419663837872,4.8260843700673));
#21607=CARTESIAN_POINT('',(10.923590324108,71.2419663837872,1.97108458242002));
#21608=CARTESIAN_POINT('Ctrl Pts',(10.923590324108,71.2419663837872,1.97108458242001));
#21609=CARTESIAN_POINT('Ctrl Pts',(10.923590324108,71.4504917689706,1.97108458242001));
#21610=CARTESIAN_POINT('Ctrl Pts',(10.9189529481978,71.6728033656157,1.99756320251457));
#21611=CARTESIAN_POINT('Ctrl Pts',(10.9000247486206,72.0047784777125,2.09788017121029));
#21612=CARTESIAN_POINT('Ctrl Pts',(10.8893164006632,72.1320608146013,2.15385498072775));
#21613=CARTESIAN_POINT('Ctrl Pts',(10.8592322762978,72.345327367031,2.30043666675914));
#21614=CARTESIAN_POINT('Ctrl Pts',(10.8416143537528,72.4299633960732,2.38317559106376));
#21615=CARTESIAN_POINT('Ctrl Pts',(10.7939140781138,72.5776598312476,2.59116419001411));
#21616=CARTESIAN_POINT('Ctrl Pts',(10.7640096789339,72.6320095746663,2.71354851071738));
#21617=CARTESIAN_POINT('Ctrl Pts',(10.7042980072763,72.6993182274866,2.93911687054846));
#21618=CARTESIAN_POINT('Ctrl Pts',(10.6757052794772,72.719076949585,3.04144651236001));
#21619=CARTESIAN_POINT('Ctrl Pts',(10.6303993749193,72.7379457354566,3.19493493602824));
#21620=CARTESIAN_POINT('Ctrl Pts',(10.6143607632877,72.7425013416222,3.24782679425072));
#21621=CARTESIAN_POINT('Ctrl Pts',(10.5848352611148,72.7475581223538,3.34263644013247));
#21622=CARTESIAN_POINT('Ctrl Pts',(10.5713719627778,72.7486976181121,3.38497499426978));
#21623=CARTESIAN_POINT('Ctrl Pts',(10.5440464900604,72.7488007243628,3.46915541003345));
#21624=CARTESIAN_POINT('Ctrl Pts',(10.5300948669954,72.7477675826252,3.51127515430942));
#21625=CARTESIAN_POINT('Ctrl Pts',(10.4986577588269,72.7430091857572,3.60431760807724));
#21626=CARTESIAN_POINT('Ctrl Pts',(10.4809238053836,72.7387110754264,3.65556102000509));
#21627=CARTESIAN_POINT('Ctrl Pts',(10.4277875554201,72.7206077607172,3.80556850694187));
#21628=CARTESIAN_POINT('Ctrl Pts',(10.3907943608646,72.7013249659841,3.9053608927504));
#21629=CARTESIAN_POINT('Ctrl Pts',(10.3076569309066,72.636226797151,4.12052228122582));
#21630=CARTESIAN_POINT('Ctrl Pts',(10.2609194762829,72.5843799091731,4.23508469600199));
#21631=CARTESIAN_POINT('Ctrl Pts',(10.177385128307,72.4419884523093,4.43185171084991));
#21632=CARTESIAN_POINT('Ctrl Pts',(10.1423018038739,72.3586087195708,4.51097817587572));
#21633=CARTESIAN_POINT('Ctrl Pts',(10.0795534681954,72.1488438578609,4.64962390940149));
#21634=CARTESIAN_POINT('Ctrl Pts',(10.0549181365495,72.0245694303455,4.70216603154115));
#21635=CARTESIAN_POINT('Ctrl Pts',(10.0078136462567,71.6831286857264,4.80191260915748));
#21636=CARTESIAN_POINT('Ctrl Pts',(9.99594466036063,71.4507884295541,4.8260843700673));
#21637=CARTESIAN_POINT('Ctrl Pts',(9.99594466036063,71.2419663837872,4.8260843700673));
#21638=CARTESIAN_POINT('',(10.923590324108,52.7419663837872,1.97108458242001));
#21639=CARTESIAN_POINT('',(-10.923590324108,34.2419663837872,1.97108458241986));
#21640=CARTESIAN_POINT('',(-9.99594466036069,34.2419663837872,4.82608437006716));
#21641=CARTESIAN_POINT('Ctrl Pts',(-10.923590324108,34.2419663837872,1.97108458241986));
#21642=CARTESIAN_POINT('Ctrl Pts',(-10.923590324108,34.0448673617026,1.97108458241986));
#21643=CARTESIAN_POINT('Ctrl Pts',(-10.9194297694542,33.8362237308825,1.99473770778571));
#21644=CARTESIAN_POINT('Ctrl Pts',(-10.9023378013987,33.5102351295631,2.08578935410087));
#21645=CARTESIAN_POINT('Ctrl Pts',(-10.8919990659682,33.3781157666071,2.14021415696922));
#21646=CARTESIAN_POINT('Ctrl Pts',(-10.8628480710775,33.1591718022942,2.28321751096736));
#21647=CARTESIAN_POINT('Ctrl Pts',(-10.8459542504862,33.0725369802663,2.36324300842611));
#21648=CARTESIAN_POINT('Ctrl Pts',(-10.798811739863,32.9165975969897,2.57075891716242));
#21649=CARTESIAN_POINT('Ctrl Pts',(-10.7683713396249,32.8583610724962,2.69640536536613));
#21650=CARTESIAN_POINT('Ctrl Pts',(-10.7066801144664,32.7862330357378,2.93058523611043));
#21651=CARTESIAN_POINT('Ctrl Pts',(-10.6768006460546,32.7652602373855,3.03777054230603));
#21652=CARTESIAN_POINT('Ctrl Pts',(-10.6301415758076,32.7459057253595,3.19579072757192));
#21653=CARTESIAN_POINT('Ctrl Pts',(-10.6141313139529,32.741377542263,3.24857469941753));
#21654=CARTESIAN_POINT('Ctrl Pts',(-10.5846349791873,32.7363522396233,3.34327049983945));
#21655=CARTESIAN_POINT('Ctrl Pts',(-10.5711713214638,32.7352238081385,3.3856014423927));
#21656=CARTESIAN_POINT('Ctrl Pts',(-10.5438414824541,32.7351419995549,3.46977851163747));
#21657=CARTESIAN_POINT('Ctrl Pts',(-10.529885689419,32.7361860749744,3.51190246484276));
#21658=CARTESIAN_POINT('Ctrl Pts',(-10.4984081487255,32.7409747471532,3.60504614935233));
#21659=CARTESIAN_POINT('Ctrl Pts',(-10.4806361487507,32.7452987075796,3.65638715519642));
#21660=CARTESIAN_POINT('Ctrl Pts',(-10.4272777059778,32.7635405469734,3.80697982312774));
#21661=CARTESIAN_POINT('Ctrl Pts',(-10.3900811268588,32.7830083481296,3.90727035830497));
#21662=CARTESIAN_POINT('Ctrl Pts',(-10.3064370015652,32.8488643339236,4.12359767513566));
#21663=CARTESIAN_POINT('Ctrl Pts',(-10.2594208731612,32.9013952313582,4.23872376230597));
#21664=CARTESIAN_POINT('Ctrl Pts',(-10.175850299107,33.0452362980267,4.43536352549505));
#21665=CARTESIAN_POINT('Ctrl Pts',(-10.1409638178524,33.1289571391804,4.5139766435786));
#21666=CARTESIAN_POINT('Ctrl Pts',(-10.0784742720544,33.3396669565366,4.651959776916));
#21667=CARTESIAN_POINT('Ctrl Pts',(-10.0539479272323,33.4647551607016,4.70423708829085));
#21668=CARTESIAN_POINT('Ctrl Pts',(-10.0083714171123,33.7994478579441,4.80070434038827));
#21669=CARTESIAN_POINT('Ctrl Pts',(-9.99594466036069,34.0281657983108,4.82608437006716));
#21670=CARTESIAN_POINT('Ctrl Pts',(-9.99594466036069,34.2419663837872,4.82608437006716));
#21671=CARTESIAN_POINT('',(-10.923590324108,71.2419663837872,1.97108458241986));
#21672=CARTESIAN_POINT('',(-10.923590324108,52.7419663837872,1.97108458241986));
#21673=CARTESIAN_POINT('',(-9.9959446603607,71.2419663837872,4.82608437006716));
#21674=CARTESIAN_POINT('Ctrl Pts',(-9.9959446603607,71.2419663837872,4.82608437006716));
#21675=CARTESIAN_POINT('Ctrl Pts',(-9.9959446603607,71.4504917689704,4.82608437006716));
#21676=CARTESIAN_POINT('Ctrl Pts',(-10.0077566868326,71.6728033656151,4.80193693525385));
#21677=CARTESIAN_POINT('Ctrl Pts',(-10.0514082864556,72.0047784777117,4.7096530861913));
#21678=CARTESIAN_POINT('Ctrl Pts',(-10.0756462185106,72.1320608146004,4.65807430502912));
#21679=CARTESIAN_POINT('Ctrl Pts',(-10.1374662039434,72.3453273670303,4.52180422533563));
#21680=CARTESIAN_POINT('Ctrl Pts',(-10.1718457246957,72.4299633960725,4.44451147442909));
#21681=CARTESIAN_POINT('Ctrl Pts',(-10.2555080221753,72.5776598312471,4.24820764469124));
#21682=CARTESIAN_POINT('Ctrl Pts',(-10.3032505538534,72.632009574666,4.13161928458065));
#21683=CARTESIAN_POINT('Ctrl Pts',(-10.3875285520126,72.6993182274865,3.91403300809335));
#21684=CARTESIAN_POINT('Ctrl Pts',(-10.4245444036369,72.719076949585,3.8144402051162));
#21685=CARTESIAN_POINT('Ctrl Pts',(-10.4781093887339,72.7379457354566,3.66363531938785));
#21686=CARTESIAN_POINT('Ctrl Pts',(-10.4962229335872,72.7425013416222,3.6114176478374));
#21687=CARTESIAN_POINT('Ctrl Pts',(-10.5280640121862,72.7475581223538,3.51736037834474));
#21688=CARTESIAN_POINT('Ctrl Pts',(-10.5420579527565,72.7486976181121,3.47519424032086));
#21689=CARTESIAN_POINT('Ctrl Pts',(-10.5694311878668,72.7488007243628,3.39102934349868));
#21690=CARTESIAN_POINT('Ctrl Pts',(-10.5829014522237,72.7477675826252,3.34875319629768));
#21691=CARTESIAN_POINT('Ctrl Pts',(-10.6121572796231,72.7430091857572,3.25500200144533));
#21692=CARTESIAN_POINT('Ctrl Pts',(-10.6279303317184,72.7387110754265,3.20312145404714));
#21693=CARTESIAN_POINT('Ctrl Pts',(-10.6731143910354,72.7206077607173,3.05053014374159));
#21694=CARTESIAN_POINT('Ctrl Pts',(-10.701842760633,72.7013249659843,2.9480523535184));
#21695=CARTESIAN_POINT('Ctrl Pts',(-10.7610518579369,72.6362267971514,2.72511617846599));
#21696=CARTESIAN_POINT('Ctrl Pts',(-10.7905785607449,72.5843799091737,2.6049616514383));
#21697=CARTESIAN_POINT('Ctrl Pts',(-10.8386546030836,72.4419884523103,2.39667353469383));
#21698=CARTESIAN_POINT('Ctrl Pts',(-10.8567809666063,72.358608719572,2.31203741907976));
#21699=CARTESIAN_POINT('Ctrl Pts',(-10.8875104141335,72.1488438578622,2.1629881181418));
#21700=CARTESIAN_POINT('Ctrl Pts',(-10.8984634966878,72.024569430347,2.10600036378334));
#21701=CARTESIAN_POINT('Ctrl Pts',(-10.9189847308192,71.6831286857275,1.9976163626495));
#21702=CARTESIAN_POINT('Ctrl Pts',(-10.923590324108,71.4507884295547,1.97108458241986));
#21703=CARTESIAN_POINT('Ctrl Pts',(-10.923590324108,71.2419663837872,1.97108458241986));
#21704=CARTESIAN_POINT('',(-9.99594466036069,52.7419663837872,4.82608437006716));
#21705=CARTESIAN_POINT('',(-5.25018788601841,34.2419663837872,-9.77985312576347));
#21706=CARTESIAN_POINT('',(-7.6787957632255,34.2419663837872,-8.01536621912375));
#21707=CARTESIAN_POINT('Ctrl Pts',(-5.25018788601841,34.2419663837872,-9.77985312576347));
#21708=CARTESIAN_POINT('Ctrl Pts',(-5.25018788601841,34.0448673617023,-9.77985312576347));
#21709=CARTESIAN_POINT('Ctrl Pts',(-5.27139766293447,33.8362237308821,-9.76858698544027));
#21710=CARTESIAN_POINT('Ctrl Pts',(-5.35271121588592,33.5102351295624,-9.72419505176736));
#21711=CARTESIAN_POINT('Ctrl Pts',(-5.40127743435383,33.3781157666064,-9.69754414106396));
#21712=CARTESIAN_POINT('Ctrl Pts',(-5.52827355320222,33.1591718022933,-9.62562943077829));
#21713=CARTESIAN_POINT('Ctrl Pts',(-5.59916184636777,33.0725369802653,-9.58483321392156));
#21714=CARTESIAN_POINT('Ctrl Pts',(-5.78195336666643,32.9165975969892,-9.47587207959609));
#21715=CARTESIAN_POINT('Ctrl Pts',(-5.89204363899044,32.8583610724958,-9.4080946508133));
#21716=CARTESIAN_POINT('Ctrl Pts',(-6.09569829406892,32.7862330357376,-9.27705724932772));
#21717=CARTESIAN_POINT('Ctrl Pts',(-6.18840431445502,32.7652602373854,-9.21551810502964));
#21718=CARTESIAN_POINT('Ctrl Pts',(-6.32427199570981,32.7459057253595,-9.1223117695258));
#21719=CARTESIAN_POINT('Ctrl Pts',(-6.3695250930919,32.741377542263,-9.09077396133048));
#21720=CARTESIAN_POINT('Ctrl Pts',(-6.45047128243422,32.7363522396233,-9.03345866831879));
#21721=CARTESIAN_POINT('Ctrl Pts',(-6.48656990214715,32.7352238081385,-9.00757298827094));
#21722=CARTESIAN_POINT('Ctrl Pts',(-6.55818166766781,32.7351419995549,-8.95556862185794));
#21723=CARTESIAN_POINT('Ctrl Pts',(-6.59393135063778,32.7361860749744,-8.92927885654133));
#21724=CARTESIAN_POINT('Ctrl Pts',(-6.67278916372665,32.7409747471532,-8.87055895491593));
#21725=CARTESIAN_POINT('Ctrl Pts',(-6.7161255118715,32.7452987075796,-8.8377915352182));
#21726=CARTESIAN_POINT('Ctrl Pts',(-6.84285898440345,32.7635405469734,-8.7405089469008));
#21727=CARTESIAN_POINT('Ctrl Pts',(-6.9267465763262,32.7830083481296,-8.67414141820095));
#21728=CARTESIAN_POINT('Ctrl Pts',(-7.1066386244556,32.8488643339238,-8.52774231054221));
#21729=CARTESIAN_POINT('Ctrl Pts',(-7.20160125716801,32.9013952313585,-8.44745139782109));
#21730=CARTESIAN_POINT('Ctrl Pts',(-7.36279205769945,33.0452362980275,-8.30720603020093));
#21731=CARTESIAN_POINT('Ctrl Pts',(-7.42677706033752,33.1289571391814,-8.24973422540447));
#21732=CARTESIAN_POINT('Ctrl Pts',(-7.53869648681466,33.3396669565382,-8.14766400253443));
#21733=CARTESIAN_POINT('Ctrl Pts',(-7.58083610709224,33.4647551607036,-8.10818348483539));
#21734=CARTESIAN_POINT('Ctrl Pts',(-7.65849799963691,33.7994478579459,-8.03502762759727));
#21735=CARTESIAN_POINT('Ctrl Pts',(-7.6787957632255,34.0281657983116,-8.01536621912375));
#21736=CARTESIAN_POINT('Ctrl Pts',(-7.6787957632255,34.2419663837872,-8.01536621912375));
#21737=CARTESIAN_POINT('',(-5.25018788601841,71.2419663837872,-9.77985312576347));
#21738=CARTESIAN_POINT('',(-5.25018788601841,52.7419663837872,-9.77985312576347));
#21739=CARTESIAN_POINT('',(-7.6787957632255,71.2419663837872,-8.01536621912375));
#21740=CARTESIAN_POINT('Ctrl Pts',(-7.6787957632255,71.2419663837872,-8.01536621912375));
#21741=CARTESIAN_POINT('Ctrl Pts',(-7.6787957632255,71.4504917689704,-8.01536621912375));
#21742=CARTESIAN_POINT('Ctrl Pts',(-7.65948030491215,71.672803365615,-8.03406209159852));
#21743=CARTESIAN_POINT('Ctrl Pts',(-7.58520223502721,72.0047784777118,-8.10409450753371));
#21744=CARTESIAN_POINT('Ctrl Pts',(-7.5436378320136,72.1320608146008,-8.14308487068458));
#21745=CARTESIAN_POINT('Ctrl Pts',(-7.43314071083521,72.3453273670311,-8.24398894111832));
#21746=CARTESIAN_POINT('Ctrl Pts',(-7.37025479259382,72.4299633960733,-8.30057058192927));
#21747=CARTESIAN_POINT('Ctrl Pts',(-7.20941182785736,72.5776598312477,-8.44079937456552));
#21748=CARTESIAN_POINT('Ctrl Pts',(-7.11328296189318,72.6320095746664,-8.5222330050427));
#21749=CARTESIAN_POINT('Ctrl Pts',(-6.93238944946695,72.6993182274868,-8.6696240015494));
#21750=CARTESIAN_POINT('Ctrl Pts',(-6.84910959243269,72.7190769495851,-8.73560403708014));
#21751=CARTESIAN_POINT('Ctrl Pts',(-6.72223811387062,72.7379457354566,-8.8331486377262));
#21752=CARTESIAN_POINT('Ctrl Pts',(-6.67817355026513,72.7425013416222,-8.86651179050778));
#21753=CARTESIAN_POINT('Ctrl Pts',(-6.59855920561544,72.7475581223538,-8.92585975051296));
#21754=CARTESIAN_POINT('Ctrl Pts',(-6.56278119073531,72.7486976181121,-8.95219883211757));
#21755=CARTESIAN_POINT('Ctrl Pts',(-6.49119441201008,72.7488007243628,-9.00424070918861));
#21756=CARTESIAN_POINT('Ctrl Pts',(-6.45514994733573,72.7477675826252,-9.03011573982327));
#21757=CARTESIAN_POINT('Ctrl Pts',(-6.3750278104121,72.7430091857572,-9.08691039756328));
#21758=CARTESIAN_POINT('Ctrl Pts',(-6.33056061889071,72.7387110754265,-9.11794343236385));
#21759=CARTESIAN_POINT('Ctrl Pts',(-6.19940030109833,72.7206077607173,-9.20806933448834));
#21760=CARTESIAN_POINT('Ctrl Pts',(-6.11081568535744,72.7013249659842,-9.26705901632166));
#21761=CARTESIAN_POINT('Ctrl Pts',(-5.9170874006442,72.6362267971512,-9.39226128088876));
#21762=CARTESIAN_POINT('Ctrl Pts',(-5.81193790770756,72.5843799091733,-9.45747263480172));
#21763=CARTESIAN_POINT('Ctrl Pts',(-5.62870045111564,72.4419884523096,-9.56756023594614));
#21764=CARTESIAN_POINT('Ctrl Pts',(-5.55380807622163,72.358608719571,-9.61095343015381));
#21765=CARTESIAN_POINT('Ctrl Pts',(-5.42154968882878,72.1488438578607,-9.68623763845631));
#21766=CARTESIAN_POINT('Ctrl Pts',(-5.37073580234716,72.0245694303451,-9.71426482356116));
#21767=CARTESIAN_POINT('Ctrl Pts',(-5.27399790189915,71.6831286857257,-9.76727417527282));
#21768=CARTESIAN_POINT('Ctrl Pts',(-5.25018788601841,71.4507884295538,-9.77985312576347));
#21769=CARTESIAN_POINT('Ctrl Pts',(-5.25018788601841,71.2419663837872,-9.77985312576347));
#21770=CARTESIAN_POINT('',(-7.6787957632255,52.7419663837872,-8.01536621912375));
#21771=CARTESIAN_POINT('Origin',(0.,275.,0.));
#21772=CARTESIAN_POINT('',(-1.35935794705356E-15,76.9512489600658,11.1));
#21773=CARTESIAN_POINT('Origin',(0.,76.9512489600658,0.));
#21774=CARTESIAN_POINT('',(-1.20009601631982E-15,261.7,11.1));
#21775=CARTESIAN_POINT('',(-1.35935794705356E-15,275.,11.1));
#21776=CARTESIAN_POINT('',(-3.1,264.8,10.6583300755794));
#21777=CARTESIAN_POINT('Ctrl Pts',(-2.22044604925031E-15,261.7,11.1));
#21778=CARTESIAN_POINT('Ctrl Pts',(-0.391454890651857,261.7,11.1));
#21779=CARTESIAN_POINT('Ctrl Pts',(-0.807604729509082,261.77865672835,11.0772325011544));
#21780=CARTESIAN_POINT('Ctrl Pts',(-1.57079416556834,262.095680105178,10.9949948149978));
#21781=CARTESIAN_POINT('Ctrl Pts',(-1.91799680212002,262.333934758763,10.9366096412455));
#21782=CARTESIAN_POINT('Ctrl Pts',(-2.46612584114063,262.882063797784,10.8261904693255));
#21783=CARTESIAN_POINT('Ctrl Pts',(-2.70433342241585,263.229241539378,10.7667771783582));
#21784=CARTESIAN_POINT('Ctrl Pts',(-3.02132222583929,263.992341466568,10.682159098241));
#21785=CARTESIAN_POINT('Ctrl Pts',(-3.09999999999999,264.408458543047,10.6583300755794));
#21786=CARTESIAN_POINT('Ctrl Pts',(-3.1,264.8,10.6583300755794));
#21787=CARTESIAN_POINT('',(-1.2694849553589E-15,267.9,11.1));
#21788=CARTESIAN_POINT('Ctrl Pts',(-3.09999999999999,264.8,10.6583300755794));
#21789=CARTESIAN_POINT('Ctrl Pts',(-3.09999999999999,265.191541456953,10.6583300755794));
#21790=CARTESIAN_POINT('Ctrl Pts',(-3.02132222583929,265.607658533432,10.682159098241));
#21791=CARTESIAN_POINT('Ctrl Pts',(-2.70433342241585,266.370758460622,10.7667771783582));
#21792=CARTESIAN_POINT('Ctrl Pts',(-2.46612584114063,266.717936202216,10.8261904693255));
#21793=CARTESIAN_POINT('Ctrl Pts',(-1.91799680212002,267.266065241237,10.9366096412455));
#21794=CARTESIAN_POINT('Ctrl Pts',(-1.57079416556834,267.504319894822,10.9949948149978));
#21795=CARTESIAN_POINT('Ctrl Pts',(-0.807604729509082,267.821343271651,
11.0772325011544));
#21796=CARTESIAN_POINT('Ctrl Pts',(-0.391454890651854,267.9,11.1));
#21797=CARTESIAN_POINT('Ctrl Pts',(0.,267.9,11.1));
#21798=CARTESIAN_POINT('',(0.,274.5,11.1));
#21799=CARTESIAN_POINT('',(-1.35935794705356E-15,275.,11.1));
#21800=CARTESIAN_POINT('Origin',(0.,274.5,0.));
#21801=CARTESIAN_POINT('',(3.09999999999999,264.8,10.6583300755794));
#21802=CARTESIAN_POINT('Ctrl Pts',(1.04083408558608E-15,267.9,11.1));
#21803=CARTESIAN_POINT('Ctrl Pts',(0.391454890651855,267.9,11.1));
#21804=CARTESIAN_POINT('Ctrl Pts',(0.807604729509082,267.821343271651,11.0772325011544));
#21805=CARTESIAN_POINT('Ctrl Pts',(1.57079416556834,267.504319894822,10.9949948149978));
#21806=CARTESIAN_POINT('Ctrl Pts',(1.91799680212002,267.266065241237,10.9366096412455));
#21807=CARTESIAN_POINT('Ctrl Pts',(2.46612584114063,266.717936202216,10.8261904693255));
#21808=CARTESIAN_POINT('Ctrl Pts',(2.70433342241585,266.370758460622,10.7667771783582));
#21809=CARTESIAN_POINT('Ctrl Pts',(3.02132222583929,265.607658533432,10.682159098241));
#21810=CARTESIAN_POINT('Ctrl Pts',(3.1,265.191541456953,10.6583300755794));
#21811=CARTESIAN_POINT('Ctrl Pts',(3.1,264.8,10.6583300755794));
#21812=CARTESIAN_POINT('Ctrl Pts',(3.09999999999999,264.8,10.6583300755794));
#21813=CARTESIAN_POINT('Ctrl Pts',(3.09999999999999,264.408458543047,10.6583300755794));
#21814=CARTESIAN_POINT('Ctrl Pts',(3.02132222583929,263.992341466568,10.682159098241));
#21815=CARTESIAN_POINT('Ctrl Pts',(2.70433342241585,263.229241539378,10.7667771783582));
#21816=CARTESIAN_POINT('Ctrl Pts',(2.46612584114063,262.882063797784,10.8261904693255));
#21817=CARTESIAN_POINT('Ctrl Pts',(1.91799680212002,262.333934758763,10.9366096412455));
#21818=CARTESIAN_POINT('Ctrl Pts',(1.57079416556834,262.095680105178,10.9949948149978));
#21819=CARTESIAN_POINT('Ctrl Pts',(0.807604729509083,261.77865672835,11.0772325011544));
#21820=CARTESIAN_POINT('Ctrl Pts',(0.391454890651857,261.7,11.1));
#21821=CARTESIAN_POINT('Ctrl Pts',(2.91433543964104E-15,261.7,11.1));
#21822=CARTESIAN_POINT('',(0.,267.9,-11.1));
#21823=CARTESIAN_POINT('',(-3.09999999999999,264.8,-10.6583300755794));
#21824=CARTESIAN_POINT('Ctrl Pts',(-4.85722573273506E-16,267.9,-11.1));
#21825=CARTESIAN_POINT('Ctrl Pts',(-0.391454890651855,267.9,-11.1));
#21826=CARTESIAN_POINT('Ctrl Pts',(-0.807604729509082,267.821343271651,
-11.0772325011544));
#21827=CARTESIAN_POINT('Ctrl Pts',(-1.57079416556834,267.504319894822,-10.9949948149978));
#21828=CARTESIAN_POINT('Ctrl Pts',(-1.91799680212002,267.266065241237,-10.9366096412455));
#21829=CARTESIAN_POINT('Ctrl Pts',(-2.46612584114063,266.717936202216,-10.8261904693255));
#21830=CARTESIAN_POINT('Ctrl Pts',(-2.70433342241585,266.370758460622,-10.7667771783582));
#21831=CARTESIAN_POINT('Ctrl Pts',(-3.02132222583929,265.607658533432,-10.682159098241));
#21832=CARTESIAN_POINT('Ctrl Pts',(-3.09999999999999,265.191541456953,-10.6583300755794));
#21833=CARTESIAN_POINT('Ctrl Pts',(-3.09999999999999,264.8,-10.6583300755794));
#21834=CARTESIAN_POINT('Ctrl Pts',(-3.09999999999999,264.8,-10.6583300755794));
#21835=CARTESIAN_POINT('Ctrl Pts',(-3.09999999999999,264.408458543047,-10.6583300755794));
#21836=CARTESIAN_POINT('Ctrl Pts',(-3.02132222583929,263.992341466568,-10.682159098241));
#21837=CARTESIAN_POINT('Ctrl Pts',(-2.70433342241585,263.229241539378,-10.7667771783582));
#21838=CARTESIAN_POINT('Ctrl Pts',(-2.46612584114063,262.882063797784,-10.8261904693255));
#21839=CARTESIAN_POINT('Ctrl Pts',(-1.91799680212002,262.333934758763,-10.9366096412455));
#21840=CARTESIAN_POINT('Ctrl Pts',(-1.57079416556834,262.095680105178,-10.9949948149978));
#21841=CARTESIAN_POINT('Ctrl Pts',(-0.807604729509082,261.77865672835,-11.0772325011544));
#21842=CARTESIAN_POINT('Ctrl Pts',(-0.391454890651854,261.7,-11.1));
#21843=CARTESIAN_POINT('Ctrl Pts',(0.391454890651854,261.7,-11.1));
#21844=CARTESIAN_POINT('Ctrl Pts',(0.807604729509082,261.77865672835,-11.0772325011544));
#21845=CARTESIAN_POINT('Ctrl Pts',(1.57079416556834,262.095680105178,-10.9949948149978));
#21846=CARTESIAN_POINT('Ctrl Pts',(1.91799680212002,262.333934758763,-10.9366096412455));
#21847=CARTESIAN_POINT('Ctrl Pts',(2.46612584114063,262.882063797784,-10.8261904693255));
#21848=CARTESIAN_POINT('Ctrl Pts',(2.70433342241585,263.229241539378,-10.7667771783582));
#21849=CARTESIAN_POINT('Ctrl Pts',(3.02132222583929,263.992341466568,-10.682159098241));
#21850=CARTESIAN_POINT('Ctrl Pts',(3.09999999999999,264.408458543047,-10.6583300755794));
#21851=CARTESIAN_POINT('Ctrl Pts',(3.09999999999999,265.191541456953,-10.6583300755794));
#21852=CARTESIAN_POINT('Ctrl Pts',(3.02132222583929,265.607658533432,-10.682159098241));
#21853=CARTESIAN_POINT('Ctrl Pts',(2.70433342241585,266.370758460622,-10.7667771783582));
#21854=CARTESIAN_POINT('Ctrl Pts',(2.46612584114063,266.717936202216,-10.8261904693255));
#21855=CARTESIAN_POINT('Ctrl Pts',(1.91799680212002,267.266065241237,-10.9366096412455));
#21856=CARTESIAN_POINT('Ctrl Pts',(1.57079416556834,267.504319894822,-10.9949948149978));
#21857=CARTESIAN_POINT('Ctrl Pts',(0.807604729509083,267.821343271651,-11.0772325011544));
#21858=CARTESIAN_POINT('Ctrl Pts',(0.391454890651858,267.9,-11.1));
#21859=CARTESIAN_POINT('Ctrl Pts',(3.67761376907083E-15,267.9,-11.1));
#21860=CARTESIAN_POINT('Origin',(0.,275.,0.));
#21861=CARTESIAN_POINT('',(0.,0.499999999999945,11.1));
#21862=CARTESIAN_POINT('',(-1.35935794705356E-15,0.499999999999945,-11.1));
#21863=CARTESIAN_POINT('Origin',(0.,0.499999999999945,0.));
#21864=CARTESIAN_POINT('Origin',(0.,0.499999999999945,0.));
#21865=CARTESIAN_POINT('',(1.61143898433164E-13,2.67704306348694,11.1));
#21866=CARTESIAN_POINT('',(-1.35935794705356E-15,275.,11.1));
#21867=CARTESIAN_POINT('',(-2.0260462879878E-12,7.32295697727983,11.1));
#21868=CARTESIAN_POINT('Ctrl Pts',(3.23647154813382E-13,2.67704306348694,
11.1));
#21869=CARTESIAN_POINT('Ctrl Pts',(-0.273139581690495,2.67704308193317,
11.1));
#21870=CARTESIAN_POINT('Ctrl Pts',(-0.544517384377054,2.72153833743136,
11.0896641648894));
#21871=CARTESIAN_POINT('Ctrl Pts',(-1.10258484109494,2.91067862507553,11.0491875912365));
#21872=CARTESIAN_POINT('Ctrl Pts',(-1.3798661147451,3.06856373870345,11.0165275551973));
#21873=CARTESIAN_POINT('Ctrl Pts',(-1.84282580329821,3.47012918997237,10.948317869715));
#21874=CARTESIAN_POINT('Ctrl Pts',(-2.02918140675796,3.7055024182498,10.9138310665725));
#21875=CARTESIAN_POINT('Ctrl Pts',(-2.29556418563575,4.22355226854262,10.8608471933831));
#21876=CARTESIAN_POINT('Ctrl Pts',(-2.3775175883224,4.49913306003288,10.8424265102952));
#21877=CARTESIAN_POINT('Ctrl Pts',(-2.40517323731289,4.78410483624288,10.8362881882372));
#21878=CARTESIAN_POINT('Ctrl Pts',(-2.42308944027353,4.96871855412709,10.8323115893201));
#21879=CARTESIAN_POINT('Ctrl Pts',(-2.41796202305408,5.15442416696364,10.8334796125597));
#21880=CARTESIAN_POINT('Ctrl Pts',(-2.36183470646002,5.5218723530959,10.8458548618846));
#21881=CARTESIAN_POINT('Ctrl Pts',(-2.3109127065596,5.70137997051123,10.8570313240313));
#21882=CARTESIAN_POINT('Ctrl Pts',(-2.11813065645628,6.15860457306728,10.8967269208308));
#21883=CARTESIAN_POINT('Ctrl Pts',(-1.94101086541288,6.41571203975272,10.9312778707514));
#21884=CARTESIAN_POINT('Ctrl Pts',(-1.49402342882342,6.85125097027356,11.0013588285694));
#21885=CARTESIAN_POINT('Ctrl Pts',(-1.22720905280096,7.02401263594798,11.0358642385009));
#21886=CARTESIAN_POINT('Ctrl Pts',(-0.642145747279439,7.26002789053428,
11.0852910865185));
#21887=CARTESIAN_POINT('Ctrl Pts',(-0.330182188115768,7.32101004289588,
11.0995604536001));
#21888=CARTESIAN_POINT('Ctrl Pts',(-0.0100813466862662,7.32294187220753,
11.0999965668345));
#21889=CARTESIAN_POINT('Ctrl Pts',(-0.00504035649498059,7.32295707066767,
11.1));
#21890=CARTESIAN_POINT('Ctrl Pts',(-4.05073321802854E-12,7.32295697727983,
11.1));
#21891=CARTESIAN_POINT('',(0.,12.4487510399342,11.1));
#21892=CARTESIAN_POINT('',(-1.35935794705356E-15,275.,11.1));
#21893=CARTESIAN_POINT('Origin',(0.,12.4487510399342,0.));
#21894=CARTESIAN_POINT('',(2.41562897926683,5.,10.833962185393));
#21895=CARTESIAN_POINT('Ctrl Pts',(-4.05073321802854E-12,7.32295697727983,
11.1));
#21896=CARTESIAN_POINT('Ctrl Pts',(0.315495834708401,7.32295113176525,11.1000000000001));
#21897=CARTESIAN_POINT('Ctrl Pts',(0.628508866369116,7.26353532669138,11.0860850371572));
#21898=CARTESIAN_POINT('Ctrl Pts',(1.21451436236122,7.03104316540582,11.0372796619423));
#21899=CARTESIAN_POINT('Ctrl Pts',(1.48278165110063,6.85960869665576,11.0029086057863));
#21900=CARTESIAN_POINT('Ctrl Pts',(1.92338507228345,6.43522915122724,10.9342333167844));
#21901=CARTESIAN_POINT('Ctrl Pts',(2.09658178139581,6.19108347331183,10.9009068044498));
#21902=CARTESIAN_POINT('Ctrl Pts',(2.3348660806695,5.65953558717099,10.852306679531));
#21903=CARTESIAN_POINT('Ctrl Pts',(2.40154335470469,5.38013985460967,10.8371002996985));
#21904=CARTESIAN_POINT('Ctrl Pts',(2.41496509132228,5.06293051253712,10.8341102760105));
#21905=CARTESIAN_POINT('Ctrl Pts',(2.41562898203172,5.03144629441105,10.8339621847766));
#21906=CARTESIAN_POINT('Ctrl Pts',(2.41562897926683,5.,10.833962185393));
#21907=CARTESIAN_POINT('Ctrl Pts',(2.41562897926683,5.,10.833962185393));
#21908=CARTESIAN_POINT('Ctrl Pts',(2.41562895648218,4.74086038603115,10.8339621904733));
#21909=CARTESIAN_POINT('Ctrl Pts',(2.37058559554881,4.48429608284729,10.8442778599772));
#21910=CARTESIAN_POINT('Ctrl Pts',(2.17946594106486,3.95311954848045,10.8844424518853));
#21911=CARTESIAN_POINT('Ctrl Pts',(2.01939079066006,3.69060671315312,10.9167481416166));
#21912=CARTESIAN_POINT('Ctrl Pts',(1.60207378032625,3.23423850139877,10.9858781650619));
#21913=CARTESIAN_POINT('Ctrl Pts',(1.3455459736091,3.0467729086828,11.0218702685321));
#21914=CARTESIAN_POINT('Ctrl Pts',(0.772856356127114,2.7777494777404,11.0768259913659));
#21915=CARTESIAN_POINT('Ctrl Pts',(0.461192262550163,2.69922142801988,11.094988270665));
#21916=CARTESIAN_POINT('Ctrl Pts',(0.0951098358302787,2.67839196589101,
11.0996944994446));
#21917=CARTESIAN_POINT('Ctrl Pts',(0.0475282448567165,2.67704306027716,
11.1));
#21918=CARTESIAN_POINT('Ctrl Pts',(3.23647154813382E-13,2.67704306348694,
11.1));
#21919=CARTESIAN_POINT('',(-2.71871589410712E-15,7.32295693650353,-11.1));
#21920=CARTESIAN_POINT('Ctrl Pts',(-2.46904150249686E-15,7.32295693650353,
-11.1));
#21921=CARTESIAN_POINT('Ctrl Pts',(-0.0695652818990985,7.32295783550982,
-11.1));
#21922=CARTESIAN_POINT('Ctrl Pts',(-0.139218809299037,7.32006775869429,
-11.0993450131274));
#21923=CARTESIAN_POINT('Ctrl Pts',(-0.528466789920203,7.28759395137216,
-11.0920220652185));
#21924=CARTESIAN_POINT('Ctrl Pts',(-0.839196549011331,7.20011126493925,
-11.0719290301748));
#21925=CARTESIAN_POINT('Ctrl Pts',(-1.40169375654943,6.91581877804573,-11.0146835965512));
#21926=CARTESIAN_POINT('Ctrl Pts',(-1.65013536422944,6.7237844228964,-10.9786031937536));
#21927=CARTESIAN_POINT('Ctrl Pts',(-2.04573187848749,6.26842859693051,-10.9115934145661));
#21928=CARTESIAN_POINT('Ctrl Pts',(-2.19481020238894,6.01339934425637,-10.8812914141919));
#21929=CARTESIAN_POINT('Ctrl Pts',(-2.38466733146137,5.46687720810133,-10.8412405251123));
#21930=CARTESIAN_POINT('Ctrl Pts',(-2.42638928271567,5.18274028883403,-10.8315657047934));
#21931=CARTESIAN_POINT('Ctrl Pts',(-2.39970912117631,4.6023397708397,-10.8375084426288));
#21932=CARTESIAN_POINT('Ctrl Pts',(-2.32789728802446,4.31417905623201,-10.8538969744193));
#21933=CARTESIAN_POINT('Ctrl Pts',(-2.0724135232689,3.7677138426677,-10.9056366497519));
#21934=CARTESIAN_POINT('Ctrl Pts',(-1.88647098366285,3.51801820624971,-10.940955305182));
#21935=CARTESIAN_POINT('Ctrl Pts',(-1.42614298609066,3.10012773169153,-11.0105048755359));
#21936=CARTESIAN_POINT('Ctrl Pts',(-1.15427898086522,2.93682125994773,-11.0438097881092));
#21937=CARTESIAN_POINT('Ctrl Pts',(-0.557940747205909,2.71881889702648,
-11.0900629860885));
#21938=CARTESIAN_POINT('Ctrl Pts',(-0.238737740968463,2.66797692828207,
-11.1020514614943));
#21939=CARTESIAN_POINT('Ctrl Pts',(0.0814759967561537,2.67836337071254,
-11.0997009717358));
#21940=CARTESIAN_POINT('Ctrl Pts',(0.285421015271941,2.68497852473075,-11.0982039382833));
#21941=CARTESIAN_POINT('Ctrl Pts',(0.487856497256365,2.71645669516471,-11.0910086113376));
#21942=CARTESIAN_POINT('Ctrl Pts',(0.877921673005148,2.8271378442534,-11.0669392231544));
#21943=CARTESIAN_POINT('Ctrl Pts',(1.06491376579154,2.90576754946889,-11.0501997293928));
#21944=CARTESIAN_POINT('Ctrl Pts',(1.50637405997121,3.15962708068845,-11.0005827675453));
#21945=CARTESIAN_POINT('Ctrl Pts',(1.74119128221293,3.36171267697428,-10.9642651821397));
#21946=CARTESIAN_POINT('Ctrl Pts',(2.10874780489197,3.831472605075,-10.8993594960467));
#21947=CARTESIAN_POINT('Ctrl Pts',(2.24332570855584,4.09096781536863,-10.8712685160658));
#21948=CARTESIAN_POINT('Ctrl Pts',(2.40531152247706,4.64373711172344,-10.8365681858915));
#21949=CARTESIAN_POINT('Ctrl Pts',(2.43274503947083,4.9297892674136,-10.8301680767129));
#21950=CARTESIAN_POINT('Ctrl Pts',(2.37669341236812,5.51144009685063,-10.8426098557504));
#21951=CARTESIAN_POINT('Ctrl Pts',(2.28908482971336,5.79836274682849,-10.8623397100488));
#21952=CARTESIAN_POINT('Ctrl Pts',(2.00213836415185,6.33610283283957,-10.9189700913053));
#21953=CARTESIAN_POINT('Ctrl Pts',(1.8006305505284,6.57828056462836,-10.9557149186307));
#21954=CARTESIAN_POINT('Ctrl Pts',(1.31295487334744,6.97413780170986,-11.0248581802782));
#21955=CARTESIAN_POINT('Ctrl Pts',(1.03053677251028,7.123233785964,-11.0562637699774));
#21956=CARTESIAN_POINT('Ctrl Pts',(0.490350610681507,7.28700460364381,-11.0916840411728));
#21957=CARTESIAN_POINT('Ctrl Pts',(0.245725806500237,7.32295376093894,-11.1));
#21958=CARTESIAN_POINT('Ctrl Pts',(-2.46904150249686E-15,7.32295693650353,
-11.1));
#21959=CARTESIAN_POINT('Origin',(0.,275.,0.));
#21960=CARTESIAN_POINT('',(0.,275.,10.6));
#21961=CARTESIAN_POINT('Origin',(0.,275.,0.));
#21962=CARTESIAN_POINT('',(-1.18790592559677E-15,275.,-9.69998799999994));
#21963=CARTESIAN_POINT('Origin',(0.,275.,0.));
#21964=CARTESIAN_POINT('Origin',(0.,0.,0.));
#21965=CARTESIAN_POINT('',(-1.2981256070962E-15,-4.85722573273506E-16,-10.6));
#21966=CARTESIAN_POINT('Origin',(0.,0.,0.));
#21967=CARTESIAN_POINT('',(0.,0.,9.70000000000007));
#21968=CARTESIAN_POINT('Origin',(0.,0.,0.));
#21969=CARTESIAN_POINT('Origin',(0.,0.,0.));
#21970=CARTESIAN_POINT('',(0.,0.500000000000066,9.2));
#21971=CARTESIAN_POINT('',(-1.12667505521557E-15,0.500000000000066,-9.2));
#21972=CARTESIAN_POINT('Origin',(0.,0.500000000000066,0.));
#21973=CARTESIAN_POINT('',(-5.63337527607783E-16,3.,-9.2));
#21974=CARTESIAN_POINT('',(-1.12667505521557E-15,0.,-9.2));
#21975=CARTESIAN_POINT('',(-2.,5.,-8.97997772825746));
#21976=CARTESIAN_POINT('Ctrl Pts',(1.38777878078145E-16,3.,-9.2));
#21977=CARTESIAN_POINT('Ctrl Pts',(-0.251982495387346,3.,-9.2));
#21978=CARTESIAN_POINT('Ctrl Pts',(-0.520217657456257,3.05052306683097,
-9.18860399767844));
#21979=CARTESIAN_POINT('Ctrl Pts',(-1.0127456170646,3.25488309906895,-9.1474267505225));
#21980=CARTESIAN_POINT('Ctrl Pts',(-1.23710338548845,3.40867626074226,-9.11820719093608));
#21981=CARTESIAN_POINT('Ctrl Pts',(-1.59133769071452,3.76291056596832,-9.06309972244743));
#21982=CARTESIAN_POINT('Ctrl Pts',(-1.7451199392152,3.98726244660274,-9.0335726503792));
#21983=CARTESIAN_POINT('Ctrl Pts',(-1.94947204040866,4.479769809412,-8.99168712872246));
#21984=CARTESIAN_POINT('Ctrl Pts',(-2.,4.74799765525699,-8.97997772825746));
#21985=CARTESIAN_POINT('Ctrl Pts',(-2.,5.,-8.97997772825746));
#21986=CARTESIAN_POINT('',(-6.67420936166391E-16,7.,-9.2));
#21987=CARTESIAN_POINT('Ctrl Pts',(-2.,5.,-8.97997772825746));
#21988=CARTESIAN_POINT('Ctrl Pts',(-2.,5.25200234474301,-8.97997772825746));
#21989=CARTESIAN_POINT('Ctrl Pts',(-1.94947204040866,5.520230190588,-8.99168712872246));
#21990=CARTESIAN_POINT('Ctrl Pts',(-1.7451199392152,6.01273755339726,-9.0335726503792));
#21991=CARTESIAN_POINT('Ctrl Pts',(-1.59133769071452,6.23708943403168,-9.06309972244743));
#21992=CARTESIAN_POINT('Ctrl Pts',(-1.23710338548845,6.59132373925774,-9.11820719093608));
#21993=CARTESIAN_POINT('Ctrl Pts',(-1.0127456170646,6.74511690093105,-9.1474267505225));
#21994=CARTESIAN_POINT('Ctrl Pts',(-0.520217657456257,6.94947693316903,
-9.18860399767844));
#21995=CARTESIAN_POINT('Ctrl Pts',(-0.251982495387347,7.,-9.2));
#21996=CARTESIAN_POINT('Ctrl Pts',(-6.93889390390723E-16,7.,-9.2));
#21997=CARTESIAN_POINT('',(-1.01436563136175E-15,261.7,-9.2));
#21998=CARTESIAN_POINT('',(-1.12667505521557E-15,0.,-9.2));
#21999=CARTESIAN_POINT('',(-3.09999999999999,264.8,-8.66198591548151));
#22000=CARTESIAN_POINT('Ctrl Pts',(0.,261.7,-9.2));
#22001=CARTESIAN_POINT('Ctrl Pts',(-0.392492181867812,261.7,-9.2));
#22002=CARTESIAN_POINT('Ctrl Pts',(-0.809098032285487,261.779064419326,
-9.17242354783845));
#22003=CARTESIAN_POINT('Ctrl Pts',(-1.57202652449705,262.096405395141,-9.07285654990429));
#22004=CARTESIAN_POINT('Ctrl Pts',(-1.91858114764766,262.334519104291,-9.00212872931236));
#22005=CARTESIAN_POINT('Ctrl Pts',(-2.46561371815086,262.881551674794,-8.86792542274352));
#22006=CARTESIAN_POINT('Ctrl Pts',(-2.70362524494473,263.228053521236,-8.79535506867642));
#22007=CARTESIAN_POINT('Ctrl Pts',(-3.02088992440016,263.990785821449,-8.69149502149012));
#22008=CARTESIAN_POINT('Ctrl Pts',(-3.09999999999999,264.407317173429,-8.66198591548151));
#22009=CARTESIAN_POINT('Ctrl Pts',(-3.09999999999999,264.8,-8.66198591548151));
#22010=CARTESIAN_POINT('',(-2.12458865598691E-15,267.9,-9.2));
#22011=CARTESIAN_POINT('Ctrl Pts',(-3.1,264.8,-8.66198591548151));
#22012=CARTESIAN_POINT('Ctrl Pts',(-3.1,265.192682826571,-8.66198591548151));
#22013=CARTESIAN_POINT('Ctrl Pts',(-3.02088992440016,265.609214178551,-8.69149502149013));
#22014=CARTESIAN_POINT('Ctrl Pts',(-2.70362524494473,266.371946478764,-8.79535506867642));
#22015=CARTESIAN_POINT('Ctrl Pts',(-2.46561371815086,266.718448325206,-8.86792542274352));
#22016=CARTESIAN_POINT('Ctrl Pts',(-1.91858114764766,267.265480895709,-9.00212872931236));
#22017=CARTESIAN_POINT('Ctrl Pts',(-1.57202652449705,267.503594604859,-9.07285654990429));
#22018=CARTESIAN_POINT('Ctrl Pts',(-0.809098032285488,267.820935580675,
-9.17242354783845));
#22019=CARTESIAN_POINT('Ctrl Pts',(-0.392492181867816,267.9,-9.2));
#22020=CARTESIAN_POINT('Ctrl Pts',(-3.53883589099269E-15,267.9,-9.2));
#22021=CARTESIAN_POINT('',(-1.12667505521557E-15,274.500012,-9.2));
#22022=CARTESIAN_POINT('',(-1.12667505521557E-15,0.,-9.2));
#22023=CARTESIAN_POINT('Origin',(0.,274.500012,0.));
#22024=CARTESIAN_POINT('',(3.09999999999999,264.8,-8.66198591548151));
#22025=CARTESIAN_POINT('Ctrl Pts',(-3.2612801348364E-15,267.9,-9.2));
#22026=CARTESIAN_POINT('Ctrl Pts',(0.392492181867809,267.9,-9.2));
#22027=CARTESIAN_POINT('Ctrl Pts',(0.809098032285487,267.820935580675,-9.17242354783845));
#22028=CARTESIAN_POINT('Ctrl Pts',(1.57202652449705,267.503594604859,-9.07285654990429));
#22029=CARTESIAN_POINT('Ctrl Pts',(1.91858114764766,267.265480895709,-9.00212872931236));
#22030=CARTESIAN_POINT('Ctrl Pts',(2.46561371815086,266.718448325206,-8.86792542274352));
#22031=CARTESIAN_POINT('Ctrl Pts',(2.70362524494473,266.371946478764,-8.79535506867642));
#22032=CARTESIAN_POINT('Ctrl Pts',(3.02088992440016,265.609214178551,-8.69149502149013));
#22033=CARTESIAN_POINT('Ctrl Pts',(3.09999999999999,265.192682826571,-8.66198591548151));
#22034=CARTESIAN_POINT('Ctrl Pts',(3.09999999999999,264.8,-8.66198591548151));
#22035=CARTESIAN_POINT('Ctrl Pts',(3.09999999999999,264.8,-8.66198591548151));
#22036=CARTESIAN_POINT('Ctrl Pts',(3.09999999999999,264.407317173429,-8.66198591548151));
#22037=CARTESIAN_POINT('Ctrl Pts',(3.02088992440016,263.990785821449,-8.69149502149012));
#22038=CARTESIAN_POINT('Ctrl Pts',(2.70362524494473,263.228053521236,-8.79535506867642));
#22039=CARTESIAN_POINT('Ctrl Pts',(2.46561371815086,262.881551674794,-8.86792542274352));
#22040=CARTESIAN_POINT('Ctrl Pts',(1.91858114764766,262.334519104291,-9.00212872931236));
#22041=CARTESIAN_POINT('Ctrl Pts',(1.57202652449705,262.096405395141,-9.07285654990429));
#22042=CARTESIAN_POINT('Ctrl Pts',(0.809098032285487,261.779064419326,-9.17242354783845));
#22043=CARTESIAN_POINT('Ctrl Pts',(0.392492181867812,261.7,-9.2));
#22044=CARTESIAN_POINT('Ctrl Pts',(3.12250225675825E-16,261.7,-9.2));
#22045=CARTESIAN_POINT('',(2.,5.,-8.97997772825746));
#22046=CARTESIAN_POINT('Ctrl Pts',(-1.38777878078145E-16,7.,-9.2));
#22047=CARTESIAN_POINT('Ctrl Pts',(0.251982495387346,7.,-9.2));
#22048=CARTESIAN_POINT('Ctrl Pts',(0.520217657456257,6.94947693316903,-9.18860399767844));
#22049=CARTESIAN_POINT('Ctrl Pts',(1.0127456170646,6.74511690093105,-9.1474267505225));
#22050=CARTESIAN_POINT('Ctrl Pts',(1.23710338548845,6.59132373925774,-9.11820719093608));
#22051=CARTESIAN_POINT('Ctrl Pts',(1.59133769071451,6.23708943403168,-9.06309972244743));
#22052=CARTESIAN_POINT('Ctrl Pts',(1.7451199392152,6.01273755339726,-9.0335726503792));
#22053=CARTESIAN_POINT('Ctrl Pts',(1.94947204040866,5.520230190588,-8.99168712872246));
#22054=CARTESIAN_POINT('Ctrl Pts',(2.,5.252002344743,-8.97997772825746));
#22055=CARTESIAN_POINT('Ctrl Pts',(2.,5.,-8.97997772825746));
#22056=CARTESIAN_POINT('Ctrl Pts',(2.,5.,-8.97997772825746));
#22057=CARTESIAN_POINT('Ctrl Pts',(2.,4.74799765525699,-8.97997772825746));
#22058=CARTESIAN_POINT('Ctrl Pts',(1.94947204040866,4.479769809412,-8.99168712872246));
#22059=CARTESIAN_POINT('Ctrl Pts',(1.7451199392152,3.98726244660274,-9.0335726503792));
#22060=CARTESIAN_POINT('Ctrl Pts',(1.59133769071452,3.76291056596832,-9.06309972244743));
#22061=CARTESIAN_POINT('Ctrl Pts',(1.23710338548845,3.40867626074226,-9.11820719093608));
#22062=CARTESIAN_POINT('Ctrl Pts',(1.0127456170646,3.25488309906895,-9.1474267505225));
#22063=CARTESIAN_POINT('Ctrl Pts',(0.520217657456257,3.05052306683097,-9.18860399767844));
#22064=CARTESIAN_POINT('Ctrl Pts',(0.251982495387346,3.,-9.2));
#22065=CARTESIAN_POINT('Ctrl Pts',(6.93889390390723E-17,3.,-9.2));
#22066=CARTESIAN_POINT('Origin',(0.,0.500000000000066,0.));
#22067=CARTESIAN_POINT('',(0.,3.,9.2));
#22068=CARTESIAN_POINT('',(-2.,5.,8.97997772825746));
#22069=CARTESIAN_POINT('Ctrl Pts',(2.08166817117217E-16,3.,9.2));
#22070=CARTESIAN_POINT('Ctrl Pts',(0.251982495387347,3.,9.2));
#22071=CARTESIAN_POINT('Ctrl Pts',(0.520217657456258,3.05052306683097,9.18860399767844));
#22072=CARTESIAN_POINT('Ctrl Pts',(1.0127456170646,3.25488309906895,9.1474267505225));
#22073=CARTESIAN_POINT('Ctrl Pts',(1.23710338548845,3.40867626074226,9.11820719093608));
#22074=CARTESIAN_POINT('Ctrl Pts',(1.59133769071451,3.76291056596832,9.06309972244743));
#22075=CARTESIAN_POINT('Ctrl Pts',(1.7451199392152,3.98726244660274,9.0335726503792));
#22076=CARTESIAN_POINT('Ctrl Pts',(1.94947204040866,4.479769809412,8.99168712872246));
#22077=CARTESIAN_POINT('Ctrl Pts',(2.,4.74799765525699,8.97997772825746));
#22078=CARTESIAN_POINT('Ctrl Pts',(2.,5.,8.97997772825746));
#22079=CARTESIAN_POINT('Ctrl Pts',(2.,5.25200234474301,8.97997772825746));
#22080=CARTESIAN_POINT('Ctrl Pts',(1.94947204040866,5.520230190588,8.99168712872246));
#22081=CARTESIAN_POINT('Ctrl Pts',(1.7451199392152,6.01273755339726,9.0335726503792));
#22082=CARTESIAN_POINT('Ctrl Pts',(1.59133769071451,6.23708943403168,9.06309972244743));
#22083=CARTESIAN_POINT('Ctrl Pts',(1.23710338548845,6.59132373925774,9.11820719093608));
#22084=CARTESIAN_POINT('Ctrl Pts',(1.0127456170646,6.74511690093105,9.1474267505225));
#22085=CARTESIAN_POINT('Ctrl Pts',(0.520217657456256,6.94947693316903,9.18860399767844));
#22086=CARTESIAN_POINT('Ctrl Pts',(0.251982495387346,7.,9.2));
#22087=CARTESIAN_POINT('Ctrl Pts',(-0.251982495387347,7.,9.2));
#22088=CARTESIAN_POINT('Ctrl Pts',(-0.520217657456257,6.94947693316903,
9.18860399767844));
#22089=CARTESIAN_POINT('Ctrl Pts',(-1.0127456170646,6.74511690093105,9.1474267505225));
#22090=CARTESIAN_POINT('Ctrl Pts',(-1.23710338548845,6.59132373925774,9.11820719093608));
#22091=CARTESIAN_POINT('Ctrl Pts',(-1.59133769071452,6.23708943403168,9.06309972244743));
#22092=CARTESIAN_POINT('Ctrl Pts',(-1.7451199392152,6.01273755339726,9.0335726503792));
#22093=CARTESIAN_POINT('Ctrl Pts',(-1.94947204040866,5.520230190588,8.99168712872246));
#22094=CARTESIAN_POINT('Ctrl Pts',(-2.,5.25200234474301,8.97997772825746));
#22095=CARTESIAN_POINT('Ctrl Pts',(-2.,5.,8.97997772825746));
#22096=CARTESIAN_POINT('Ctrl Pts',(-2.,5.,8.97997772825746));
#22097=CARTESIAN_POINT('Ctrl Pts',(-2.,4.74799765525699,8.97997772825746));
#22098=CARTESIAN_POINT('Ctrl Pts',(-1.94947204040866,4.479769809412,8.99168712872246));
#22099=CARTESIAN_POINT('Ctrl Pts',(-1.7451199392152,3.98726244660274,9.0335726503792));
#22100=CARTESIAN_POINT('Ctrl Pts',(-1.59133769071452,3.76291056596832,9.06309972244743));
#22101=CARTESIAN_POINT('Ctrl Pts',(-1.23710338548845,3.40867626074226,9.11820719093608));
#22102=CARTESIAN_POINT('Ctrl Pts',(-1.0127456170646,3.25488309906895,9.1474267505225));
#22103=CARTESIAN_POINT('Ctrl Pts',(-0.520217657456257,3.05052306683097,
9.18860399767844));
#22104=CARTESIAN_POINT('Ctrl Pts',(-0.251982495387346,3.,9.2));
#22105=CARTESIAN_POINT('Ctrl Pts',(1.38777878078145E-16,3.,9.2));
#22106=CARTESIAN_POINT('',(0.,261.7,9.2));
#22107=CARTESIAN_POINT('',(-3.09999999999999,264.8,8.66198591548151));
#22108=CARTESIAN_POINT('Ctrl Pts',(6.93889390390723E-17,261.7,9.2));
#22109=CARTESIAN_POINT('Ctrl Pts',(0.392492181867812,261.7,9.2));
#22110=CARTESIAN_POINT('Ctrl Pts',(0.809098032285487,261.779064419326,9.17242354783845));
#22111=CARTESIAN_POINT('Ctrl Pts',(1.57202652449705,262.096405395141,9.07285654990429));
#22112=CARTESIAN_POINT('Ctrl Pts',(1.91858114764766,262.334519104291,9.00212872931236));
#22113=CARTESIAN_POINT('Ctrl Pts',(2.46561371815086,262.881551674794,8.86792542274352));
#22114=CARTESIAN_POINT('Ctrl Pts',(2.70362524494473,263.228053521236,8.79535506867642));
#22115=CARTESIAN_POINT('Ctrl Pts',(3.02088992440016,263.990785821449,8.69149502149013));
#22116=CARTESIAN_POINT('Ctrl Pts',(3.09999999999999,264.407317173429,8.66198591548151));
#22117=CARTESIAN_POINT('Ctrl Pts',(3.09999999999999,264.8,8.66198591548151));
#22118=CARTESIAN_POINT('Ctrl Pts',(3.09999999999999,265.192682826571,8.66198591548151));
#22119=CARTESIAN_POINT('Ctrl Pts',(3.02088992440016,265.609214178551,8.69149502149012));
#22120=CARTESIAN_POINT('Ctrl Pts',(2.70362524494473,266.371946478764,8.79535506867642));
#22121=CARTESIAN_POINT('Ctrl Pts',(2.46561371815086,266.718448325206,8.86792542274352));
#22122=CARTESIAN_POINT('Ctrl Pts',(1.91858114764766,267.265480895709,9.00212872931236));
#22123=CARTESIAN_POINT('Ctrl Pts',(1.57202652449705,267.503594604859,9.07285654990429));
#22124=CARTESIAN_POINT('Ctrl Pts',(0.809098032285487,267.820935580675,9.17242354783845));
#22125=CARTESIAN_POINT('Ctrl Pts',(0.392492181867812,267.9,9.2));
#22126=CARTESIAN_POINT('Ctrl Pts',(-0.392492181867813,267.9,9.2));
#22127=CARTESIAN_POINT('Ctrl Pts',(-0.809098032285488,267.820935580675,
9.17242354783845));
#22128=CARTESIAN_POINT('Ctrl Pts',(-1.57202652449705,267.503594604859,9.07285654990429));
#22129=CARTESIAN_POINT('Ctrl Pts',(-1.91858114764766,267.265480895709,9.00212872931236));
#22130=CARTESIAN_POINT('Ctrl Pts',(-2.46561371815086,266.718448325206,8.86792542274352));
#22131=CARTESIAN_POINT('Ctrl Pts',(-2.70362524494473,266.371946478764,8.79535506867642));
#22132=CARTESIAN_POINT('Ctrl Pts',(-3.02088992440016,265.609214178551,8.69149502149013));
#22133=CARTESIAN_POINT('Ctrl Pts',(-3.09999999999999,265.192682826571,8.66198591548151));
#22134=CARTESIAN_POINT('Ctrl Pts',(-3.09999999999999,264.8,8.66198591548151));
#22135=CARTESIAN_POINT('Ctrl Pts',(-3.09999999999999,264.8,8.66198591548151));
#22136=CARTESIAN_POINT('Ctrl Pts',(-3.09999999999999,264.407317173429,8.66198591548151));
#22137=CARTESIAN_POINT('Ctrl Pts',(-3.02088992440016,263.990785821449,8.69149502149012));
#22138=CARTESIAN_POINT('Ctrl Pts',(-2.70362524494473,263.228053521236,8.79535506867642));
#22139=CARTESIAN_POINT('Ctrl Pts',(-2.46561371815086,262.881551674794,8.86792542274352));
#22140=CARTESIAN_POINT('Ctrl Pts',(-1.91858114764766,262.334519104291,9.00212872931236));
#22141=CARTESIAN_POINT('Ctrl Pts',(-1.57202652449705,262.096405395141,9.07285654990429));
#22142=CARTESIAN_POINT('Ctrl Pts',(-0.809098032285487,261.779064419326,
9.17242354783845));
#22143=CARTESIAN_POINT('Ctrl Pts',(-0.392492181867816,261.7,9.2));
#22144=CARTESIAN_POINT('Ctrl Pts',(-4.09394740330526E-15,261.7,9.2));
#22145=CARTESIAN_POINT('Origin',(0.,264.8,-11.1));
#22146=CARTESIAN_POINT('',(-3.09999999999999,264.8,-11.1));
#22147=CARTESIAN_POINT('Origin',(0.,264.8,-11.1));
#22148=CARTESIAN_POINT('',(-3.09999999999999,264.8,-11.1));
#22149=CARTESIAN_POINT('Origin',(0.,5.,-11.1));
#22150=CARTESIAN_POINT('',(5.66553889764798E-16,7.,-10.6741648723787));
#22151=CARTESIAN_POINT('',(-2.,5.00000000004607,-10.4183332065073));
#22152=CARTESIAN_POINT('Ctrl Pts',(3.90311824664763E-16,7.,-10.6741648723787));
#22153=CARTESIAN_POINT('Ctrl Pts',(0.0905425845562135,7.,-10.67416643345));
#22154=CARTESIAN_POINT('Ctrl Pts',(0.180978358532567,6.99385302819578,-10.6726039986148));
#22155=CARTESIAN_POINT('Ctrl Pts',(0.522624030520656,6.94717907361443,-10.6609110333759));
#22156=CARTESIAN_POINT('Ctrl Pts',(0.764749077005449,6.86522985952275,-10.6402575275526));
#22157=CARTESIAN_POINT('Ctrl Pts',(1.21107417380008,6.61272549366747,-10.5843663956255));
#22158=CARTESIAN_POINT('Ctrl Pts',(1.41000159084709,6.44194367972254,-10.5494794983223));
#22159=CARTESIAN_POINT('Ctrl Pts',(1.7318707401912,6.03366519693967,-10.4846434012231));
#22160=CARTESIAN_POINT('Ctrl Pts',(1.85210598322984,5.79898238439151,-10.4555004640632));
#22161=CARTESIAN_POINT('Ctrl Pts',(1.9583401576163,5.42531015059408,-10.4290848493575));
#22162=CARTESIAN_POINT('Ctrl Pts',(1.98132978273519,5.30063336475968,-10.4231531964456));
#22163=CARTESIAN_POINT('Ctrl Pts',(2.00342374231953,5.0482782950185,-10.4174536861239));
#22164=CARTESIAN_POINT('Ctrl Pts',(2.00246887275993,4.92144779768745,-10.417702628372));
#22165=CARTESIAN_POINT('Ctrl Pts',(1.96358997015029,4.54336430699628,-10.4277230327553));
#22166=CARTESIAN_POINT('Ctrl Pts',(1.89017432113397,4.29951442558204,-10.4468643148236));
#22167=CARTESIAN_POINT('Ctrl Pts',(1.65371382249779,3.84551301214123,-10.5008923916095));
#22168=CARTESIAN_POINT('Ctrl Pts',(1.48992823087753,3.64081189954436,-10.5355071129865));
#22169=CARTESIAN_POINT('Ctrl Pts',(1.15765910613943,3.35964601502151,-10.5903139385164));
#22170=CARTESIAN_POINT('Ctrl Pts',(1.00877965860273,3.26405647735089,-10.6113011130337));
#22171=CARTESIAN_POINT('Ctrl Pts',(0.689508174816086,3.11436672263152,-10.645705448787));
#22172=CARTESIAN_POINT('Ctrl Pts',(0.52056030432242,3.06085078015626,-10.6589513899869));
#22173=CARTESIAN_POINT('Ctrl Pts',(0.346363582765798,3.03022024872484,-10.6665813564896));
#22174=CARTESIAN_POINT('Ctrl Pts',(0.222541532025453,3.00844753576438,-10.6720048690046));
#22175=CARTESIAN_POINT('Ctrl Pts',(0.096919746131382,2.99838937465003,-10.6745722719829));
#22176=CARTESIAN_POINT('Ctrl Pts',(-0.155712937316322,3.00204261420003,
-10.6736481591137));
#22177=CARTESIAN_POINT('Ctrl Pts',(-0.281945001971389,3.01593008051804,
-10.6701129134356));
#22178=CARTESIAN_POINT('Ctrl Pts',(-0.530158060286785,3.06737632605939,
-10.6573695392721));
#22179=CARTESIAN_POINT('Ctrl Pts',(-0.651515034820079,3.10486401462923,
-10.6481781924527));
#22180=CARTESIAN_POINT('Ctrl Pts',(-0.885673237124933,3.20229798323634,
-10.6253615082331));
#22181=CARTESIAN_POINT('Ctrl Pts',(-0.997931263074252,3.26212905175645,
-10.6117666796584));
#22182=CARTESIAN_POINT('Ctrl Pts',(-1.32191353329698,3.47649890889909,-10.5662536960044));
#22183=CARTESIAN_POINT('Ctrl Pts',(-1.50972131261701,3.66237708090707,-10.5305737460068));
#22184=CARTESIAN_POINT('Ctrl Pts',(-1.80282581791566,4.09551861849479,-10.4681951081463));
#22185=CARTESIAN_POINT('Ctrl Pts',(-1.90588825604454,4.33912828055132,-10.4422956738487));
#22186=CARTESIAN_POINT('Ctrl Pts',(-1.98631219662309,4.72977681278504,-10.4219160701683));
#22187=CARTESIAN_POINT('Ctrl Pts',(-2.00000000000623,4.86485757992022,-10.4183330488132));
#22188=CARTESIAN_POINT('Ctrl Pts',(-2.,5.00000000009213,-10.4183332065073));
#22189=CARTESIAN_POINT('',(-2.,5.,-11.1));
#22190=CARTESIAN_POINT('Ctrl Pts',(-2.,5.00000000009213,-10.4183332065073));
#22191=CARTESIAN_POINT('Ctrl Pts',(-1.99999999999466,5.11601901023085,-10.4183333418869));
#22192=CARTESIAN_POINT('Ctrl Pts',(-1.98991020136398,5.23208345991214,-10.4209668626609));
#22193=CARTESIAN_POINT('Ctrl Pts',(-1.92592478911155,5.59532890146743,-10.4372741617203));
#22194=CARTESIAN_POINT('Ctrl Pts',(-1.83579428369438,5.83229365962327,-10.4601816506442));
#22195=CARTESIAN_POINT('Ctrl Pts',(-1.56865648998154,6.26765940551044,-10.5187492985391));
#22196=CARTESIAN_POINT('Ctrl Pts',(-1.39075219046935,6.46059804253605,-10.5540922604607));
#22197=CARTESIAN_POINT('Ctrl Pts',(-1.07565913626136,6.69115396916685,-10.6015152323924));
#22198=CARTESIAN_POINT('Ctrl Pts',(-0.962845797709129,6.75786177513161,
-10.6163207779944));
#22199=CARTESIAN_POINT('Ctrl Pts',(-0.728007424527183,6.86719321021018,
-10.6414854333641));
#22200=CARTESIAN_POINT('Ctrl Pts',(-0.606894860616944,6.91001907374113,
-10.6518486458756));
#22201=CARTESIAN_POINT('Ctrl Pts',(-0.358236021802618,6.97180044684728,
-10.6670261603999));
#22202=CARTESIAN_POINT('Ctrl Pts',(-0.231503426306791,6.99067815064411,
-10.6718103168311));
#22203=CARTESIAN_POINT('Ctrl Pts',(-0.0690990145370653,6.99910518679761,
-10.6739387219855));
#22204=CARTESIAN_POINT('Ctrl Pts',(-0.0345417346423837,7.,-10.6741642768345));
#22205=CARTESIAN_POINT('Ctrl Pts',(3.0952483991701E-16,7.,-10.6741648723787));
#22206=CARTESIAN_POINT('Origin',(0.,5.,-11.1));
#22207=CARTESIAN_POINT('',(-2.,4.99999999999881,10.4183332085574));
#22208=CARTESIAN_POINT('',(-2.,5.,-11.1));
#22209=CARTESIAN_POINT('',(2.,5.,10.4183332061262));
#22210=CARTESIAN_POINT('Ctrl Pts',(-2.,4.99999999999762,10.4183332085574));
#22211=CARTESIAN_POINT('Ctrl Pts',(-1.99999999999971,4.75764050990674,10.4183333996923));
#22212=CARTESIAN_POINT('Ctrl Pts',(-1.95601203851425,4.51791095132192,10.4300808595327));
#22213=CARTESIAN_POINT('Ctrl Pts',(-1.78001439082704,4.05299932846605,10.4725856857188));
#22214=CARTESIAN_POINT('Ctrl Pts',(-1.64486906100864,3.83420865177878,10.5037554238368));
#22215=CARTESIAN_POINT('Ctrl Pts',(-1.29669691407628,3.45521458398486,10.5694095067776));
#22216=CARTESIAN_POINT('Ctrl Pts',(-1.08447711464625,3.29935703486476,10.6031801734129));
#22217=CARTESIAN_POINT('Ctrl Pts',(-0.614102032533418,3.07920133939685,
10.6537952714221));
#22218=CARTESIAN_POINT('Ctrl Pts',(-0.361056943994989,3.01584209266149,
10.6701647452922));
#22219=CARTESIAN_POINT('Ctrl Pts',(0.151263373348514,2.9896593782464,10.6767753112161));
#22220=CARTESIAN_POINT('Ctrl Pts',(0.40405218080261,3.0249721729091,10.667493673275));
#22221=CARTESIAN_POINT('Ctrl Pts',(0.887315218439553,3.18921348309502,10.6280783550302));
#22222=CARTESIAN_POINT('Ctrl Pts',(1.11205311096585,3.31806661278736,10.598173329718));
#22223=CARTESIAN_POINT('Ctrl Pts',(1.50518996696904,3.65702224569566,10.5326192482352));
#22224=CARTESIAN_POINT('Ctrl Pts',(1.66885927304681,3.86665024154239,10.4976296441678));
#22225=CARTESIAN_POINT('Ctrl Pts',(1.84524281816655,4.21783738115516,10.4570160383264));
#22226=CARTESIAN_POINT('Ctrl Pts',(1.89199289101732,4.33881643265941,10.4455972008102));
#22227=CARTESIAN_POINT('Ctrl Pts',(1.97544365595881,4.63862060372576,10.4248069793727));
#22228=CARTESIAN_POINT('Ctrl Pts',(2.,4.81896546073527,10.4183332250375));
#22229=CARTESIAN_POINT('Ctrl Pts',(2.,5.,10.4183332061262));
#22230=CARTESIAN_POINT('Ctrl Pts',(2.,5.,10.4183332061262));
#22231=CARTESIAN_POINT('Ctrl Pts',(2.,5.07412445802377,10.418333198383));
#22232=CARTESIAN_POINT('Ctrl Pts',(1.99588006958343,5.14836454540958,10.419403803429));
#22233=CARTESIAN_POINT('Ctrl Pts',(1.97348611150443,5.34850362220855,10.4251649570087));
#22234=CARTESIAN_POINT('Ctrl Pts',(1.94744895610822,5.47275424065624,10.4318462442253));
#22235=CARTESIAN_POINT('Ctrl Pts',(1.87218782309222,5.7148378129423,10.4504277671373));
#22236=CARTESIAN_POINT('Ctrl Pts',(1.82319167245477,5.83183046398235,10.4622438955467));
#22237=CARTESIAN_POINT('Ctrl Pts',(1.64087140867284,6.17270872224318,10.5036508546895));
#22238=CARTESIAN_POINT('Ctrl Pts',(1.47469697164074,6.37574114434066,10.5384558490889));
#22239=CARTESIAN_POINT('Ctrl Pts',(1.22410831831214,6.58299080923761,10.5792185726714));
#22240=CARTESIAN_POINT('Ctrl Pts',(1.17151858524451,6.62229933469441,10.5872695267222));
#22241=CARTESIAN_POINT('Ctrl Pts',(1.00965163715467,6.73129131268717,10.6103041534442));
#22242=CARTESIAN_POINT('Ctrl Pts',(0.895447882346682,6.79304313854791,10.6242895223643));
#22243=CARTESIAN_POINT('Ctrl Pts',(0.657087920935124,6.89336884418513,10.6477466535023));
#22244=CARTESIAN_POINT('Ctrl Pts',(0.533548659590622,6.93184892211207,10.6571764889425));
#22245=CARTESIAN_POINT('Ctrl Pts',(0.157607534485302,7.00998184253995,10.6765326365133));
#22246=CARTESIAN_POINT('Ctrl Pts',(-0.0990741273170037,7.01373005525968,
10.677526398444));
#22247=CARTESIAN_POINT('Ctrl Pts',(-0.475136684057559,6.94689825343089,
10.6608827373417));
#22248=CARTESIAN_POINT('Ctrl Pts',(-0.597744082024631,6.91279020306442,
10.65245495717));
#22249=CARTESIAN_POINT('Ctrl Pts',(-0.834479354355938,6.8220104651307,10.6309662827231));
#22250=CARTESIAN_POINT('Ctrl Pts',(-0.948120173018753,6.76552135149282,
10.6179467410782));
#22251=CARTESIAN_POINT('Ctrl Pts',(-1.27766645441521,6.56075349650328,10.5736998888191));
#22252=CARTESIAN_POINT('Ctrl Pts',(-1.4704451602617,6.38058619310992,10.5381856353254));
#22253=CARTESIAN_POINT('Ctrl Pts',(-1.7410164018396,6.00479346392452,10.4817961217748));
#22254=CARTESIAN_POINT('Ctrl Pts',(-1.83374938940646,5.82370479851062,10.4597876312556));
#22255=CARTESIAN_POINT('Ctrl Pts',(-1.9617280423452,5.43897136051534,10.4284252760763));
#22256=CARTESIAN_POINT('Ctrl Pts',(-1.99618860231403,5.2378760573922,10.4193156447857));
#22257=CARTESIAN_POINT('Ctrl Pts',(-1.99970195790469,5.03455443435168,10.4184105149837));
#22258=CARTESIAN_POINT('Ctrl Pts',(-1.99990107789324,5.02303114893203,10.4183592166078));
#22259=CARTESIAN_POINT('Ctrl Pts',(-2.00000000000001,5.0115126072,10.4183331994781));
#22260=CARTESIAN_POINT('Ctrl Pts',(-2.,4.99999999999762,10.4183332085574));
#22261=CARTESIAN_POINT('Origin',(0.,13.2,0.));
#22262=CARTESIAN_POINT('Origin',(-1.39303573403011E-15,13.2,11.375));
#22263=CARTESIAN_POINT('Origin',(0.,76.2,0.));
#22264=CARTESIAN_POINT('Origin',(-1.39303573403011E-15,76.2,11.375));
#22265=CARTESIAN_POINT('Ctrl Pts',(0.,32.7351420011818,-14.8300672611831));
#22266=CARTESIAN_POINT('Ctrl Pts',(0.,33.045415593,-14.3047121186603));
#22267=CARTESIAN_POINT('Ctrl Pts',(0.,33.63686551036,-13.97));
#22268=CARTESIAN_POINT('Ctrl Pts',(0.,34.2419663837872,-13.97));
#22269=CARTESIAN_POINT('Ctrl Pts',(3.73,32.7351420011818,-14.8300672611831));
#22270=CARTESIAN_POINT('Ctrl Pts',(3.73,33.045415593,-14.3047121186603));
#22271=CARTESIAN_POINT('Ctrl Pts',(3.73,33.63686551036,-13.97));
#22272=CARTESIAN_POINT('Ctrl Pts',(3.73,34.2419663837872,-13.97));
#22273=CARTESIAN_POINT('Ctrl Pts',(3.73,32.7351420011818,-11.1000672611831));
#22274=CARTESIAN_POINT('Ctrl Pts',(3.73,33.045415593,-10.5747121186603));
#22275=CARTESIAN_POINT('Ctrl Pts',(3.73,33.63686551036,-10.24));
#22276=CARTESIAN_POINT('Ctrl Pts',(3.73,34.2419663837872,-10.24));
#22277=CARTESIAN_POINT('Ctrl Pts',(2.28396628040981E-16,32.7351420011818,
-11.1000672611831));
#22278=CARTESIAN_POINT('Ctrl Pts',(2.28396628040981E-16,33.045415593,-10.5747121186603));
#22279=CARTESIAN_POINT('Ctrl Pts',(2.28396628040981E-16,33.63686551036,
-10.24));
#22280=CARTESIAN_POINT('Ctrl Pts',(2.28396628040981E-16,34.2419663837872,
-10.24));
#22281=CARTESIAN_POINT('Ctrl Pts',(-3.73,32.7351420011818,-11.1000672611831));
#22282=CARTESIAN_POINT('Ctrl Pts',(-3.73,33.045415593,-10.5747121186603));
#22283=CARTESIAN_POINT('Ctrl Pts',(-3.73,33.63686551036,-10.24));
#22284=CARTESIAN_POINT('Ctrl Pts',(-3.73,34.2419663837872,-10.24));
#22285=CARTESIAN_POINT('Ctrl Pts',(-3.73,32.7351420011818,-14.8300672611831));
#22286=CARTESIAN_POINT('Ctrl Pts',(-3.73,33.045415593,-14.3047121186603));
#22287=CARTESIAN_POINT('Ctrl Pts',(-3.73,33.63686551036,-13.97));
#22288=CARTESIAN_POINT('Ctrl Pts',(-3.73,34.2419663837872,-13.97));
#22289=CARTESIAN_POINT('Ctrl Pts',(0.,32.7351420011818,-14.8300672611831));
#22290=CARTESIAN_POINT('Ctrl Pts',(0.,33.045415593,-14.3047121186603));
#22291=CARTESIAN_POINT('Ctrl Pts',(0.,33.63686551036,-13.97));
#22292=CARTESIAN_POINT('Ctrl Pts',(0.,34.2419663837872,-13.97));
#22293=CARTESIAN_POINT('Origin',(0.,34.2419663837872,-12.105));
#22294=CARTESIAN_POINT('Origin',(0.,34.2419663837872,-12.105));
#22295=CARTESIAN_POINT('Origin',(0.,71.2419663837872,-12.105));
#22296=CARTESIAN_POINT('Ctrl Pts',(0.,71.2419663837872,-13.97));
#22297=CARTESIAN_POINT('Ctrl Pts',(0.,71.847073728999,-13.97));
#22298=CARTESIAN_POINT('Ctrl Pts',(0.,72.4385298261441,-14.3047192784616));
#22299=CARTESIAN_POINT('Ctrl Pts',(0.,72.7488007217793,-14.8300841178694));
#22300=CARTESIAN_POINT('Ctrl Pts',(3.73,71.2419663837872,-13.97));
#22301=CARTESIAN_POINT('Ctrl Pts',(3.73,71.847073728999,-13.97));
#22302=CARTESIAN_POINT('Ctrl Pts',(3.73,72.4385298261441,-14.3047192784616));
#22303=CARTESIAN_POINT('Ctrl Pts',(3.73,72.7488007217793,-14.8300841178694));
#22304=CARTESIAN_POINT('Ctrl Pts',(3.73,71.2419663837872,-10.24));
#22305=CARTESIAN_POINT('Ctrl Pts',(3.73,71.847073728999,-10.24));
#22306=CARTESIAN_POINT('Ctrl Pts',(3.73,72.4385298261441,-10.5747192784616));
#22307=CARTESIAN_POINT('Ctrl Pts',(3.73,72.7488007217793,-11.1000841178694));
#22308=CARTESIAN_POINT('Ctrl Pts',(2.28396628040981E-16,71.2419663837872,
-10.24));
#22309=CARTESIAN_POINT('Ctrl Pts',(2.28396628040981E-16,71.847073728999,
-10.24));
#22310=CARTESIAN_POINT('Ctrl Pts',(2.28396628040981E-16,72.4385298261441,
-10.5747192784616));
#22311=CARTESIAN_POINT('Ctrl Pts',(2.28396628040981E-16,72.7488007217793,
-11.1000841178694));
#22312=CARTESIAN_POINT('Ctrl Pts',(-3.73,71.2419663837872,-10.24));
#22313=CARTESIAN_POINT('Ctrl Pts',(-3.73,71.847073728999,-10.24));
#22314=CARTESIAN_POINT('Ctrl Pts',(-3.73,72.4385298261441,-10.5747192784616));
#22315=CARTESIAN_POINT('Ctrl Pts',(-3.73,72.7488007217793,-11.1000841178694));
#22316=CARTESIAN_POINT('Ctrl Pts',(-3.73,71.2419663837872,-13.97));
#22317=CARTESIAN_POINT('Ctrl Pts',(-3.73,71.847073728999,-13.97));
#22318=CARTESIAN_POINT('Ctrl Pts',(-3.73,72.4385298261441,-14.3047192784616));
#22319=CARTESIAN_POINT('Ctrl Pts',(-3.73,72.7488007217793,-14.8300841178694));
#22320=CARTESIAN_POINT('Ctrl Pts',(0.,71.2419663837872,-13.97));
#22321=CARTESIAN_POINT('Ctrl Pts',(0.,71.847073728999,-13.97));
#22322=CARTESIAN_POINT('Ctrl Pts',(0.,72.4385298261441,-14.3047192784616));
#22323=CARTESIAN_POINT('Ctrl Pts',(0.,72.7488007217793,-14.8300841178694));
#22324=CARTESIAN_POINT('Ctrl Pts',(8.71689482662887,32.7351420011818,-11.9977764420207));
#22325=CARTESIAN_POINT('Ctrl Pts',(8.40809882163646,33.045415593,-11.5727552036368));
#22326=CARTESIAN_POINT('Ctrl Pts',(8.21135997452586,33.63686551036,-11.301967411418));
#22327=CARTESIAN_POINT('Ctrl Pts',(8.21135997452587,34.2419663837872,-11.301967411418));
#22328=CARTESIAN_POINT('Ctrl Pts',(11.7345282156474,32.7351420011818,-9.80533745096972));
#22329=CARTESIAN_POINT('Ctrl Pts',(11.4257322106545,33.045415593,-9.38031621258584));
#22330=CARTESIAN_POINT('Ctrl Pts',(11.2289933635444,33.63686551036,-9.10952842036708));
#22331=CARTESIAN_POINT('Ctrl Pts',(11.2289933635444,34.2419663837872,-9.10952842036708));
#22332=CARTESIAN_POINT('Ctrl Pts',(9.54208922459649,32.7351420011818,-6.78770406195117));
#22333=CARTESIAN_POINT('Ctrl Pts',(9.23329321960567,33.045415593,-6.36268282356729));
#22334=CARTESIAN_POINT('Ctrl Pts',(9.03655437249349,33.63686551036,-6.09189503134852));
#22335=CARTESIAN_POINT('Ctrl Pts',(9.03655437249349,34.2419663837872,-6.09189503134852));
#22336=CARTESIAN_POINT('Ctrl Pts',(6.52445583557794,32.7351420011818,-8.9801430530021));
#22337=CARTESIAN_POINT('Ctrl Pts',(6.21565983058659,33.045415593,-8.55512181461823));
#22338=CARTESIAN_POINT('Ctrl Pts',(6.01892098347494,33.63686551036,-8.28433402239945));
#22339=CARTESIAN_POINT('Ctrl Pts',(6.01892098347494,34.2419663837872,-8.28433402239945));
#22340=CARTESIAN_POINT('Ctrl Pts',(3.50682244655939,32.7351420011818,-11.172582044053));
#22341=CARTESIAN_POINT('Ctrl Pts',(3.19802644156751,33.045415593,-10.7475608056691));
#22342=CARTESIAN_POINT('Ctrl Pts',(3.00128759445638,33.63686551036,-10.4767730134504));
#22343=CARTESIAN_POINT('Ctrl Pts',(3.00128759445639,34.2419663837872,-10.4767730134504));
#22344=CARTESIAN_POINT('Ctrl Pts',(5.69926143761032,32.7351420011818,-14.1902154330716));
#22345=CARTESIAN_POINT('Ctrl Pts',(5.39046543261844,33.045415593,-13.7651941946877));
#22346=CARTESIAN_POINT('Ctrl Pts',(5.19372658550731,33.63686551036,-13.4944064024689));
#22347=CARTESIAN_POINT('Ctrl Pts',(5.19372658550731,34.2419663837872,-13.4944064024689));
#22348=CARTESIAN_POINT('Ctrl Pts',(8.71689482662887,32.7351420011818,-11.9977764420207));
#22349=CARTESIAN_POINT('Ctrl Pts',(8.40809882163646,33.045415593,-11.5727552036368));
#22350=CARTESIAN_POINT('Ctrl Pts',(8.21135997452586,33.63686551036,-11.301967411418));
#22351=CARTESIAN_POINT('Ctrl Pts',(8.21135997452587,34.2419663837872,-11.301967411418));
#22352=CARTESIAN_POINT('Origin',(7.1151404790004,34.2419663837872,-9.79315071690873));
#22353=CARTESIAN_POINT('Origin',(7.1151404790004,34.2419663837872,-9.79315071690873));
#22354=CARTESIAN_POINT('Origin',(7.1151404790004,71.2419663837872,-9.79315071690873));
#22355=CARTESIAN_POINT('Ctrl Pts',(8.21135997452587,71.2419663837872,-11.301967411418));
#22356=CARTESIAN_POINT('Ctrl Pts',(8.21135997452587,71.847073728999,-11.301967411418));
#22357=CARTESIAN_POINT('Ctrl Pts',(8.40810303006151,72.4385298261441,-11.572760996038));
#22358=CARTESIAN_POINT('Ctrl Pts',(8.71690473474048,72.7488007217793,-11.9977900793663));
#22359=CARTESIAN_POINT('Ctrl Pts',(11.2289933635444,71.2419663837872,-9.10952842036708));
#22360=CARTESIAN_POINT('Ctrl Pts',(11.2289933635444,71.847073728999,-9.10952842036708));
#22361=CARTESIAN_POINT('Ctrl Pts',(11.4257364190791,72.4385298261441,-9.38032200498704));
#22362=CARTESIAN_POINT('Ctrl Pts',(11.734538123759,72.7488007217793,-9.8053510883154));
#22363=CARTESIAN_POINT('Ctrl Pts',(9.03655437249349,71.2419663837872,-6.09189503134853));
#22364=CARTESIAN_POINT('Ctrl Pts',(9.03655437249349,71.847073728999,-6.09189503134853));
#22365=CARTESIAN_POINT('Ctrl Pts',(9.23329742803191,72.4385298261441,-6.36268861596848));
#22366=CARTESIAN_POINT('Ctrl Pts',(9.5420991327081,72.7488007217793,-6.78771769929685));
#22367=CARTESIAN_POINT('Ctrl Pts',(6.01892098347494,71.2419663837872,-8.28433402239945));
#22368=CARTESIAN_POINT('Ctrl Pts',(6.01892098347494,71.847073728999,-8.28433402239945));
#22369=CARTESIAN_POINT('Ctrl Pts',(6.21566403901243,72.4385298261441,-8.55512760701941));
#22370=CARTESIAN_POINT('Ctrl Pts',(6.52446574368955,72.7488007217793,-8.98015669034778));
#22371=CARTESIAN_POINT('Ctrl Pts',(3.00128759445639,71.2419663837872,-10.4767730134504));
#22372=CARTESIAN_POINT('Ctrl Pts',(3.00128759445639,71.847073728999,-10.4767730134504));
#22373=CARTESIAN_POINT('Ctrl Pts',(3.19803064999295,72.4385298261441,-10.7475665980703));
#22374=CARTESIAN_POINT('Ctrl Pts',(3.506832354671,72.7488007217793,-11.1725956813987));
#22375=CARTESIAN_POINT('Ctrl Pts',(5.19372658550732,71.2419663837872,-13.4944064024689));
#22376=CARTESIAN_POINT('Ctrl Pts',(5.19372658550732,71.847073728999,-13.4944064024689));
#22377=CARTESIAN_POINT('Ctrl Pts',(5.39046964104388,72.4385298261441,-13.7651999870889));
#22378=CARTESIAN_POINT('Ctrl Pts',(5.69927134572193,72.7488007217793,-14.1902290704173));
#22379=CARTESIAN_POINT('Ctrl Pts',(8.21135997452587,71.2419663837872,-11.301967411418));
#22380=CARTESIAN_POINT('Ctrl Pts',(8.21135997452587,71.847073728999,-11.301967411418));
#22381=CARTESIAN_POINT('Ctrl Pts',(8.40810303006151,72.4385298261441,-11.572760996038));
#22382=CARTESIAN_POINT('Ctrl Pts',(8.71690473474048,72.7488007217793,-11.9977900793663));
#22383=CARTESIAN_POINT('Ctrl Pts',(14.1042321058436,32.7351420011818,-4.58274281142907));
#22384=CARTESIAN_POINT('Ctrl Pts',(13.604589674176,33.045415593,-4.42039914430687));
#22385=CARTESIAN_POINT('Ctrl Pts',(13.2862595326433,33.63686551036,-4.31696741141798));
#22386=CARTESIAN_POINT('Ctrl Pts',(13.2862595326433,34.2419663837872,-4.31696741141798));
#22387=CARTESIAN_POINT('Ctrl Pts',(15.2568654948622,32.7351420011818,-1.03530200564814));
#22388=CARTESIAN_POINT('Ctrl Pts',(14.7572230631946,33.045415593,-0.872958338525147));
#22389=CARTESIAN_POINT('Ctrl Pts',(14.4388929216619,33.63686551036,-0.76952660563705));
#22390=CARTESIAN_POINT('Ctrl Pts',(14.4388929216619,34.2419663837872,-0.769526605637051));
#22391=CARTESIAN_POINT('Ctrl Pts',(11.7094246890812,32.7351420011818,0.117331383370402));
#22392=CARTESIAN_POINT('Ctrl Pts',(11.2097822574136,33.045415593,0.279675050492603));
#22393=CARTESIAN_POINT('Ctrl Pts',(10.8914521158809,33.63686551036,0.383106783381494));
#22394=CARTESIAN_POINT('Ctrl Pts',(10.8914521158809,34.2419663837872,0.383106783381493));
#22395=CARTESIAN_POINT('Ctrl Pts',(10.5567913000627,32.7351420011818,-3.43010942241053));
#22396=CARTESIAN_POINT('Ctrl Pts',(10.0571488683951,33.045415593,-3.26776575528832));
#22397=CARTESIAN_POINT('Ctrl Pts',(9.73881872686238,33.63686551036,-3.16433402239943));
#22398=CARTESIAN_POINT('Ctrl Pts',(9.73881872686238,34.2419663837872,-3.16433402239943));
#22399=CARTESIAN_POINT('Ctrl Pts',(9.40415791104414,32.7351420011818,-6.97755022819145));
#22400=CARTESIAN_POINT('Ctrl Pts',(8.90451547937655,33.045415593,-6.81520656106925));
#22401=CARTESIAN_POINT('Ctrl Pts',(8.58618533784384,33.63686551036,-6.71177482818036));
#22402=CARTESIAN_POINT('Ctrl Pts',(8.58618533784384,34.2419663837872,-6.71177482818036));
#22403=CARTESIAN_POINT('Ctrl Pts',(12.9515987168251,32.7351420011818,-8.13018361720999));
#22404=CARTESIAN_POINT('Ctrl Pts',(12.4519562851575,33.045415593,-7.96783995008859));
#22405=CARTESIAN_POINT('Ctrl Pts',(12.1336261436248,33.63686551036,-7.86440821719891));
#22406=CARTESIAN_POINT('Ctrl Pts',(12.1336261436248,34.2419663837872,-7.86440821719891));
#22407=CARTESIAN_POINT('Ctrl Pts',(14.1042321058436,32.7351420011818,-4.58274281142907));
#22408=CARTESIAN_POINT('Ctrl Pts',(13.604589674176,33.045415593,-4.42039914430687));
#22409=CARTESIAN_POINT('Ctrl Pts',(13.2862595326433,33.63686551036,-4.31696741141798));
#22410=CARTESIAN_POINT('Ctrl Pts',(13.2862595326433,34.2419663837872,-4.31696741141798));
#22411=CARTESIAN_POINT('Origin',(11.5125391297528,34.2419663837872,-3.74065071690871));
#22412=CARTESIAN_POINT('Origin',(11.5125391297528,34.2419663837872,-3.74065071690871));
#22413=CARTESIAN_POINT('Origin',(11.5125391297528,71.2419663837872,-3.74065071690871));
#22414=CARTESIAN_POINT('Ctrl Pts',(13.2862595326433,71.2419663837872,-4.31696741141798));
#22415=CARTESIAN_POINT('Ctrl Pts',(13.2862595326433,71.847073728999,-4.31696741141798));
#22416=CARTESIAN_POINT('Ctrl Pts',(13.6045964835519,72.4385298261441,-4.42040135680742));
#22417=CARTESIAN_POINT('Ctrl Pts',(14.104248137505,72.7488007217793,-4.5827480204316));
#22418=CARTESIAN_POINT('Ctrl Pts',(14.4388929216619,71.2419663837872,-0.769526605637053));
#22419=CARTESIAN_POINT('Ctrl Pts',(14.4388929216619,71.847073728999,-0.769526605637052));
#22420=CARTESIAN_POINT('Ctrl Pts',(14.7572298725705,72.4385298261441,-0.872960551026562));
#22421=CARTESIAN_POINT('Ctrl Pts',(15.2568815265235,72.7488007217793,-1.03530721465068));
#22422=CARTESIAN_POINT('Ctrl Pts',(10.8914521158809,71.2419663837872,0.383106783381491));
#22423=CARTESIAN_POINT('Ctrl Pts',(10.8914521158809,71.847073728999,0.383106783381492));
#22424=CARTESIAN_POINT('Ctrl Pts',(11.2097890667895,72.4385298261441,0.279672837992247));
#22425=CARTESIAN_POINT('Ctrl Pts',(11.7094407207426,72.7488007217793,0.117326174367868));
#22426=CARTESIAN_POINT('Ctrl Pts',(9.73881872686238,71.2419663837872,-3.16433402239944));
#22427=CARTESIAN_POINT('Ctrl Pts',(9.73881872686238,71.847073728999,-3.16433402239943));
#22428=CARTESIAN_POINT('Ctrl Pts',(10.057155677771,72.4385298261441,-3.26776796778875));
#22429=CARTESIAN_POINT('Ctrl Pts',(10.556807331724,72.7488007217793,-3.43011463141306));
#22430=CARTESIAN_POINT('Ctrl Pts',(8.58618533784384,71.2419663837872,-6.71177482818036));
#22431=CARTESIAN_POINT('Ctrl Pts',(8.58618533784384,71.847073728999,-6.71177482818036));
#22432=CARTESIAN_POINT('Ctrl Pts',(8.90452228875243,72.4385298261441,-6.81520877356974));
#22433=CARTESIAN_POINT('Ctrl Pts',(9.40417394270549,72.7488007217793,-6.97755543719399));
#22434=CARTESIAN_POINT('Ctrl Pts',(12.1336261436248,71.2419663837872,-7.86440821719891));
#22435=CARTESIAN_POINT('Ctrl Pts',(12.1336261436248,71.847073728999,-7.86440821719891));
#22436=CARTESIAN_POINT('Ctrl Pts',(12.4519630945334,72.4385298261441,-7.96784216258828));
#22437=CARTESIAN_POINT('Ctrl Pts',(12.9516147484864,72.7488007217793,-8.13018882621253));
#22438=CARTESIAN_POINT('Ctrl Pts',(13.2862595326433,71.2419663837872,-4.31696741141798));
#22439=CARTESIAN_POINT('Ctrl Pts',(13.2862595326433,71.847073728999,-4.31696741141798));
#22440=CARTESIAN_POINT('Ctrl Pts',(13.6045964835519,72.4385298261441,-4.42040135680742));
#22441=CARTESIAN_POINT('Ctrl Pts',(14.104248137505,72.7488007217793,-4.5827480204316));
#22442=CARTESIAN_POINT('Ctrl Pts',(14.1042321058436,32.7351420011818,4.58274281142917));
#22443=CARTESIAN_POINT('Ctrl Pts',(13.604589674176,33.045415593,4.42039914430803));
#22444=CARTESIAN_POINT('Ctrl Pts',(13.2862595326433,33.63686551036,4.31696741141807));
#22445=CARTESIAN_POINT('Ctrl Pts',(13.2862595326433,34.2419663837872,4.31696741141807));
#22446=CARTESIAN_POINT('Ctrl Pts',(12.951598716825,32.7351420011818,8.1301836172101));
#22447=CARTESIAN_POINT('Ctrl Pts',(12.4519562851574,33.045415593,7.96783995008948));
#22448=CARTESIAN_POINT('Ctrl Pts',(12.1336261436247,33.63686551036,7.86440821719899));
#22449=CARTESIAN_POINT('Ctrl Pts',(12.1336261436247,34.2419663837872,7.86440821719899));
#22450=CARTESIAN_POINT('Ctrl Pts',(9.40415791104411,32.7351420011818,6.97755022819152));
#22451=CARTESIAN_POINT('Ctrl Pts',(8.90451547937651,33.045415593,6.81520656107038));
#22452=CARTESIAN_POINT('Ctrl Pts',(8.58618533784379,33.63686551036,6.71177482818042));
#22453=CARTESIAN_POINT('Ctrl Pts',(8.58618533784379,34.2419663837872,6.71177482818042));
#22454=CARTESIAN_POINT('Ctrl Pts',(10.5567913000627,32.7351420011818,3.43010942241061));
#22455=CARTESIAN_POINT('Ctrl Pts',(10.0571488683951,33.045415593,3.26776575528946));
#22456=CARTESIAN_POINT('Ctrl Pts',(9.73881872686236,33.63686551036,3.1643340223995));
#22457=CARTESIAN_POINT('Ctrl Pts',(9.73881872686236,34.2419663837872,3.16433402239951));
#22458=CARTESIAN_POINT('Ctrl Pts',(11.7094246890812,32.7351420011818,-0.117331383370314));
#22459=CARTESIAN_POINT('Ctrl Pts',(11.2097822574137,33.045415593,-0.279675050491458));
#22460=CARTESIAN_POINT('Ctrl Pts',(10.8914521158809,33.63686551036,-0.383106783381414));
#22461=CARTESIAN_POINT('Ctrl Pts',(10.8914521158809,34.2419663837872,-0.383106783381413));
#22462=CARTESIAN_POINT('Ctrl Pts',(15.2568654948622,32.7351420011818,1.03530200564826));
#22463=CARTESIAN_POINT('Ctrl Pts',(14.7572230631946,33.045415593,0.872958338526582));
#22464=CARTESIAN_POINT('Ctrl Pts',(14.4388929216619,33.63686551036,0.769526605637155));
#22465=CARTESIAN_POINT('Ctrl Pts',(14.4388929216619,34.2419663837872,0.769526605637156));
#22466=CARTESIAN_POINT('Ctrl Pts',(14.1042321058436,32.7351420011818,4.58274281142917));
#22467=CARTESIAN_POINT('Ctrl Pts',(13.604589674176,33.045415593,4.42039914430803));
#22468=CARTESIAN_POINT('Ctrl Pts',(13.2862595326433,33.63686551036,4.31696741141807));
#22469=CARTESIAN_POINT('Ctrl Pts',(13.2862595326433,34.2419663837872,4.31696741141807));
#22470=CARTESIAN_POINT('Origin',(11.5125391297528,34.2419663837872,3.74065071690879));
#22471=CARTESIAN_POINT('Origin',(11.5125391297528,34.2419663837872,3.74065071690879));
#22472=CARTESIAN_POINT('Origin',(11.5125391297528,71.2419663837872,3.74065071690879));
#22473=CARTESIAN_POINT('Ctrl Pts',(13.2862595326433,71.2419663837872,4.31696741141807));
#22474=CARTESIAN_POINT('Ctrl Pts',(13.2862595326433,71.847073728999,4.31696741141807));
#22475=CARTESIAN_POINT('Ctrl Pts',(13.6045964835519,72.4385298261441,4.42040135680726));
#22476=CARTESIAN_POINT('Ctrl Pts',(14.1042481375049,72.7488007217793,4.58274802043171));
#22477=CARTESIAN_POINT('Ctrl Pts',(12.1336261436247,71.2419663837872,7.86440821719899));
#22478=CARTESIAN_POINT('Ctrl Pts',(12.1336261436247,71.847073728999,7.86440821719899));
#22479=CARTESIAN_POINT('Ctrl Pts',(12.4519630945333,72.4385298261441,7.96784216258811));
#22480=CARTESIAN_POINT('Ctrl Pts',(12.9516147484864,72.7488007217793,8.13018882621263));
#22481=CARTESIAN_POINT('Ctrl Pts',(8.58618533784379,71.2419663837872,6.71177482818042));
#22482=CARTESIAN_POINT('Ctrl Pts',(8.58618533784379,71.847073728999,6.71177482818042));
#22483=CARTESIAN_POINT('Ctrl Pts',(8.90452228875239,72.4385298261441,6.81520877356968));
#22484=CARTESIAN_POINT('Ctrl Pts',(9.40417394270545,72.7488007217793,6.97755543719405));
#22485=CARTESIAN_POINT('Ctrl Pts',(9.73881872686236,71.2419663837872,3.16433402239951));
#22486=CARTESIAN_POINT('Ctrl Pts',(9.73881872686236,71.847073728999,3.16433402239951));
#22487=CARTESIAN_POINT('Ctrl Pts',(10.057155677771,72.4385298261441,3.26776796778882));
#22488=CARTESIAN_POINT('Ctrl Pts',(10.556807331724,72.7488007217793,3.43011463141314));
#22489=CARTESIAN_POINT('Ctrl Pts',(10.8914521158809,71.2419663837872,-0.383106783381413));
#22490=CARTESIAN_POINT('Ctrl Pts',(10.8914521158809,71.847073728999,-0.383106783381413));
#22491=CARTESIAN_POINT('Ctrl Pts',(11.2097890667895,72.4385298261441,-0.27967283799203));
#22492=CARTESIAN_POINT('Ctrl Pts',(11.7094407207426,72.7488007217793,-0.117326174367781));
#22493=CARTESIAN_POINT('Ctrl Pts',(14.4388929216619,71.2419663837872,0.769526605637156));
#22494=CARTESIAN_POINT('Ctrl Pts',(14.4388929216619,71.847073728999,0.769526605637156));
#22495=CARTESIAN_POINT('Ctrl Pts',(14.7572298725704,72.4385298261441,0.872960551026407));
#22496=CARTESIAN_POINT('Ctrl Pts',(15.2568815265235,72.7488007217793,1.03530721465079));
#22497=CARTESIAN_POINT('Ctrl Pts',(13.2862595326433,71.2419663837872,4.31696741141807));
#22498=CARTESIAN_POINT('Ctrl Pts',(13.2862595326433,71.847073728999,4.31696741141807));
#22499=CARTESIAN_POINT('Ctrl Pts',(13.6045964835519,72.4385298261441,4.42040135680726));
#22500=CARTESIAN_POINT('Ctrl Pts',(14.1042481375049,72.7488007217793,4.58274802043171));
#22501=CARTESIAN_POINT('Ctrl Pts',(8.71689482662879,32.7351420011818,11.9977764420207));
#22502=CARTESIAN_POINT('Ctrl Pts',(8.40809882163849,33.045415593,11.5727552036368));
#22503=CARTESIAN_POINT('Ctrl Pts',(8.21135997452579,33.63686551036,11.3019674114181));
#22504=CARTESIAN_POINT('Ctrl Pts',(8.21135997452579,34.2419663837872,11.3019674114181));
#22505=CARTESIAN_POINT('Ctrl Pts',(5.69926143761022,32.7351420011818,14.1902154330716));
#22506=CARTESIAN_POINT('Ctrl Pts',(5.39046543261953,33.045415593,13.7651941946877));
#22507=CARTESIAN_POINT('Ctrl Pts',(5.19372658550722,33.63686551036,13.494406402469));
#22508=CARTESIAN_POINT('Ctrl Pts',(5.19372658550722,34.2419663837872,13.494406402469));
#22509=CARTESIAN_POINT('Ctrl Pts',(3.50682244655931,32.7351420011818,11.172582044053));
#22510=CARTESIAN_POINT('Ctrl Pts',(3.19802644156862,33.045415593,10.7475608056692));
#22511=CARTESIAN_POINT('Ctrl Pts',(3.00128759445631,33.63686551036,10.4767730134504));
#22512=CARTESIAN_POINT('Ctrl Pts',(3.00128759445631,34.2419663837872,10.4767730134504));
#22513=CARTESIAN_POINT('Ctrl Pts',(6.52445583557788,32.7351420011818,8.98014305300214));
#22514=CARTESIAN_POINT('Ctrl Pts',(6.21565983058679,33.045415593,8.55512181461826));
#22515=CARTESIAN_POINT('Ctrl Pts',(6.01892098347488,33.63686551036,8.28433402239949));
#22516=CARTESIAN_POINT('Ctrl Pts',(6.01892098347488,34.2419663837872,8.2843340223995));
#22517=CARTESIAN_POINT('Ctrl Pts',(9.54208922459645,32.7351420011818,6.78770406195123));
#22518=CARTESIAN_POINT('Ctrl Pts',(9.23329321960496,33.045415593,6.36268282356736));
#22519=CARTESIAN_POINT('Ctrl Pts',(9.03655437249344,33.63686551036,6.09189503134859));
#22520=CARTESIAN_POINT('Ctrl Pts',(9.03655437249345,34.2419663837872,6.09189503134859));
#22521=CARTESIAN_POINT('Ctrl Pts',(11.7345282156474,32.7351420011818,9.8053374509698));
#22522=CARTESIAN_POINT('Ctrl Pts',(11.4257322106575,33.045415593,9.38031621258592));
#22523=CARTESIAN_POINT('Ctrl Pts',(11.2289933635444,33.63686551036,9.10952842036716));
#22524=CARTESIAN_POINT('Ctrl Pts',(11.2289933635444,34.2419663837872,9.10952842036715));
#22525=CARTESIAN_POINT('Ctrl Pts',(8.71689482662879,32.7351420011818,11.9977764420207));
#22526=CARTESIAN_POINT('Ctrl Pts',(8.40809882163849,33.045415593,11.5727552036368));
#22527=CARTESIAN_POINT('Ctrl Pts',(8.21135997452579,33.63686551036,11.3019674114181));
#22528=CARTESIAN_POINT('Ctrl Pts',(8.21135997452579,34.2419663837872,11.3019674114181));
#22529=CARTESIAN_POINT('Origin',(7.11514047900033,34.2419663837872,9.79315071690878));
#22530=CARTESIAN_POINT('Origin',(7.11514047900033,34.2419663837872,9.79315071690878));
#22531=CARTESIAN_POINT('Origin',(7.11514047900033,71.2419663837872,9.79315071690878));
#22532=CARTESIAN_POINT('Ctrl Pts',(8.21135997452579,71.2419663837872,11.3019674114181));
#22533=CARTESIAN_POINT('Ctrl Pts',(8.21135997452579,71.847073728999,11.3019674114181));
#22534=CARTESIAN_POINT('Ctrl Pts',(8.40810303006512,72.4385298261441,11.572760996038));
#22535=CARTESIAN_POINT('Ctrl Pts',(8.7169047347404,72.7488007217793,11.9977900793664));
#22536=CARTESIAN_POINT('Ctrl Pts',(5.19372658550722,71.2419663837872,13.494406402469));
#22537=CARTESIAN_POINT('Ctrl Pts',(5.19372658550722,71.847073728999,13.494406402469));
#22538=CARTESIAN_POINT('Ctrl Pts',(5.39046964104563,72.4385298261441,13.7651999870889));
#22539=CARTESIAN_POINT('Ctrl Pts',(5.69927134572183,72.7488007217793,14.1902290704173));
#22540=CARTESIAN_POINT('Ctrl Pts',(3.00128759445631,71.2419663837872,10.4767730134504));
#22541=CARTESIAN_POINT('Ctrl Pts',(3.00128759445631,71.847073728999,10.4767730134504));
#22542=CARTESIAN_POINT('Ctrl Pts',(3.19803064999473,72.4385298261441,10.7475665980704));
#22543=CARTESIAN_POINT('Ctrl Pts',(3.50683235467092,72.7488007217793,11.1725956813987));
#22544=CARTESIAN_POINT('Ctrl Pts',(6.01892098347488,71.2419663837872,8.2843340223995));
#22545=CARTESIAN_POINT('Ctrl Pts',(6.01892098347488,71.847073728999,8.2843340223995));
#22546=CARTESIAN_POINT('Ctrl Pts',(6.21566403901237,72.4385298261441,8.55512760701946));
#22547=CARTESIAN_POINT('Ctrl Pts',(6.52446574368949,72.7488007217793,8.98015669034783));
#22548=CARTESIAN_POINT('Ctrl Pts',(9.03655437249345,71.2419663837872,6.09189503134859));
#22549=CARTESIAN_POINT('Ctrl Pts',(9.03655437249345,71.847073728999,6.09189503134859));
#22550=CARTESIAN_POINT('Ctrl Pts',(9.23329742803001,72.4385298261441,6.36268861596855));
#22551=CARTESIAN_POINT('Ctrl Pts',(9.54209913270805,72.7488007217793,6.78771769929692));
#22552=CARTESIAN_POINT('Ctrl Pts',(11.2289933635444,71.2419663837872,9.10952842036715));
#22553=CARTESIAN_POINT('Ctrl Pts',(11.2289933635444,71.847073728999,9.10952842036715));
#22554=CARTESIAN_POINT('Ctrl Pts',(11.4257364190846,72.4385298261441,9.38032200498712));
#22555=CARTESIAN_POINT('Ctrl Pts',(11.734538123759,72.7488007217793,9.80535108831548));
#22556=CARTESIAN_POINT('Ctrl Pts',(8.21135997452579,71.2419663837872,11.3019674114181));
#22557=CARTESIAN_POINT('Ctrl Pts',(8.21135997452579,71.847073728999,11.3019674114181));
#22558=CARTESIAN_POINT('Ctrl Pts',(8.40810303006512,72.4385298261441,11.572760996038));
#22559=CARTESIAN_POINT('Ctrl Pts',(8.7169047347404,72.7488007217793,11.9977900793664));
#22560=CARTESIAN_POINT('Ctrl Pts',(0.,32.7351420011818,14.8300672611831));
#22561=CARTESIAN_POINT('Ctrl Pts',(0.,33.045415593,14.3047121186603));
#22562=CARTESIAN_POINT('Ctrl Pts',(0.,33.63686551036,13.97));
#22563=CARTESIAN_POINT('Ctrl Pts',(0.,34.2419663837872,13.97));
#22564=CARTESIAN_POINT('Ctrl Pts',(-3.73,32.7351420011818,14.8300672611831));
#22565=CARTESIAN_POINT('Ctrl Pts',(-3.73,33.045415593,14.3047121186603));
#22566=CARTESIAN_POINT('Ctrl Pts',(-3.73,33.63686551036,13.97));
#22567=CARTESIAN_POINT('Ctrl Pts',(-3.73,34.2419663837872,13.97));
#22568=CARTESIAN_POINT('Ctrl Pts',(-3.73,32.7351420011818,11.1000672611831));
#22569=CARTESIAN_POINT('Ctrl Pts',(-3.73,33.045415593,10.5747121186603));
#22570=CARTESIAN_POINT('Ctrl Pts',(-3.73,33.63686551036,10.24));
#22571=CARTESIAN_POINT('Ctrl Pts',(-3.73,34.2419663837872,10.24));
#22572=CARTESIAN_POINT('Ctrl Pts',(-2.28396628040981E-16,32.7351420011818,
11.1000672611831));
#22573=CARTESIAN_POINT('Ctrl Pts',(-2.28396628040981E-16,33.045415593,10.5747121186603));
#22574=CARTESIAN_POINT('Ctrl Pts',(-2.28396628040981E-16,33.63686551036,
10.24));
#22575=CARTESIAN_POINT('Ctrl Pts',(-2.28396628040981E-16,34.2419663837872,
10.24));
#22576=CARTESIAN_POINT('Ctrl Pts',(3.73,32.7351420011818,11.1000672611831));
#22577=CARTESIAN_POINT('Ctrl Pts',(3.73,33.045415593,10.5747121186603));
#22578=CARTESIAN_POINT('Ctrl Pts',(3.73,33.63686551036,10.24));
#22579=CARTESIAN_POINT('Ctrl Pts',(3.73,34.2419663837872,10.24));
#22580=CARTESIAN_POINT('Ctrl Pts',(3.73,32.7351420011818,14.8300672611831));
#22581=CARTESIAN_POINT('Ctrl Pts',(3.73,33.045415593,14.3047121186603));
#22582=CARTESIAN_POINT('Ctrl Pts',(3.73,33.63686551036,13.97));
#22583=CARTESIAN_POINT('Ctrl Pts',(3.73,34.2419663837872,13.97));
#22584=CARTESIAN_POINT('Ctrl Pts',(0.,32.7351420011818,14.8300672611831));
#22585=CARTESIAN_POINT('Ctrl Pts',(0.,33.045415593,14.3047121186603));
#22586=CARTESIAN_POINT('Ctrl Pts',(0.,33.63686551036,13.97));
#22587=CARTESIAN_POINT('Ctrl Pts',(0.,34.2419663837872,13.97));
#22588=CARTESIAN_POINT('Origin',(0.,34.2419663837872,12.105));
#22589=CARTESIAN_POINT('Origin',(0.,34.2419663837872,12.105));
#22590=CARTESIAN_POINT('Origin',(0.,71.2419663837872,12.105));
#22591=CARTESIAN_POINT('Ctrl Pts',(0.,71.2419663837872,13.97));
#22592=CARTESIAN_POINT('Ctrl Pts',(0.,71.847073728999,13.97));
#22593=CARTESIAN_POINT('Ctrl Pts',(0.,72.4385298261441,14.3047192784616));
#22594=CARTESIAN_POINT('Ctrl Pts',(0.,72.7488007217793,14.8300841178694));
#22595=CARTESIAN_POINT('Ctrl Pts',(-3.73,71.2419663837872,13.97));
#22596=CARTESIAN_POINT('Ctrl Pts',(-3.73,71.847073728999,13.97));
#22597=CARTESIAN_POINT('Ctrl Pts',(-3.73,72.4385298261441,14.3047192784616));
#22598=CARTESIAN_POINT('Ctrl Pts',(-3.73,72.7488007217793,14.8300841178694));
#22599=CARTESIAN_POINT('Ctrl Pts',(-3.73,71.2419663837872,10.24));
#22600=CARTESIAN_POINT('Ctrl Pts',(-3.73,71.847073728999,10.24));
#22601=CARTESIAN_POINT('Ctrl Pts',(-3.73,72.4385298261441,10.5747192784616));
#22602=CARTESIAN_POINT('Ctrl Pts',(-3.73,72.7488007217793,11.1000841178694));
#22603=CARTESIAN_POINT('Ctrl Pts',(-2.28396628040981E-16,71.2419663837872,
10.24));
#22604=CARTESIAN_POINT('Ctrl Pts',(-2.28396628040981E-16,71.847073728999,
10.24));
#22605=CARTESIAN_POINT('Ctrl Pts',(-2.28396628040981E-16,72.4385298261441,
10.5747192784616));
#22606=CARTESIAN_POINT('Ctrl Pts',(-2.28396628040981E-16,72.7488007217793,
11.1000841178694));
#22607=CARTESIAN_POINT('Ctrl Pts',(3.73,71.2419663837872,10.24));
#22608=CARTESIAN_POINT('Ctrl Pts',(3.73,71.847073728999,10.24));
#22609=CARTESIAN_POINT('Ctrl Pts',(3.73,72.4385298261441,10.5747192784616));
#22610=CARTESIAN_POINT('Ctrl Pts',(3.73,72.7488007217793,11.1000841178694));
#22611=CARTESIAN_POINT('Ctrl Pts',(3.73,71.2419663837872,13.97));
#22612=CARTESIAN_POINT('Ctrl Pts',(3.73,71.847073728999,13.97));
#22613=CARTESIAN_POINT('Ctrl Pts',(3.73,72.4385298261441,14.3047192784616));
#22614=CARTESIAN_POINT('Ctrl Pts',(3.73,72.7488007217793,14.8300841178694));
#22615=CARTESIAN_POINT('Ctrl Pts',(0.,71.2419663837872,13.97));
#22616=CARTESIAN_POINT('Ctrl Pts',(0.,71.847073728999,13.97));
#22617=CARTESIAN_POINT('Ctrl Pts',(0.,72.4385298261441,14.3047192784616));
#22618=CARTESIAN_POINT('Ctrl Pts',(0.,72.7488007217793,14.8300841178694));
#22619=CARTESIAN_POINT('Ctrl Pts',(-8.71689482662896,32.7351420011818,11.9977764420206));
#22620=CARTESIAN_POINT('Ctrl Pts',(-8.40809882163708,33.045415593,11.5727552036367));
#22621=CARTESIAN_POINT('Ctrl Pts',(-8.21135997452595,33.63686551036,11.3019674114179));
#22622=CARTESIAN_POINT('Ctrl Pts',(-8.21135997452595,34.2419663837872,11.3019674114179));
#22623=CARTESIAN_POINT('Ctrl Pts',(-11.7345282156475,32.7351420011818,9.80533745096963));
#22624=CARTESIAN_POINT('Ctrl Pts',(-11.4257322106552,33.045415593,9.38031621258576));
#22625=CARTESIAN_POINT('Ctrl Pts',(-11.2289933635445,33.63686551036,9.10952842036699));
#22626=CARTESIAN_POINT('Ctrl Pts',(-11.2289933635445,34.2419663837872,9.10952842036699));
#22627=CARTESIAN_POINT('Ctrl Pts',(-9.54208922459654,32.7351420011818,6.7877040619511));
#22628=CARTESIAN_POINT('Ctrl Pts',(-9.23329321960506,33.045415593,6.36268282356722));
#22629=CARTESIAN_POINT('Ctrl Pts',(-9.03655437249353,33.63686551036,6.09189503134845));
#22630=CARTESIAN_POINT('Ctrl Pts',(-9.03655437249353,34.2419663837872,6.09189503134846));
#22631=CARTESIAN_POINT('Ctrl Pts',(-6.52445583557801,32.7351420011818,8.98014305300205));
#22632=CARTESIAN_POINT('Ctrl Pts',(-6.21565983058692,33.045415593,8.55512181461817));
#22633=CARTESIAN_POINT('Ctrl Pts',(-6.018920983475,33.63686551036,8.28433402239941));
#22634=CARTESIAN_POINT('Ctrl Pts',(-6.018920983475,34.2419663837872,8.28433402239941));
#22635=CARTESIAN_POINT('Ctrl Pts',(-3.50682244655947,32.7351420011818,11.172582044053));
#22636=CARTESIAN_POINT('Ctrl Pts',(-3.19802644156878,33.045415593,10.7475608056691));
#22637=CARTESIAN_POINT('Ctrl Pts',(-3.00128759445646,33.63686551036,10.4767730134504));
#22638=CARTESIAN_POINT('Ctrl Pts',(-3.00128759445646,34.2419663837872,10.4767730134504));
#22639=CARTESIAN_POINT('Ctrl Pts',(-5.69926143761042,32.7351420011818,14.1902154330715));
#22640=CARTESIAN_POINT('Ctrl Pts',(-5.39046543261894,33.045415593,13.7651941946877));
#22641=CARTESIAN_POINT('Ctrl Pts',(-5.19372658550741,33.63686551036,13.4944064024689));
#22642=CARTESIAN_POINT('Ctrl Pts',(-5.19372658550741,34.2419663837872,13.4944064024689));
#22643=CARTESIAN_POINT('Ctrl Pts',(-8.71689482662896,32.7351420011818,11.9977764420206));
#22644=CARTESIAN_POINT('Ctrl Pts',(-8.40809882163708,33.045415593,11.5727552036367));
#22645=CARTESIAN_POINT('Ctrl Pts',(-8.21135997452595,33.63686551036,11.3019674114179));
#22646=CARTESIAN_POINT('Ctrl Pts',(-8.21135997452595,34.2419663837872,11.3019674114179));
#22647=CARTESIAN_POINT('Origin',(-7.11514047900047,34.2419663837872,9.79315071690868));
#22648=CARTESIAN_POINT('Origin',(-7.11514047900047,34.2419663837872,9.79315071690868));
#22649=CARTESIAN_POINT('Origin',(-7.11514047900048,71.2419663837872,9.79315071690868));
#22650=CARTESIAN_POINT('Ctrl Pts',(-8.21135997452595,71.2419663837872,11.3019674114179));
#22651=CARTESIAN_POINT('Ctrl Pts',(-8.21135997452595,71.847073728999,11.3019674114179));
#22652=CARTESIAN_POINT('Ctrl Pts',(-8.40810303006371,72.4385298261441,11.5727609960379));
#22653=CARTESIAN_POINT('Ctrl Pts',(-8.71690473474057,72.7488007217793,11.9977900793663));
#22654=CARTESIAN_POINT('Ctrl Pts',(-11.2289933635445,71.2419663837872,9.10952842036699));
#22655=CARTESIAN_POINT('Ctrl Pts',(-11.2289933635445,71.847073728999,9.10952842036699));
#22656=CARTESIAN_POINT('Ctrl Pts',(-11.4257364190824,72.4385298261441,9.38032200498695));
#22657=CARTESIAN_POINT('Ctrl Pts',(-11.7345381237591,72.7488007217793,9.80535108831532));
#22658=CARTESIAN_POINT('Ctrl Pts',(-9.03655437249354,71.2419663837872,6.09189503134846));
#22659=CARTESIAN_POINT('Ctrl Pts',(-9.03655437249354,71.847073728999,6.09189503134846));
#22660=CARTESIAN_POINT('Ctrl Pts',(-9.23329742803116,72.4385298261441,6.36268861596841));
#22661=CARTESIAN_POINT('Ctrl Pts',(-9.54209913270815,72.7488007217793,6.78771769929678));
#22662=CARTESIAN_POINT('Ctrl Pts',(-6.018920983475,71.2419663837872,8.28433402239941));
#22663=CARTESIAN_POINT('Ctrl Pts',(-6.018920983475,71.847073728999,8.28433402239941));
#22664=CARTESIAN_POINT('Ctrl Pts',(-6.2156640390125,72.4385298261441,8.55512760701937));
#22665=CARTESIAN_POINT('Ctrl Pts',(-6.52446574368962,72.7488007217793,8.98015669034773));
#22666=CARTESIAN_POINT('Ctrl Pts',(-3.00128759445646,71.2419663837872,10.4767730134504));
#22667=CARTESIAN_POINT('Ctrl Pts',(-3.00128759445646,71.847073728999,10.4767730134504));
#22668=CARTESIAN_POINT('Ctrl Pts',(-3.19803064999383,72.4385298261441,10.7475665980703));
#22669=CARTESIAN_POINT('Ctrl Pts',(-3.50683235467108,72.7488007217793,11.1725956813987));
#22670=CARTESIAN_POINT('Ctrl Pts',(-5.19372658550742,71.2419663837872,13.4944064024689));
#22671=CARTESIAN_POINT('Ctrl Pts',(-5.19372658550742,71.847073728999,13.4944064024689));
#22672=CARTESIAN_POINT('Ctrl Pts',(-5.39046964104504,72.4385298261441,13.7651999870889));
#22673=CARTESIAN_POINT('Ctrl Pts',(-5.69927134572203,72.7488007217793,14.1902290704172));
#22674=CARTESIAN_POINT('Ctrl Pts',(-8.21135997452595,71.2419663837872,11.3019674114179));
#22675=CARTESIAN_POINT('Ctrl Pts',(-8.21135997452595,71.847073728999,11.3019674114179));
#22676=CARTESIAN_POINT('Ctrl Pts',(-8.40810303006371,72.4385298261441,11.5727609960379));
#22677=CARTESIAN_POINT('Ctrl Pts',(-8.71690473474057,72.7488007217793,11.9977900793663));
#22678=CARTESIAN_POINT('Ctrl Pts',(-14.1042321058437,32.7351420011818,4.58274281142898));
#22679=CARTESIAN_POINT('Ctrl Pts',(-13.6045896741761,33.045415593,4.42039914430651));
#22680=CARTESIAN_POINT('Ctrl Pts',(-13.2862595326433,33.63686551036,4.31696741141789));
#22681=CARTESIAN_POINT('Ctrl Pts',(-13.2862595326433,34.2419663837872,4.31696741141789));
#22682=CARTESIAN_POINT('Ctrl Pts',(-15.2568654948622,32.7351420011818,1.03530200564804));
#22683=CARTESIAN_POINT('Ctrl Pts',(-14.7572230631946,33.045415593,0.872958338525508));
#22684=CARTESIAN_POINT('Ctrl Pts',(-14.4388929216619,33.63686551036,0.769526605636954));
#22685=CARTESIAN_POINT('Ctrl Pts',(-14.4388929216619,34.2419663837872,0.769526605636955));
#22686=CARTESIAN_POINT('Ctrl Pts',(-11.7094246890812,32.7351420011818,-0.117331383370479));
#22687=CARTESIAN_POINT('Ctrl Pts',(-11.2097822574136,33.045415593,-0.27967505049288));
#22688=CARTESIAN_POINT('Ctrl Pts',(-10.8914521158809,33.63686551036,-0.383106783381566));
#22689=CARTESIAN_POINT('Ctrl Pts',(-10.8914521158809,34.2419663837872,-0.383106783381565));
#22690=CARTESIAN_POINT('Ctrl Pts',(-10.5567913000627,32.7351420011818,3.43010942241045));
#22691=CARTESIAN_POINT('Ctrl Pts',(-10.0571488683951,33.045415593,3.26776575528812));
#22692=CARTESIAN_POINT('Ctrl Pts',(-9.7388187268624,33.63686551036,3.16433402239937));
#22693=CARTESIAN_POINT('Ctrl Pts',(-9.7388187268624,34.2419663837872,3.16433402239937));
#22694=CARTESIAN_POINT('Ctrl Pts',(-9.4041579110442,32.7351420011818,6.97755022819139));
#22695=CARTESIAN_POINT('Ctrl Pts',(-8.9045154793766,33.045415593,6.81520656106912));
#22696=CARTESIAN_POINT('Ctrl Pts',(-8.58618533784388,33.63686551036,6.7117748281803));
#22697=CARTESIAN_POINT('Ctrl Pts',(-8.58618533784388,34.2419663837872,6.7117748281803));
#22698=CARTESIAN_POINT('Ctrl Pts',(-12.9515987168251,32.7351420011818,8.13018361720991));
#22699=CARTESIAN_POINT('Ctrl Pts',(-12.4519562851575,33.045415593,7.96783995008751));
#22700=CARTESIAN_POINT('Ctrl Pts',(-12.1336261436248,33.63686551036,7.86440821719883));
#22701=CARTESIAN_POINT('Ctrl Pts',(-12.1336261436248,34.2419663837872,7.86440821719883));
#22702=CARTESIAN_POINT('Ctrl Pts',(-14.1042321058437,32.7351420011818,4.58274281142898));
#22703=CARTESIAN_POINT('Ctrl Pts',(-13.6045896741761,33.045415593,4.42039914430651));
#22704=CARTESIAN_POINT('Ctrl Pts',(-13.2862595326433,33.63686551036,4.31696741141789));
#22705=CARTESIAN_POINT('Ctrl Pts',(-13.2862595326433,34.2419663837872,4.31696741141789));
#22706=CARTESIAN_POINT('Origin',(-11.5125391297529,34.2419663837872,3.74065071690863));
#22707=CARTESIAN_POINT('Origin',(-11.5125391297529,34.2419663837872,3.74065071690863));
#22708=CARTESIAN_POINT('Origin',(-11.5125391297529,71.2419663837872,3.74065071690863));
#22709=CARTESIAN_POINT('Ctrl Pts',(-13.2862595326433,71.2419663837872,4.31696741141789));
#22710=CARTESIAN_POINT('Ctrl Pts',(-13.2862595326433,71.847073728999,4.31696741141789));
#22711=CARTESIAN_POINT('Ctrl Pts',(-13.6045964835519,72.4385298261441,4.42040135680733));
#22712=CARTESIAN_POINT('Ctrl Pts',(-14.104248137505,72.7488007217793,4.58274802043151));
#22713=CARTESIAN_POINT('Ctrl Pts',(-14.4388929216619,71.2419663837872,0.769526605636955));
#22714=CARTESIAN_POINT('Ctrl Pts',(-14.4388929216619,71.847073728999,0.769526605636955));
#22715=CARTESIAN_POINT('Ctrl Pts',(-14.7572298725705,72.4385298261441,0.872960551026527));
#22716=CARTESIAN_POINT('Ctrl Pts',(-15.2568815265235,72.7488007217793,1.03530721465058));
#22717=CARTESIAN_POINT('Ctrl Pts',(-10.8914521158809,71.2419663837872,-0.383106783381565));
#22718=CARTESIAN_POINT('Ctrl Pts',(-10.8914521158809,71.847073728999,-0.383106783381565));
#22719=CARTESIAN_POINT('Ctrl Pts',(-11.2097890667895,72.4385298261441,-0.279672837992126));
#22720=CARTESIAN_POINT('Ctrl Pts',(-11.7094407207426,72.7488007217793,-0.117326174367942));
#22721=CARTESIAN_POINT('Ctrl Pts',(-9.7388187268624,71.2419663837872,3.16433402239937));
#22722=CARTESIAN_POINT('Ctrl Pts',(-9.7388187268624,71.847073728999,3.16433402239937));
#22723=CARTESIAN_POINT('Ctrl Pts',(-10.057155677771,72.4385298261441,3.26776796778881));
#22724=CARTESIAN_POINT('Ctrl Pts',(-10.5568073317241,72.7488007217793,3.43011463141299));
#22725=CARTESIAN_POINT('Ctrl Pts',(-8.58618533784388,71.2419663837872,6.7117748281803));
#22726=CARTESIAN_POINT('Ctrl Pts',(-8.58618533784388,71.847073728999,6.7117748281803));
#22727=CARTESIAN_POINT('Ctrl Pts',(-8.90452228875249,72.4385298261441,6.81520877356975));
#22728=CARTESIAN_POINT('Ctrl Pts',(-9.40417394270555,72.7488007217793,6.97755543719393));
#22729=CARTESIAN_POINT('Ctrl Pts',(-12.1336261436248,71.2419663837872,7.86440821719883));
#22730=CARTESIAN_POINT('Ctrl Pts',(-12.1336261436248,71.847073728999,7.86440821719883));
#22731=CARTESIAN_POINT('Ctrl Pts',(-12.4519630945334,72.4385298261441,7.96784216258813));
#22732=CARTESIAN_POINT('Ctrl Pts',(-12.9516147484865,72.7488007217793,8.13018882621245));
#22733=CARTESIAN_POINT('Ctrl Pts',(-13.2862595326433,71.2419663837872,4.31696741141789));
#22734=CARTESIAN_POINT('Ctrl Pts',(-13.2862595326433,71.847073728999,4.31696741141789));
#22735=CARTESIAN_POINT('Ctrl Pts',(-13.6045964835519,72.4385298261441,4.42040135680733));
#22736=CARTESIAN_POINT('Ctrl Pts',(-14.104248137505,72.7488007217793,4.58274802043151));
#22737=CARTESIAN_POINT('Ctrl Pts',(-14.1042321058436,32.7351420011818,-4.58274281142927));
#22738=CARTESIAN_POINT('Ctrl Pts',(-13.604589674176,33.045415593,-4.42039914430733));
#22739=CARTESIAN_POINT('Ctrl Pts',(-13.2862595326432,33.63686551036,-4.31696741141817));
#22740=CARTESIAN_POINT('Ctrl Pts',(-13.2862595326432,34.2419663837872,-4.31696741141817));
#22741=CARTESIAN_POINT('Ctrl Pts',(-12.951598716825,32.7351420011818,-8.13018361721019));
#22742=CARTESIAN_POINT('Ctrl Pts',(-12.4519562851574,33.045415593,-7.96783995008897));
#22743=CARTESIAN_POINT('Ctrl Pts',(-12.1336261436246,33.63686551036,-7.86440821719908));
#22744=CARTESIAN_POINT('Ctrl Pts',(-12.1336261436247,34.2419663837872,-7.86440821719908));
#22745=CARTESIAN_POINT('Ctrl Pts',(-9.40415791104406,32.7351420011818,-6.97755022819159));
#22746=CARTESIAN_POINT('Ctrl Pts',(-8.90451547937646,33.045415593,-6.81520656107025));
#22747=CARTESIAN_POINT('Ctrl Pts',(-8.58618533784374,33.63686551036,-6.71177482818048));
#22748=CARTESIAN_POINT('Ctrl Pts',(-8.58618533784374,34.2419663837872,-6.71177482818048));
#22749=CARTESIAN_POINT('Ctrl Pts',(-10.5567913000627,32.7351420011818,-3.43010942241068));
#22750=CARTESIAN_POINT('Ctrl Pts',(-10.0571488683951,33.045415593,-3.26776575528914));
#22751=CARTESIAN_POINT('Ctrl Pts',(-9.73881872686233,33.63686551036,-3.16433402239957));
#22752=CARTESIAN_POINT('Ctrl Pts',(-9.73881872686234,34.2419663837872,-3.16433402239957));
#22753=CARTESIAN_POINT('Ctrl Pts',(-11.7094246890813,32.7351420011818,0.117331383370231));
#22754=CARTESIAN_POINT('Ctrl Pts',(-11.2097822574137,33.045415593,0.279675050491972));
#22755=CARTESIAN_POINT('Ctrl Pts',(-10.8914521158809,33.63686551036,0.383106783381337));
#22756=CARTESIAN_POINT('Ctrl Pts',(-10.8914521158809,34.2419663837872,0.383106783381337));
#22757=CARTESIAN_POINT('Ctrl Pts',(-15.2568654948622,32.7351420011818,-1.03530200564836));
#22758=CARTESIAN_POINT('Ctrl Pts',(-14.7572230631946,33.045415593,-0.872958338525696));
#22759=CARTESIAN_POINT('Ctrl Pts',(-14.4388929216618,33.63686551036,-0.769526605637257));
#22760=CARTESIAN_POINT('Ctrl Pts',(-14.4388929216618,34.2419663837872,-0.769526605637258));
#22761=CARTESIAN_POINT('Ctrl Pts',(-14.1042321058436,32.7351420011818,-4.58274281142927));
#22762=CARTESIAN_POINT('Ctrl Pts',(-13.604589674176,33.045415593,-4.42039914430733));
#22763=CARTESIAN_POINT('Ctrl Pts',(-13.2862595326432,33.63686551036,-4.31696741141817));
#22764=CARTESIAN_POINT('Ctrl Pts',(-13.2862595326432,34.2419663837872,-4.31696741141817));
#22765=CARTESIAN_POINT('Origin',(-11.5125391297528,34.2419663837872,-3.74065071690887));
#22766=CARTESIAN_POINT('Origin',(-11.5125391297528,34.2419663837872,-3.74065071690887));
#22767=CARTESIAN_POINT('Origin',(-11.5125391297528,71.2419663837872,-3.74065071690887));
#22768=CARTESIAN_POINT('Ctrl Pts',(-13.2862595326432,71.2419663837872,-4.31696741141817));
#22769=CARTESIAN_POINT('Ctrl Pts',(-13.2862595326432,71.847073728999,-4.31696741141817));
#22770=CARTESIAN_POINT('Ctrl Pts',(-13.6045964835518,72.4385298261441,-4.42040135680736));
#22771=CARTESIAN_POINT('Ctrl Pts',(-14.1042481375049,72.7488007217793,-4.5827480204318));
#22772=CARTESIAN_POINT('Ctrl Pts',(-12.1336261436247,71.2419663837872,-7.86440821719908));
#22773=CARTESIAN_POINT('Ctrl Pts',(-12.1336261436247,71.847073728999,-7.86440821719908));
#22774=CARTESIAN_POINT('Ctrl Pts',(-12.4519630945332,72.4385298261441,-7.96784216258827));
#22775=CARTESIAN_POINT('Ctrl Pts',(-12.9516147484863,72.7488007217793,-8.13018882621271));
#22776=CARTESIAN_POINT('Ctrl Pts',(-8.58618533784374,71.2419663837872,-6.71177482818048));
#22777=CARTESIAN_POINT('Ctrl Pts',(-8.58618533784374,71.847073728999,-6.71177482818048));
#22778=CARTESIAN_POINT('Ctrl Pts',(-8.90452228875233,72.4385298261441,-6.81520877356967));
#22779=CARTESIAN_POINT('Ctrl Pts',(-9.40417394270539,72.7488007217793,-6.97755543719412));
#22780=CARTESIAN_POINT('Ctrl Pts',(-9.73881872686234,71.2419663837872,-3.16433402239957));
#22781=CARTESIAN_POINT('Ctrl Pts',(-9.73881872686234,71.847073728999,-3.16433402239957));
#22782=CARTESIAN_POINT('Ctrl Pts',(-10.0571556777709,72.4385298261441,-3.26776796778876));
#22783=CARTESIAN_POINT('Ctrl Pts',(-10.556807331724,72.7488007217793,-3.43011463141321));
#22784=CARTESIAN_POINT('Ctrl Pts',(-10.8914521158809,71.2419663837872,0.383106783381337));
#22785=CARTESIAN_POINT('Ctrl Pts',(-10.8914521158809,71.847073728999,0.383106783381337));
#22786=CARTESIAN_POINT('Ctrl Pts',(-11.2097890667895,72.4385298261441,0.279672837992146));
#22787=CARTESIAN_POINT('Ctrl Pts',(-11.7094407207426,72.7488007217793,0.117326174367701));
#22788=CARTESIAN_POINT('Ctrl Pts',(-14.4388929216618,71.2419663837872,-0.769526605637258));
#22789=CARTESIAN_POINT('Ctrl Pts',(-14.4388929216618,71.847073728999,-0.769526605637258));
#22790=CARTESIAN_POINT('Ctrl Pts',(-14.7572298725704,72.4385298261441,-0.872960551026448));
#22791=CARTESIAN_POINT('Ctrl Pts',(-15.2568815265235,72.7488007217793,-1.03530721465089));
#22792=CARTESIAN_POINT('Ctrl Pts',(-13.2862595326432,71.2419663837872,-4.31696741141817));
#22793=CARTESIAN_POINT('Ctrl Pts',(-13.2862595326432,71.847073728999,-4.31696741141817));
#22794=CARTESIAN_POINT('Ctrl Pts',(-13.6045964835518,72.4385298261441,-4.42040135680736));
#22795=CARTESIAN_POINT('Ctrl Pts',(-14.1042481375049,72.7488007217793,-4.5827480204318));
#22796=CARTESIAN_POINT('Ctrl Pts',(-8.71689482662869,32.7351420011818,-11.9977764420208));
#22797=CARTESIAN_POINT('Ctrl Pts',(-8.40809882163841,33.045415593,-11.5727552036369));
#22798=CARTESIAN_POINT('Ctrl Pts',(-8.2113599745257,33.63686551036,-11.3019674114181));
#22799=CARTESIAN_POINT('Ctrl Pts',(-8.2113599745257,34.2419663837872,-11.3019674114181));
#22800=CARTESIAN_POINT('Ctrl Pts',(-5.69926143761011,32.7351420011818,-14.1902154330717));
#22801=CARTESIAN_POINT('Ctrl Pts',(-5.39046543262022,33.045415593,-13.7651941946878));
#22802=CARTESIAN_POINT('Ctrl Pts',(-5.19372658550712,33.63686551036,-13.494406402469));
#22803=CARTESIAN_POINT('Ctrl Pts',(-5.19372658550712,34.2419663837872,-13.494406402469));
#22804=CARTESIAN_POINT('Ctrl Pts',(-3.50682244655923,32.7351420011818,-11.1725820440531));
#22805=CARTESIAN_POINT('Ctrl Pts',(-3.19802644156854,33.045415593,-10.7475608056692));
#22806=CARTESIAN_POINT('Ctrl Pts',(-3.00128759445623,33.63686551036,-10.4767730134504));
#22807=CARTESIAN_POINT('Ctrl Pts',(-3.00128759445624,34.2419663837872,-10.4767730134504));
#22808=CARTESIAN_POINT('Ctrl Pts',(-6.52445583557781,32.7351420011818,-8.98014305300219));
#22809=CARTESIAN_POINT('Ctrl Pts',(-6.21565983058673,33.045415593,-8.55512181461832));
#22810=CARTESIAN_POINT('Ctrl Pts',(-6.01892098347482,33.63686551036,-8.28433402239954));
#22811=CARTESIAN_POINT('Ctrl Pts',(-6.01892098347482,34.2419663837872,-8.28433402239954));
#22812=CARTESIAN_POINT('Ctrl Pts',(-9.54208922459639,32.7351420011818,-6.78770406195131));
#22813=CARTESIAN_POINT('Ctrl Pts',(-9.23329321960491,33.045415593,-6.36268282356744));
#22814=CARTESIAN_POINT('Ctrl Pts',(-9.0365543724934,33.63686551036,-6.09189503134865));
#22815=CARTESIAN_POINT('Ctrl Pts',(-9.0365543724934,34.2419663837872,-6.09189503134866));
#22816=CARTESIAN_POINT('Ctrl Pts',(-11.7345282156473,32.7351420011818,-9.80533745096989));
#22817=CARTESIAN_POINT('Ctrl Pts',(-11.4257322106566,33.045415593,-9.38031621258602));
#22818=CARTESIAN_POINT('Ctrl Pts',(-11.2289933635443,33.63686551036,-9.10952842036724));
#22819=CARTESIAN_POINT('Ctrl Pts',(-11.2289933635443,34.2419663837872,-9.10952842036724));
#22820=CARTESIAN_POINT('Ctrl Pts',(-8.71689482662869,32.7351420011818,-11.9977764420208));
#22821=CARTESIAN_POINT('Ctrl Pts',(-8.40809882163841,33.045415593,-11.5727552036369));
#22822=CARTESIAN_POINT('Ctrl Pts',(-8.2113599745257,33.63686551036,-11.3019674114181));
#22823=CARTESIAN_POINT('Ctrl Pts',(-8.2113599745257,34.2419663837872,-11.3019674114181));
#22824=CARTESIAN_POINT('Origin',(-7.11514047900026,34.2419663837872,-9.79315071690883));
#22825=CARTESIAN_POINT('Origin',(-7.11514047900026,34.2419663837872,-9.79315071690883));
#22826=CARTESIAN_POINT('Origin',(-7.11514047900026,71.2419663837872,-9.79315071690883));
#22827=CARTESIAN_POINT('Ctrl Pts',(-8.2113599745257,71.2419663837872,-11.3019674114181));
#22828=CARTESIAN_POINT('Ctrl Pts',(-8.2113599745257,71.847073728999,-11.3019674114181));
#22829=CARTESIAN_POINT('Ctrl Pts',(-8.40810303006345,72.4385298261441,-11.5727609960386));
#22830=CARTESIAN_POINT('Ctrl Pts',(-8.71690473474031,72.7488007217793,-11.9977900793665));
#22831=CARTESIAN_POINT('Ctrl Pts',(-5.19372658550712,71.2419663837872,-13.494406402469));
#22832=CARTESIAN_POINT('Ctrl Pts',(-5.19372658550712,71.847073728999,-13.494406402469));
#22833=CARTESIAN_POINT('Ctrl Pts',(-5.390469641045,72.4385298261441,-13.7651999870895));
#22834=CARTESIAN_POINT('Ctrl Pts',(-5.69927134572172,72.7488007217793,-14.1902290704173));
#22835=CARTESIAN_POINT('Ctrl Pts',(-3.00128759445624,71.2419663837872,-10.4767730134504));
#22836=CARTESIAN_POINT('Ctrl Pts',(-3.00128759445624,71.847073728999,-10.4767730134504));
#22837=CARTESIAN_POINT('Ctrl Pts',(-3.19803064999385,72.4385298261441,-10.7475665980709));
#22838=CARTESIAN_POINT('Ctrl Pts',(-3.50683235467084,72.7488007217793,-11.1725956813988));
#22839=CARTESIAN_POINT('Ctrl Pts',(-6.01892098347482,71.2419663837872,-8.28433402239954));
#22840=CARTESIAN_POINT('Ctrl Pts',(-6.01892098347482,71.847073728999,-8.28433402239954));
#22841=CARTESIAN_POINT('Ctrl Pts',(-6.2156640390123,72.4385298261441,-8.55512760702004));
#22842=CARTESIAN_POINT('Ctrl Pts',(-6.52446574368942,72.7488007217793,-8.98015669034787));
#22843=CARTESIAN_POINT('Ctrl Pts',(-9.0365543724934,71.2419663837872,-6.09189503134866));
#22844=CARTESIAN_POINT('Ctrl Pts',(-9.0365543724934,71.847073728999,-6.09189503134866));
#22845=CARTESIAN_POINT('Ctrl Pts',(-9.23329742803075,72.4385298261441,-6.36268861596915));
#22846=CARTESIAN_POINT('Ctrl Pts',(-9.542099132708,72.7488007217793,-6.78771769929699));
#22847=CARTESIAN_POINT('Ctrl Pts',(-11.2289933635443,71.2419663837872,-9.10952842036724));
#22848=CARTESIAN_POINT('Ctrl Pts',(-11.2289933635443,71.847073728999,-9.10952842036724));
#22849=CARTESIAN_POINT('Ctrl Pts',(-11.4257364190819,72.4385298261441,-9.38032200498773));
#22850=CARTESIAN_POINT('Ctrl Pts',(-11.7345381237589,72.7488007217793,-9.80535108831557));
#22851=CARTESIAN_POINT('Ctrl Pts',(-8.2113599745257,71.2419663837872,-11.3019674114181));
#22852=CARTESIAN_POINT('Ctrl Pts',(-8.2113599745257,71.847073728999,-11.3019674114181));
#22853=CARTESIAN_POINT('Ctrl Pts',(-8.40810303006345,72.4385298261441,-11.5727609960386));
#22854=CARTESIAN_POINT('Ctrl Pts',(-8.71690473474031,72.7488007217793,-11.9977900793665));
#22855=CARTESIAN_POINT('Ctrl Pts',(2.4156304102994,5.,10.8339636164256));
#22856=CARTESIAN_POINT('Ctrl Pts',(2.41563040646342,4.96191046202733,10.8339636166853));
#22857=CARTESIAN_POINT('Ctrl Pts',(2.4146547402783,4.92371376427368,10.8341812987099));
#22858=CARTESIAN_POINT('Ctrl Pts',(2.41072929832241,4.84720274160474,10.8350554324849));
#22859=CARTESIAN_POINT('Ctrl Pts',(2.40775787877141,4.80871695881661,10.8357166882541));
#22860=CARTESIAN_POINT('Ctrl Pts',(2.39988157827119,4.73242631317627,10.8374638426754));
#22861=CARTESIAN_POINT('Ctrl Pts',(2.39497737791963,4.6945034108209,10.8385495849069));
#22862=CARTESIAN_POINT('Ctrl Pts',(2.38327169996162,4.61914358580643,10.8411295401524));
#22863=CARTESIAN_POINT('Ctrl Pts',(2.37647039420389,4.58169825793974,10.8426237055241));
#22864=CARTESIAN_POINT('Ctrl Pts',(2.35325442553652,4.47005693394489,10.847694801622));
#22865=CARTESIAN_POINT('Ctrl Pts',(2.3340338175079,4.39655416040346,10.8518604682163));
#22866=CARTESIAN_POINT('Ctrl Pts',(2.29959460874979,4.28768080804602,10.8591914690199));
#22867=CARTESIAN_POINT('Ctrl Pts',(2.28717862543041,4.25162018871417,10.8618155803769));
#22868=CARTESIAN_POINT('Ctrl Pts',(2.26045417586942,4.17996386393482,10.8674086381803));
#22869=CARTESIAN_POINT('Ctrl Pts',(2.24614896131211,4.14437664773035,10.8703769337531));
#22870=CARTESIAN_POINT('Ctrl Pts',(2.22323683546441,4.09132438210188,10.8750777516754));
#22871=CARTESIAN_POINT('Ctrl Pts',(2.21535159730481,4.07368696613903,10.876687111824));
#22872=CARTESIAN_POINT('Ctrl Pts',(2.19918231004094,4.03871821508943,10.8799679279219));
#22873=CARTESIAN_POINT('Ctrl Pts',(2.19088543945954,4.0213559005185,10.881642029533));
#22874=CARTESIAN_POINT('Ctrl Pts',(2.1653921502188,3.96969451639992,10.8867540523146));
#22875=CARTESIAN_POINT('Ctrl Pts',(2.14756476939503,3.93575377943081,10.8902875627326));
#22876=CARTESIAN_POINT('Ctrl Pts',(2.09168081411357,3.83552515343858,10.9012085469626));
#22877=CARTESIAN_POINT('Ctrl Pts',(2.05118520112225,3.77072933843846,10.9089252412181));
#22878=CARTESIAN_POINT('Ctrl Pts',(1.9856514830744,3.67657009081119,10.9209760193803));
#22879=CARTESIAN_POINT('Ctrl Pts',(1.96300593858833,3.64568758622464,10.9250725911264));
#22880=CARTESIAN_POINT('Ctrl Pts',(1.91610256695852,3.58493352527622,10.9333962768342));
#22881=CARTESIAN_POINT('Ctrl Pts',(1.8918447870784,3.55506189924222,10.9376234277111));
#22882=CARTESIAN_POINT('Ctrl Pts',(1.84169472079833,3.49634022773492,10.9461793901794));
#22883=CARTESIAN_POINT('Ctrl Pts',(1.81579980814473,3.46748730973486,10.950508647301));
#22884=CARTESIAN_POINT('Ctrl Pts',(1.762350359702,3.41083271569288,10.9592376624932));
#22885=CARTESIAN_POINT('Ctrl Pts',(1.7350155020693,3.38326334323313,10.9636014218412));
#22886=CARTESIAN_POINT('Ctrl Pts',(1.67913447380159,3.3295910796627,10.9722988530446));
#22887=CARTESIAN_POINT('Ctrl Pts',(1.65059069640107,3.30349081702451,10.976632138154));
#22888=CARTESIAN_POINT('Ctrl Pts',(1.59231052652113,3.25274008369802,10.9852378081031));
#22889=CARTESIAN_POINT('Ctrl Pts',(1.56257408110084,3.22808968398168,10.9895102305428));
#22890=CARTESIAN_POINT('Ctrl Pts',(1.47158319578018,3.15629691321311,11.0021919668541));
#22891=CARTESIAN_POINT('Ctrl Pts',(1.4085487056756,3.11130657146225,11.0104663920413));
#22892=CARTESIAN_POINT('Ctrl Pts',(1.31039752202577,3.04816755746305,11.0224307105556));
#22893=CARTESIAN_POINT('Ctrl Pts',(1.27707162401967,3.02784269906396,11.026345142236));
#22894=CARTESIAN_POINT('Ctrl Pts',(1.20921161545083,2.98867493489448,11.0339932853651));
#22895=CARTESIAN_POINT('Ctrl Pts',(1.17462206754654,2.96980348548508,11.0377327364982));
#22896=CARTESIAN_POINT('Ctrl Pts',(1.10437191556843,2.93366312106671,11.0449827080004));
#22897=CARTESIAN_POINT('Ctrl Pts',(1.06896163113932,2.91651856790947,11.0484679583694));
#22898=CARTESIAN_POINT('Ctrl Pts',(0.99745210450957,2.8839794871732,11.0551532019847));
#22899=CARTESIAN_POINT('Ctrl Pts',(0.961374437599674,2.86859606260606,11.0583509995041));
#22900=CARTESIAN_POINT('Ctrl Pts',(0.852182302673737,2.82507151370299,11.0674818389069));
#22901=CARTESIAN_POINT('Ctrl Pts',(0.778110692064935,2.79955051761125,11.072952549289));
#22902=CARTESIAN_POINT('Ctrl Pts',(0.627408873998724,2.75548409895438,11.0825128433466));
#22903=CARTESIAN_POINT('Ctrl Pts',(0.550764519707227,2.73694017621321,11.0866023912725));
#22904=CARTESIAN_POINT('Ctrl Pts',(0.453346626462258,2.71823575173535,11.0907572215327));
#22905=CARTESIAN_POINT('Ctrl Pts',(0.433768364290407,2.71471972381952,11.091540182064));
#22906=CARTESIAN_POINT('Ctrl Pts',(0.394471422995838,2.70814371620271,11.0930073608194));
#22907=CARTESIAN_POINT('Ctrl Pts',(0.374709949322281,2.70507888898263,11.0936926629967));
#22908=CARTESIAN_POINT('Ctrl Pts',(0.315428279537668,2.69661093714137,11.0955891856498));
#22909=CARTESIAN_POINT('Ctrl Pts',(0.275950761088858,2.69193338400005,11.0966410913946));
#22910=CARTESIAN_POINT('Ctrl Pts',(0.196982185499563,2.68446381383399,11.0983237617));
#22911=CARTESIAN_POINT('Ctrl Pts',(0.15750785306126,2.6816738708479,11.0989540709247));
#22912=CARTESIAN_POINT('Ctrl Pts',(0.0785788629130702,2.67796041583801,
11.0997934908188));
#22913=CARTESIAN_POINT('Ctrl Pts',(0.0391242055410394,2.67703693714379,
11.1000026010139));
#22914=CARTESIAN_POINT('Ctrl Pts',(-0.0397655306445661,2.67704700686668,
11.1000003220684));
#22915=CARTESIAN_POINT('Ctrl Pts',(-0.0792006094009493,2.67798056075966,
11.0997889324828));
#22916=CARTESIAN_POINT('Ctrl Pts',(-0.158051149433861,2.68170867442521,
11.0989462083064));
#22917=CARTESIAN_POINT('Ctrl Pts',(-0.197466610929021,2.68450321228798,
11.0983148732779));
#22918=CARTESIAN_POINT('Ctrl Pts',(-0.276277740964502,2.691970802071,11.0966326754737));
#22919=CARTESIAN_POINT('Ctrl Pts',(-0.315692244683293,2.6966476678611,11.0955809556022));
#22920=CARTESIAN_POINT('Ctrl Pts',(-0.394425801998236,2.70789613574509,
11.0930617027531));
#22921=CARTESIAN_POINT('Ctrl Pts',(-0.433929268879025,2.71450588894859,
11.0915857051179));
#22922=CARTESIAN_POINT('Ctrl Pts',(-0.512099892385214,2.72951817727644,
11.088251080714));
#22923=CARTESIAN_POINT('Ctrl Pts',(-0.550844005958438,2.73792358666081,
11.0863917748127));
#22924=CARTESIAN_POINT('Ctrl Pts',(-0.627648551372376,2.75650099223247,
11.0823088358929));
#22925=CARTESIAN_POINT('Ctrl Pts',(-0.665711553652418,2.76667258968464,
11.0800852864604));
#22926=CARTESIAN_POINT('Ctrl Pts',(-0.778896822997667,2.79980374463825,
11.0728980009129));
#22927=CARTESIAN_POINT('Ctrl Pts',(-0.853017446172679,2.82537397001114,
11.0674174899872));
#22928=CARTESIAN_POINT('Ctrl Pts',(-0.962206209010363,2.86894308941064,
11.0582786539946));
#22929=CARTESIAN_POINT('Ctrl Pts',(-0.998269898716162,2.88433653123043,
11.0550793011122));
#22930=CARTESIAN_POINT('Ctrl Pts',(-1.06972690046675,2.91688220503822,11.0483938054367));
#22931=CARTESIAN_POINT('Ctrl Pts',(-1.10511644984475,2.93403302039874,11.0449079354868));
#22932=CARTESIAN_POINT('Ctrl Pts',(-1.15770183492388,2.96110559714924,11.0394778777837));
#22933=CARTESIAN_POINT('Ctrl Pts',(-1.17516443843644,2.97036515149108,11.0376322386051));
#22934=CARTESIAN_POINT('Ctrl Pts',(-1.2097533438837,2.98924572661077,11.0338947272429));
#22935=CARTESIAN_POINT('Ctrl Pts',(-1.22689739274055,2.99887498930594,11.0320011655461));
#22936=CARTESIAN_POINT('Ctrl Pts',(-1.27783270600622,3.02829829309359,11.0262569913433));
#22937=CARTESIAN_POINT('Ctrl Pts',(-1.31119618898078,3.04866234676234,11.0223358849783));
#22938=CARTESIAN_POINT('Ctrl Pts',(-1.40939028702048,3.11188658794701,11.0103586558181));
#22939=CARTESIAN_POINT('Ctrl Pts',(-1.47245317748874,3.15693830849233,11.0020755577165));
#22940=CARTESIAN_POINT('Ctrl Pts',(-1.56344017683738,3.22879604108859,10.9893870450015));
#22941=CARTESIAN_POINT('Ctrl Pts',(-1.59317047816761,3.25346508699623,10.9851130961949));
#22942=CARTESIAN_POINT('Ctrl Pts',(-1.65142959479989,3.30424588822654,10.9765059300651));
#22943=CARTESIAN_POINT('Ctrl Pts',(-1.67995846001316,3.33035757709127,10.9721726752733));
#22944=CARTESIAN_POINT('Ctrl Pts',(-1.73580177581937,3.38404418683126,10.9634769150375));
#22945=CARTESIAN_POINT('Ctrl Pts',(-1.76310394536657,3.41160605178525,10.9591164076345));
#22946=CARTESIAN_POINT('Ctrl Pts',(-1.81652054390736,3.46827741771502,10.950389075345));
#22947=CARTESIAN_POINT('Ctrl Pts',(-1.84243547813984,3.49717550469378,10.9460549961774));
#22948=CARTESIAN_POINT('Ctrl Pts',(-1.91759973418787,3.58528425276366,10.9332254057859));
#22949=CARTESIAN_POINT('Ctrl Pts',(-1.96446790094007,3.64607226263407,10.924873889815));
#22950=CARTESIAN_POINT('Ctrl Pts',(-2.05174009021352,3.77158859432735,10.9088206765596));
#22951=CARTESIAN_POINT('Ctrl Pts',(-2.09216488383321,3.83633288700501,10.901115442483));
#22952=CARTESIAN_POINT('Ctrl Pts',(-2.16654149406423,3.96984994441741,10.8865775716981));
#22953=CARTESIAN_POINT('Ctrl Pts',(-2.20049638474852,4.03862680065782,10.8797440406559));
#22954=CARTESIAN_POINT('Ctrl Pts',(-2.26167466414558,4.18036900107911,10.8671908711269));
#22955=CARTESIAN_POINT('Ctrl Pts',(-2.28842901591865,4.25224727888041,10.861569105968));
#22956=CARTESIAN_POINT('Ctrl Pts',(-2.32294443531106,4.36156646287466,10.8542206101891));
#22957=CARTESIAN_POINT('Ctrl Pts',(-2.33351137927865,4.39825592106845,10.8519518627414));
#22958=CARTESIAN_POINT('Ctrl Pts',(-2.35276891893271,4.47213522058744,10.8477930062897));
#22959=CARTESIAN_POINT('Ctrl Pts',(-2.36145955719913,4.50932505011558,10.8459028807817));
#22960=CARTESIAN_POINT('Ctrl Pts',(-2.37695087388553,4.58420950581499,10.842518395405));
#22961=CARTESIAN_POINT('Ctrl Pts',(-2.38375121930333,4.62190806642754,10.8410241061104));
#22962=CARTESIAN_POINT('Ctrl Pts',(-2.39543543506865,4.69780231164114,10.8384483539548));
#22963=CARTESIAN_POINT('Ctrl Pts',(-2.40032026602255,4.73607758644075,10.8373666666763));
#22964=CARTESIAN_POINT('Ctrl Pts',(-2.4080591253686,4.81229232838475,10.8356497156866));
#22965=CARTESIAN_POINT('Ctrl Pts',(-2.41094073121308,4.85039249837638,10.8350083744313));
#22966=CARTESIAN_POINT('Ctrl Pts',(-2.41474521241477,4.92648239506272,10.8341611253141));
#22967=CARTESIAN_POINT('Ctrl Pts',(-2.41567073860182,4.96448834035588,10.8339546120371));
#22968=CARTESIAN_POINT('Ctrl Pts',(-2.41554570444982,5.07839028587593,10.8339825280547));
#22969=CARTESIAN_POINT('Ctrl Pts',(-2.41159986026808,5.15417063580015,10.8348645066324));
#22970=CARTESIAN_POINT('Ctrl Pts',(-2.39987263492885,5.26760931939004,10.8374657949017));
#22971=CARTESIAN_POINT('Ctrl Pts',(-2.3949939379871,5.30538351494416,10.8385459312144));
#22972=CARTESIAN_POINT('Ctrl Pts',(-2.38327313722814,5.38085361371876,10.8411292271885));
#22973=CARTESIAN_POINT('Ctrl Pts',(-2.37643605907484,5.41852509424237,10.842631312589));
#22974=CARTESIAN_POINT('Ctrl Pts',(-2.36074019728461,5.49388602647724,10.8460595647364));
#22975=CARTESIAN_POINT('Ctrl Pts',(-2.35192727742988,5.53133066944476,10.847975598964));
#22976=CARTESIAN_POINT('Ctrl Pts',(-2.33249514119272,5.60538197638679,10.8521704144231));
#22977=CARTESIAN_POINT('Ctrl Pts',(-2.32185976834581,5.64206644689879,10.8544527161351));
#22978=CARTESIAN_POINT('Ctrl Pts',(-2.28725682906933,5.75104027067158,10.8618161407086));
#22979=CARTESIAN_POINT('Ctrl Pts',(-2.26058751143076,5.82230286023678,10.8674161778334));
#22980=CARTESIAN_POINT('Ctrl Pts',(-2.20012765225572,5.96207070793676,10.879817410451));
#22981=CARTESIAN_POINT('Ctrl Pts',(-2.16632117305358,6.03059585160356,10.8866217931097));
#22982=CARTESIAN_POINT('Ctrl Pts',(-2.11021062948697,6.13124662702467,10.8975875763066));
#22983=CARTESIAN_POINT('Ctrl Pts',(-2.09055922533177,6.16450059218788,10.9013776540111));
#22984=CARTESIAN_POINT('Ctrl Pts',(-2.0495249337574,6.23010608733983,10.9091667943008));
#22985=CARTESIAN_POINT('Ctrl Pts',(-2.02827774511065,6.26224430958768,10.9131400653633));
#22986=CARTESIAN_POINT('Ctrl Pts',(-1.98427798089149,6.32533987135752,10.921226002024));
#22987=CARTESIAN_POINT('Ctrl Pts',(-1.96153794828895,6.35627729755836,10.9253362970998));
#22988=CARTESIAN_POINT('Ctrl Pts',(-1.91459588826076,6.41695053601302,10.9336602605952));
#22989=CARTESIAN_POINT('Ctrl Pts',(-1.89039379550754,6.44668629011437,10.9378739665585));
#22990=CARTESIAN_POINT('Ctrl Pts',(-1.81560525975469,6.53410605383734,10.9506242215266));
#22991=CARTESIAN_POINT('Ctrl Pts',(-1.76282588318345,6.59001917192089,10.9592724352714));
#22992=CARTESIAN_POINT('Ctrl Pts',(-1.67929121916504,6.67026153860375,10.9722747191892));
#22993=CARTESIAN_POINT('Ctrl Pts',(-1.65068440659162,6.69642949301749,10.9766184770752));
#22994=CARTESIAN_POINT('Ctrl Pts',(-1.60668911510993,6.73473798863923,10.9831145720195));
#22995=CARTESIAN_POINT('Ctrl Pts',(-1.5918286735277,6.74736125538106,10.9852786585169));
#22996=CARTESIAN_POINT('Ctrl Pts',(-1.56173096481231,6.77229914034996,10.9895979272402));
#22997=CARTESIAN_POINT('Ctrl Pts',(-1.54649511948918,6.78461114468206,10.9917527484078));
#22998=CARTESIAN_POINT('Ctrl Pts',(-1.50046299609324,6.8208863539386,10.9981636505124));
#22999=CARTESIAN_POINT('Ctrl Pts',(-1.46926889933719,6.8442557123388,11.0023772465835));
#23000=CARTESIAN_POINT('Ctrl Pts',(-1.4058819134907,6.88939440371742,11.0106562928922));
#23001=CARTESIAN_POINT('Ctrl Pts',(-1.37368942458412,6.91116409133562,11.014721793832));
#23002=CARTESIAN_POINT('Ctrl Pts',(-1.27562769998999,6.97410209399274,11.0266560937395));
#23003=CARTESIAN_POINT('Ctrl Pts',(-1.20827745529124,7.01290459305882,11.0342629589178));
#23004=CARTESIAN_POINT('Ctrl Pts',(-1.10427269937667,7.06637670145155,11.0449911598163));
#23005=CARTESIAN_POINT('Ctrl Pts',(-1.06910708126474,7.08341081377451,11.0484536090625));
#23006=CARTESIAN_POINT('Ctrl Pts',(-0.997767307365202,7.1158814910318,11.0551244811633));
#23007=CARTESIAN_POINT('Ctrl Pts',(-0.961574891490949,7.13132421016612,
11.0583342396346));
#23008=CARTESIAN_POINT('Ctrl Pts',(-0.888233537645138,7.16055810015767,
11.0644671680054));
#23009=CARTESIAN_POINT('Ctrl Pts',(-0.850905427704504,7.174408118809,11.0674029783619));
#23010=CARTESIAN_POINT('Ctrl Pts',(-0.775972604593802,7.20017590695015,
11.0729086838722));
#23011=CARTESIAN_POINT('Ctrl Pts',(-0.738304539072183,7.21212774105555,
11.0754854863593));
#23012=CARTESIAN_POINT('Ctrl Pts',(-0.662579844985102,7.23419056906833,
11.0802734702955));
#23013=CARTESIAN_POINT('Ctrl Pts',(-0.624521775547128,7.24430304346141,
11.082484955623));
#23014=CARTESIAN_POINT('Ctrl Pts',(-0.548017474289304,7.26270849228187,
11.0865313321938));
#23015=CARTESIAN_POINT('Ctrl Pts',(-0.509571237699919,7.27100144163261,
11.0883662321975));
#23016=CARTESIAN_POINT('Ctrl Pts',(-0.432291130932363,7.28577276473672,
11.0916478861797));
#23017=CARTESIAN_POINT('Ctrl Pts',(-0.393457261520405,7.29225114048083,
11.0930946487716));
#23018=CARTESIAN_POINT('Ctrl Pts',(-0.315399720419757,7.30338509498235,
11.095588332377));
#23019=CARTESIAN_POINT('Ctrl Pts',(-0.276176055080666,7.30804070294351,
11.0966352622835));
#23020=CARTESIAN_POINT('Ctrl Pts',(-0.197333992891634,7.31550747812966,
11.0983172863715));
#23021=CARTESIAN_POINT('Ctrl Pts',(-0.157704437931099,7.31831807552468,
11.0989522478944));
#23022=CARTESIAN_POINT('Ctrl Pts',(-0.0780874231236657,7.32206150143807,
11.0997984477102));
#23023=CARTESIAN_POINT('Ctrl Pts',(-0.0379603180932254,7.32298838989236,
11.1000083329759));
#23024=CARTESIAN_POINT('Ctrl Pts',(0.0417241354210129,7.32292629716545,
11.099994280309));
#23025=CARTESIAN_POINT('Ctrl Pts',(0.0814525850909876,7.32194969219772,
11.0997731475059));
#23026=CARTESIAN_POINT('Ctrl Pts',(0.160590954427694,7.31813222019943,11.0989102633425));
#23027=CARTESIAN_POINT('Ctrl Pts',(0.20001689949773,7.31529243258597,11.0982687691481));
#23028=CARTESIAN_POINT('Ctrl Pts',(0.317869850089211,7.30401006241601,11.0957274457278));
#23029=CARTESIAN_POINT('Ctrl Pts',(0.39587285156736,7.29281046628245,11.0932107509896));
#23030=CARTESIAN_POINT('Ctrl Pts',(0.512030046125537,7.27049131741402,11.0882532445282));
#23031=CARTESIAN_POINT('Ctrl Pts',(0.550607673542793,7.26213015717154,11.086403628318));
#23032=CARTESIAN_POINT('Ctrl Pts',(0.627477206669618,7.24354385437346,11.0823186508056));
#23033=CARTESIAN_POINT('Ctrl Pts',(0.665755064237897,7.23332253883107,11.0800840952145));
#23034=CARTESIAN_POINT('Ctrl Pts',(0.722996099836931,7.21655528832399,11.0764469056906));
#23035=CARTESIAN_POINT('Ctrl Pts',(0.742042918675023,7.21072650572253,11.0751869081376));
#23036=CARTESIAN_POINT('Ctrl Pts',(0.779849633212899,7.19865927796806,11.0725889483452));
#23037=CARTESIAN_POINT('Ctrl Pts',(0.798649001180196,7.19240958846945,11.0712485432115));
#23038=CARTESIAN_POINT('Ctrl Pts',(0.854666863641607,7.17304031601826,11.067112468226));
#23039=CARTESIAN_POINT('Ctrl Pts',(0.891570912702515,7.15928178548173,11.0641978059314));
#23040=CARTESIAN_POINT('Ctrl Pts',(1.00088099062815,7.11554187341872,11.0550267106888));
#23041=CARTESIAN_POINT('Ctrl Pts',(1.07196896812727,7.0830775621415,11.0483378721597));
#23042=CARTESIAN_POINT('Ctrl Pts',(1.21057840344948,7.01162593460114,11.0340105647525));
#23043=CARTESIAN_POINT('Ctrl Pts',(1.27812692254345,6.97261769660203,11.0263679610096));
#23044=CARTESIAN_POINT('Ctrl Pts',(1.37669697349307,6.90916978481267,11.0143471976774));
#23045=CARTESIAN_POINT('Ctrl Pts',(1.40914141553145,6.88715448579056,11.0102403439491));
#23046=CARTESIAN_POINT('Ctrl Pts',(1.47300711921128,6.8415030610202,11.0018780835753));
#23047=CARTESIAN_POINT('Ctrl Pts',(1.50419107014757,6.81803676660196,10.997653926145));
#23048=CARTESIAN_POINT('Ctrl Pts',(1.56518118183191,6.76978651362157,10.9891396747484));
#23049=CARTESIAN_POINT('Ctrl Pts',(1.59497278844201,6.74501293387364,10.9848514749544));
#23050=CARTESIAN_POINT('Ctrl Pts',(1.65317070166917,6.69418444296186,10.976243756771));
#23051=CARTESIAN_POINT('Ctrl Pts',(1.68157694109886,6.66812947486887,10.9719242010104));
#23052=CARTESIAN_POINT('Ctrl Pts',(1.76473424719298,6.58805129410511,10.9589642510358));
#23053=CARTESIAN_POINT('Ctrl Pts',(1.81743452458119,6.53211093866748,10.9503210215531));
#23054=CARTESIAN_POINT('Ctrl Pts',(1.89232452431014,6.44435373899584,10.9375402227472));
#23055=CARTESIAN_POINT('Ctrl Pts',(1.91660671007598,6.41443993771718,10.933308141626));
#23056=CARTESIAN_POINT('Ctrl Pts',(1.95195872350825,6.36860811698971,10.9270323866911));
#23057=CARTESIAN_POINT('Ctrl Pts',(1.96357402652069,6.35315622680682,10.9249507025615));
#23058=CARTESIAN_POINT('Ctrl Pts',(1.98643628446213,6.3219390979067,10.9208169219368));
#23059=CARTESIAN_POINT('Ctrl Pts',(1.9977042602328,6.30614290086018,10.9187609319534));
#23060=CARTESIAN_POINT('Ctrl Pts',(2.03081608796765,6.25847073177151,10.9126681102492));
#23061=CARTESIAN_POINT('Ctrl Pts',(2.05198092012552,6.22630457810867,10.9087046566163));
#23062=CARTESIAN_POINT('Ctrl Pts',(2.09256316418001,6.16115702982226,10.9009927356767));
#23063=CARTESIAN_POINT('Ctrl Pts',(2.11197419513562,6.12818538630473,10.8972454344251));
#23064=CARTESIAN_POINT('Ctrl Pts',(2.16759831848063,6.02808738494578,10.8863668497116));
#23065=CARTESIAN_POINT('Ctrl Pts',(2.20120809777231,5.95978047562522,10.8795986198096));
#23066=CARTESIAN_POINT('Ctrl Pts',(2.2614896280558,5.82000298645159,10.8672282185851));
#23067=CARTESIAN_POINT('Ctrl Pts',(2.2881589362429,5.74852711829037,10.8616262047409));
#23068=CARTESIAN_POINT('Ctrl Pts',(2.31704068721011,5.65715216261029,10.8554776448299));
#23069=CARTESIAN_POINT('Ctrl Pts',(2.32259192245271,5.63877136657054,10.854291036586));
#23070=CARTESIAN_POINT('Ctrl Pts',(2.33324304840448,5.60180732026267,10.8520064569235));
#23071=CARTESIAN_POINT('Ctrl Pts',(2.33834431821141,5.5832109511349,10.8509081711304));
#23072=CARTESIAN_POINT('Ctrl Pts',(2.35288057231345,5.52742057732017,10.84776883442));
#23073=CARTESIAN_POINT('Ctrl Pts',(2.36157792726873,5.49014214904587,10.8458770896334));
#23074=CARTESIAN_POINT('Ctrl Pts',(2.3770239137965,5.41539753514177,10.8425023671237));
#23075=CARTESIAN_POINT('Ctrl Pts',(2.38377222451045,5.37793487473886,10.8410194554346));
#23076=CARTESIAN_POINT('Ctrl Pts',(2.39534115048824,5.30283063923535,10.8384691587443));
#23077=CARTESIAN_POINT('Ctrl Pts',(2.40016173520365,5.26518906149763,10.8374017701789));
#23078=CARTESIAN_POINT('Ctrl Pts',(2.40788262248997,5.18972752394682,10.8356889400362));
#23079=CARTESIAN_POINT('Ctrl Pts',(2.4107829231545,5.1519075640333,10.8350434949868));
#23080=CARTESIAN_POINT('Ctrl Pts',(2.41465680569752,5.07608856983399,10.8341808348376));
#23081=CARTESIAN_POINT('Ctrl Pts',(2.41563041413539,5.03808953797268,10.8339636161659));
#23082=CARTESIAN_POINT('Ctrl Pts',(2.4156304102994,5.,10.8339636164256));
#23083=CARTESIAN_POINT('Ctrl Pts',(1.99999329969225,5.,10.4183265058185));
#23084=CARTESIAN_POINT('Ctrl Pts',(1.99999329651629,4.9672060898008,10.4183265060683));
#23085=CARTESIAN_POINT('Ctrl Pts',(1.99918550496642,4.93431991835465,10.4185358368808));
#23086=CARTESIAN_POINT('Ctrl Pts',(1.99593548063469,4.8684463021299,10.4193764351511));
#23087=CARTESIAN_POINT('Ctrl Pts',(1.99347532813476,4.83531123743932,10.4200123223252));
#23088=CARTESIAN_POINT('Ctrl Pts',(1.98695423610042,4.76962735899715,10.4216924484417));
#23089=CARTESIAN_POINT('Ctrl Pts',(1.9828938600587,4.73697691689266,10.4227365369645));
#23090=CARTESIAN_POINT('Ctrl Pts',(1.97320227918419,4.67209444612268,10.4252175141091));
#23091=CARTESIAN_POINT('Ctrl Pts',(1.96757121663137,4.63985518083304,10.4266543569164));
#23092=CARTESIAN_POINT('Ctrl Pts',(1.94834982349861,4.5437354653307,10.4315309041118));
#23093=CARTESIAN_POINT('Ctrl Pts',(1.93243634306278,4.48045185824893,10.4355367579463));
#23094=CARTESIAN_POINT('Ctrl Pts',(1.90392279791606,4.38671528043056,10.442586510252));
#23095=CARTESIAN_POINT('Ctrl Pts',(1.89364312792087,4.35566820621918,10.4451099494912));
#23096=CARTESIAN_POINT('Ctrl Pts',(1.87151692855195,4.29397433422457,10.4504884337122));
#23097=CARTESIAN_POINT('Ctrl Pts',(1.8596730913725,4.26333484541557,10.4533428527908));
#23098=CARTESIAN_POINT('Ctrl Pts',(1.84070326139284,4.21765849102848,10.4578633272628));
#23099=CARTESIAN_POINT('Ctrl Pts',(1.83417476952651,4.20247322320904,10.4594109454833));
#23100=CARTESIAN_POINT('Ctrl Pts',(1.82078759487817,4.1723662137063,10.4625658954651));
#23101=CARTESIAN_POINT('Ctrl Pts',(1.8139182967022,4.15741779964833,10.4641757713891));
#23102=CARTESIAN_POINT('Ctrl Pts',(1.79281142230163,4.11293895107949,10.469091675146));
#23103=CARTESIAN_POINT('Ctrl Pts',(1.77805144823985,4.08371702979842,10.4724896250146));
#23104=CARTESIAN_POINT('Ctrl Pts',(1.73178297287775,3.99742329311597,10.4829916336515));
#23105=CARTESIAN_POINT('Ctrl Pts',(1.69825509779176,3.94163610714523,10.4904122825615));
#23106=CARTESIAN_POINT('Ctrl Pts',(1.64399721279419,3.86056791689028,10.5020007414106));
#23107=CARTESIAN_POINT('Ctrl Pts',(1.62524809577395,3.83397903878751,10.5059401511702));
#23108=CARTESIAN_POINT('Ctrl Pts',(1.58641499092785,3.78167167763213,10.5139445047481));
#23109=CARTESIAN_POINT('Ctrl Pts',(1.56633104223321,3.7559531345937,10.5180094840654));
#23110=CARTESIAN_POINT('Ctrl Pts',(1.52480987404805,3.70539559767788,10.5262372032753));
#23111=CARTESIAN_POINT('Ctrl Pts',(1.50337048018112,3.68055413064413,10.5304003716057));
#23112=CARTESIAN_POINT('Ctrl Pts',(1.45911762663949,3.63177628328041,10.538794504498));
#23113=CARTESIAN_POINT('Ctrl Pts',(1.43648604695728,3.60803990912586,10.5429908514021));
#23114=CARTESIAN_POINT('Ctrl Pts',(1.39021999498227,3.56182975575039,10.5513546120022));
#23115=CARTESIAN_POINT('Ctrl Pts',(1.36658750414032,3.53935823956277,10.5555216537896));
#23116=CARTESIAN_POINT('Ctrl Pts',(1.31833511057554,3.4956634330663,10.563797173489));
#23117=CARTESIAN_POINT('Ctrl Pts',(1.29371516402102,3.4744402038623,10.5679056875586));
#23118=CARTESIAN_POINT('Ctrl Pts',(1.21838031138833,3.41262885610495,10.5801008983079));
#23119=CARTESIAN_POINT('Ctrl Pts',(1.16619163330238,3.3738935679989,10.588057881209));
#23120=CARTESIAN_POINT('Ctrl Pts',(1.0849284943634,3.3195328362764,10.5995631973718));
#23121=CARTESIAN_POINT('Ctrl Pts',(1.05733670199568,3.30203376391625,10.6033274547364));
#23122=CARTESIAN_POINT('Ctrl Pts',(1.00115279162757,3.26831153442107,10.6106821824337));
#23123=CARTESIAN_POINT('Ctrl Pts',(0.972514774920624,3.25206380209878,10.6142781722521));
#23124=CARTESIAN_POINT('Ctrl Pts',(0.91435197292097,3.22094806984305,10.6212500038866));
#23125=CARTESIAN_POINT('Ctrl Pts',(0.885034436887127,3.20618714160478,10.6246015451677));
#23126=CARTESIAN_POINT('Ctrl Pts',(0.825828950189364,3.17817200284419,10.6310303142887));
#23127=CARTESIAN_POINT('Ctrl Pts',(0.795958862538632,3.16492735167072,10.6341054306391));
#23128=CARTESIAN_POINT('Ctrl Pts',(0.705554495503631,3.12745406571931,10.6428859720493));
#23129=CARTESIAN_POINT('Ctrl Pts',(0.644227760967397,3.10548128005308,10.6481468026185));
#23130=CARTESIAN_POINT('Ctrl Pts',(0.519455931177073,3.06754146105868,10.6573403229691));
#23131=CARTESIAN_POINT('Ctrl Pts',(0.455999123235534,3.05157571903715,10.6612729783714));
#23132=CARTESIAN_POINT('Ctrl Pts',(0.375343103600641,3.03547178999415,10.6652684116006));
#23133=CARTESIAN_POINT('Ctrl Pts',(0.359133507551698,3.03244459906876,10.6660213344221));
#23134=CARTESIAN_POINT('Ctrl Pts',(0.326598058853661,3.02678286057751,10.6674322259349));
#23135=CARTESIAN_POINT('Ctrl Pts',(0.31023677495422,3.02414413944877,10.6680912369941));
#23136=CARTESIAN_POINT('Ctrl Pts',(0.261155201109811,3.01685349569121,10.6699150009392));
#23137=CARTESIAN_POINT('Ctrl Pts',(0.22847024564255,3.01282626759034,10.6709265510874));
#23138=CARTESIAN_POINT('Ctrl Pts',(0.163089125504509,3.00639519947324,10.6725446669741));
#23139=CARTESIAN_POINT('Ctrl Pts',(0.130406807857837,3.00399314513972,10.6731507948452));
#23140=CARTESIAN_POINT('Ctrl Pts',(0.0650584620285826,3.00079597561227,
10.6739580110074));
#23141=CARTESIAN_POINT('Ctrl Pts',(0.0323924341257924,3.00000088911391,
10.6741590988424));
#23142=CARTESIAN_POINT('Ctrl Pts',(-0.032923411838495,3.00000955883287,
10.6741569073271));
#23143=CARTESIAN_POINT('Ctrl Pts',(-0.0655732298525685,3.00081331976463,
10.6739536275487));
#23144=CARTESIAN_POINT('Ctrl Pts',(-0.130856623814915,3.0040231099398,10.6731432338706));
#23145=CARTESIAN_POINT('Ctrl Pts',(-0.163490199944121,3.0064291203195,10.6725361195498));
#23146=CARTESIAN_POINT('Ctrl Pts',(-0.228740964854252,3.01285848338826,
10.6709184580371));
#23147=CARTESIAN_POINT('Ctrl Pts',(-0.261373748002534,3.0168851197008,10.6699070866313));
#23148=CARTESIAN_POINT('Ctrl Pts',(-0.326560287476677,3.02656970148655,
10.6674844830799));
#23149=CARTESIAN_POINT('Ctrl Pts',(-0.359266726646795,3.03226049388052,
10.6660651110172));
#23150=CARTESIAN_POINT('Ctrl Pts',(-0.423987191574684,3.04518560826949,
10.6628584170459));
#23151=CARTESIAN_POINT('Ctrl Pts',(-0.456064932944746,3.05242240491246,
10.6610704420591));
#23152=CARTESIAN_POINT('Ctrl Pts',(-0.519654369291847,3.06841697461527,
10.6571441421124));
#23153=CARTESIAN_POINT('Ctrl Pts',(-0.551168192433233,3.07717440437623,
10.6550058975318));
#23154=CARTESIAN_POINT('Ctrl Pts',(-0.644878628993597,3.10569930066508,
10.6480943469511));
#23155=CARTESIAN_POINT('Ctrl Pts',(-0.706245942918383,3.12771447121482,
10.6428240918291));
#23156=CARTESIAN_POINT('Ctrl Pts',(-0.796647518071845,3.16522613098054,
10.6340358606123));
#23157=CARTESIAN_POINT('Ctrl Pts',(-0.826506033457877,3.17847940669766,
10.6309592485692));
#23158=CARTESIAN_POINT('Ctrl Pts',(-0.885668032788551,3.20650022188821,
10.6245302370582));
#23159=CARTESIAN_POINT('Ctrl Pts',(-0.914968401476247,3.22126654168918,
10.6211780999659));
#23160=CARTESIAN_POINT('Ctrl Pts',(-0.958505863735288,3.24457519015467,
10.6159563624653));
#23161=CARTESIAN_POINT('Ctrl Pts',(-0.972963824634976,3.25254737910032,
10.6141815298874));
#23162=CARTESIAN_POINT('Ctrl Pts',(-1.00160130942706,3.26880296837598,10.6105874054219));
#23163=CARTESIAN_POINT('Ctrl Pts',(-1.01579552667855,3.27709346474105,10.6087664888383));
#23164=CARTESIAN_POINT('Ctrl Pts',(-1.05796683103677,3.3024260162378,10.6032426856883));
#23165=CARTESIAN_POINT('Ctrl Pts',(-1.08558974144489,3.31995883450879,10.5994720097086));
#23166=CARTESIAN_POINT('Ctrl Pts',(-1.16688841085728,3.37439294419322,10.5879542782074));
#23167=CARTESIAN_POINT('Ctrl Pts',(-1.21910060269637,3.4131810775366,10.579988955122));
#23168=CARTESIAN_POINT('Ctrl Pts',(-1.2944322379834,3.47504835541167,10.5677872279407));
#23169=CARTESIAN_POINT('Ctrl Pts',(-1.31904709760952,3.49628763840776,10.5636772460622));
#23170=CARTESIAN_POINT('Ctrl Pts',(-1.36728206038105,3.54000833243635,10.555400287582));
#23171=CARTESIAN_POINT('Ctrl Pts',(-1.39090220484978,3.5624896862504,10.5512332749491));
#23172=CARTESIAN_POINT('Ctrl Pts',(-1.43713703322785,3.60871219123269,10.542871121211));
#23173=CARTESIAN_POINT('Ctrl Pts',(-1.45974154918718,3.63244210165777,10.5386779014935));
#23174=CARTESIAN_POINT('Ctrl Pts',(-1.5039672050319,3.68123438909642,10.5302853869406));
#23175=CARTESIAN_POINT('Ctrl Pts',(-1.52542317553505,3.70611474522063,10.5261175815582));
#23176=CARTESIAN_POINT('Ctrl Pts',(-1.5876545532419,3.781973643112,10.5137801890434));
#23177=CARTESIAN_POINT('Ctrl Pts',(-1.62645851061903,3.83431023323932,10.5057490728896));
#23178=CARTESIAN_POINT('Ctrl Pts',(-1.69871451180625,3.94237589980096,10.4903117294499));
#23179=CARTESIAN_POINT('Ctrl Pts',(-1.73218375281194,3.99811872665182,10.4829021010573));
#23180=CARTESIAN_POINT('Ctrl Pts',(-1.79376300826393,4.11307276977823,10.4689219650798));
#23181=CARTESIAN_POINT('Ctrl Pts',(-1.8218755678564,4.1722875087188,10.4623505974706));
#23182=CARTESIAN_POINT('Ctrl Pts',(-1.87252741772401,4.29432314473221,10.450279021133));
#23183=CARTESIAN_POINT('Ctrl Pts',(-1.89467837428495,4.3562081113934,10.4448729308931));
#23184=CARTESIAN_POINT('Ctrl Pts',(-1.92325501714616,4.45032853641604,10.4378063547941));
#23185=CARTESIAN_POINT('Ctrl Pts',(-1.93200379636489,4.48191702137343,10.435624646187));
#23186=CARTESIAN_POINT('Ctrl Pts',(-1.94794785391295,4.54552480563549,10.4316253412292));
#23187=CARTESIAN_POINT('Ctrl Pts',(-1.95514316749603,4.57754409478369,10.4298077290074));
#23188=CARTESIAN_POINT('Ctrl Pts',(-1.96796902423475,4.64201728732508,10.4265530869432));
#23189=CARTESIAN_POINT('Ctrl Pts',(-1.97359929168517,4.67447457815043,10.4251161249672));
#23190=CARTESIAN_POINT('Ctrl Pts',(-1.983273103185,4.73981716812693,10.4226391896641));
#23191=CARTESIAN_POINT('Ctrl Pts',(-1.98731744255768,4.77277099197138,10.4215990005289));
#23192=CARTESIAN_POINT('Ctrl Pts',(-1.99372474177576,4.83838951968663,10.4199479191114));
#23193=CARTESIAN_POINT('Ctrl Pts',(-1.99611053405461,4.87119258372489,10.4193311824455));
#23194=CARTESIAN_POINT('Ctrl Pts',(-1.99926041032697,4.93670362354867,10.4185164374226));
#23195=CARTESIAN_POINT('Ctrl Pts',(-2.00002668904448,4.96942556304549,10.4183178468768));
#23196=CARTESIAN_POINT('Ctrl Pts',(-1.99992316846238,5.06749160352923,10.4183446919168));
#23197=CARTESIAN_POINT('Ctrl Pts',(-1.99665625234319,5.13273613319904,10.4191928340298));
#23198=CARTESIAN_POINT('Ctrl Pts',(-1.98694683156342,5.23040331953685,10.4216943257723));
#23199=CARTESIAN_POINT('Ctrl Pts',(-1.98290757077532,5.2629257297,10.4227330234433));
#23200=CARTESIAN_POINT('Ctrl Pts',(-1.9732034691524,5.32790314275541,10.4252172131519));
#23201=CARTESIAN_POINT('Ctrl Pts',(-1.96754278925792,5.36033711846412,10.4266616721418));
#23202=CARTESIAN_POINT('Ctrl Pts',(-1.9545475817628,5.4252205425165,10.4299584018965));
#23203=CARTESIAN_POINT('Ctrl Pts',(-1.94725102655095,5.4574592181287,10.4318009288688));
#23204=CARTESIAN_POINT('Ctrl Pts',(-1.93116241377835,5.52121509544425,10.4358348132929));
#23205=CARTESIAN_POINT('Ctrl Pts',(-1.92235697965934,5.55279928616215,10.4380295561648));
#23206=CARTESIAN_POINT('Ctrl Pts',(-1.8937078757207,5.64662236675201,10.4451104883262));
#23207=CARTESIAN_POINT('Ctrl Pts',(-1.87162732218956,5.70797724494732,10.4504956841121));
#23208=CARTESIAN_POINT('Ctrl Pts',(-1.82157028004747,5.82831302453619,10.462421152487));
#23209=CARTESIAN_POINT('Ctrl Pts',(-1.79358059602456,5.88731104676773,10.4689644899698));
#23210=CARTESIAN_POINT('Ctrl Pts',(-1.74712451951398,5.97396824099842,10.4795095788929));
#23211=CARTESIAN_POINT('Ctrl Pts',(-1.73085436639918,6.00259887306966,10.4831542530315));
#23212=CARTESIAN_POINT('Ctrl Pts',(-1.69688049860201,6.05908316852454,10.4906445686363));
#23213=CARTESIAN_POINT('Ctrl Pts',(-1.67928913414922,6.08675318056602,10.4944654080531));
#23214=CARTESIAN_POINT('Ctrl Pts',(-1.64286003752453,6.14107650126717,10.5022411336526));
#23215=CARTESIAN_POINT('Ctrl Pts',(-1.62403269015965,6.16771266517537,10.5061937402564));
#23216=CARTESIAN_POINT('Ctrl Pts',(-1.58516755370093,6.2199504406717,10.5141983609647));
#23217=CARTESIAN_POINT('Ctrl Pts',(-1.56512971051978,6.2455520021926,10.5182504111727));
#23218=CARTESIAN_POINT('Ctrl Pts',(-1.50320940608863,6.32081770594603,10.5305115119104));
#23219=CARTESIAN_POINT('Ctrl Pts',(-1.45951133081404,6.36895716551933,10.5388279432439));
#23220=CARTESIAN_POINT('Ctrl Pts',(-1.39034977049567,6.43804335315058,10.5513314040246));
#23221=CARTESIAN_POINT('Ctrl Pts',(-1.36666509041035,6.46057314985643,10.5555085168081));
#23222=CARTESIAN_POINT('Ctrl Pts',(-1.33023969693693,6.49355557579673,10.5617553938089));
#23223=CARTESIAN_POINT('Ctrl Pts',(-1.31793616595463,6.50442381673603,10.5638364567065));
#23224=CARTESIAN_POINT('Ctrl Pts',(-1.29301711562714,6.5258945618213,10.5679900198363));
#23225=CARTESIAN_POINT('Ctrl Pts',(-1.28040277345317,6.53649481548491,10.5700621728617));
#23226=CARTESIAN_POINT('Ctrl Pts',(-1.24229100852006,6.56772664496179,10.5762271253839));
#23227=CARTESIAN_POINT('Ctrl Pts',(-1.21646421637671,6.58784693734603,10.5802790699156));
#23228=CARTESIAN_POINT('Ctrl Pts',(-1.16398369351188,6.62670994987825,10.5882404966524));
#23229=CARTESIAN_POINT('Ctrl Pts',(-1.13733029411824,6.64545297536011,10.5921500276145));
#23230=CARTESIAN_POINT('Ctrl Pts',(-1.05614122177108,6.69964064255493,10.6036264768123));
#23231=CARTESIAN_POINT('Ctrl Pts',(-1.00037936451277,6.73304839013043,10.6109415101573));
#23232=CARTESIAN_POINT('Ctrl Pts',(-0.914269828020596,6.77908621610956,
10.6212581314547));
#23233=CARTESIAN_POINT('Ctrl Pts',(-0.885154860638645,6.79375205821659,
10.6245877463615));
#23234=CARTESIAN_POINT('Ctrl Pts',(-0.826089918753355,6.82170830370448,
10.6310026953207));
#23235=CARTESIAN_POINT('Ctrl Pts',(-0.796124826023135,6.83500400566012,
10.6340893137497));
#23236=CARTESIAN_POINT('Ctrl Pts',(-0.7354026991366,6.86017347775672,10.6399869567978));
#23237=CARTESIAN_POINT('Ctrl Pts',(-0.704497321620944,6.87209791402106,
10.6428101369315));
#23238=CARTESIAN_POINT('Ctrl Pts',(-0.642457556136971,6.89428317998444,
10.6481046200665));
#23239=CARTESIAN_POINT('Ctrl Pts',(-0.611270716323594,6.90457333825948,
10.650582565406));
#23240=CARTESIAN_POINT('Ctrl Pts',(-0.548575330411194,6.92356874852439,
10.6551868618314));
#23241=CARTESIAN_POINT('Ctrl Pts',(-0.51706559135898,6.93227527516635,10.6573135051376));
#23242=CARTESIAN_POINT('Ctrl Pts',(-0.453724738693371,6.94812179544253,
10.6612046454231));
#23243=CARTESIAN_POINT('Ctrl Pts',(-0.421893621131155,6.95526176748658,
10.6629691508268));
#23244=CARTESIAN_POINT('Ctrl Pts',(-0.357910449253673,6.96797941829523,
10.666124906548));
#23245=CARTESIAN_POINT('Ctrl Pts',(-0.325758395572844,6.97355709877383,
10.6675161651485));
#23246=CARTESIAN_POINT('Ctrl Pts',(-0.261131555917996,6.98314308809049,
10.6699141804015));
#23247=CARTESIAN_POINT('Ctrl Pts',(-0.228656775201119,6.98715142207219,
10.6709209456059));
#23248=CARTESIAN_POINT('Ctrl Pts',(-0.163380400371696,6.99358008379832,
10.6725384400668));
#23249=CARTESIAN_POINT('Ctrl Pts',(-0.130569568031515,6.99599992093688,
10.6731490417541));
#23250=CARTESIAN_POINT('Ctrl Pts',(-0.0646515801295788,6.99922289448238,
10.6739627777313));
#23251=CARTESIAN_POINT('Ctrl Pts',(-0.0314288069565178,7.00002091667821,
10.6741646109019));
#23252=CARTESIAN_POINT('Ctrl Pts',(0.034545016044109,6.99996745676729,10.6741510973553));
#23253=CARTESIAN_POINT('Ctrl Pts',(0.0674377271166929,6.99912663019606,
10.6739384481509));
#23254=CARTESIAN_POINT('Ctrl Pts',(0.132959426026927,6.99583990526937,10.6731086679089));
#23255=CARTESIAN_POINT('Ctrl Pts',(0.165601681910348,6.99339493625858,10.6724917841714));
#23256=CARTESIAN_POINT('Ctrl Pts',(0.263176671250974,6.98368116565678,10.6700479567701));
#23257=CARTESIAN_POINT('Ctrl Pts',(0.327758355453141,6.97403866093226,10.6676278131896));
#23258=CARTESIAN_POINT('Ctrl Pts',(0.423929363170454,6.95482256636443,10.662860497847));
#23259=CARTESIAN_POINT('Ctrl Pts',(0.455869264250656,6.94762386685945,10.6610818408133));
#23260=CARTESIAN_POINT('Ctrl Pts',(0.51951250642408,6.93162163692076,10.6571535804832));
#23261=CARTESIAN_POINT('Ctrl Pts',(0.551204216520391,6.92282140142685,10.6550047519871));
#23262=CARTESIAN_POINT('Ctrl Pts',(0.598596270858466,6.90838531906186,10.651507100586));
#23263=CARTESIAN_POINT('Ctrl Pts',(0.614365864540558,6.90336691812094,10.6502954419199));
#23264=CARTESIAN_POINT('Ctrl Pts',(0.645667497206255,6.89297740949471,10.6477971509597));
#23265=CARTESIAN_POINT('Ctrl Pts',(0.661232216797669,6.88759662077693,10.6465081694911));
#23266=CARTESIAN_POINT('Ctrl Pts',(0.707611559063241,6.870920278264,10.6425307720051));
#23267=CARTESIAN_POINT('Ctrl Pts',(0.738165840271985,6.85907461042715,10.6397279286031));
#23268=CARTESIAN_POINT('Ctrl Pts',(0.828667856850741,6.82141590347851,10.6309086757391));
#23269=CARTESIAN_POINT('Ctrl Pts',(0.887524326813267,6.79346513890245,10.6244764496207));
#23270=CARTESIAN_POINT('Ctrl Pts',(1.00228440796659,6.73194750487758,10.61069879891));
#23271=CARTESIAN_POINT('Ctrl Pts',(1.05821042421503,6.69836262246893,10.6033493980851));
#23272=CARTESIAN_POINT('Ctrl Pts',(1.13982035950534,6.64373593932943,10.5917898025677));
#23273=CARTESIAN_POINT('Ctrl Pts',(1.166682360582,6.62478145005242,10.587840505287));
#23274=CARTESIAN_POINT('Ctrl Pts',(1.21955923234813,6.58547698998104,10.5797990569321));
#23275=CARTESIAN_POINT('Ctrl Pts',(1.24537762437723,6.5652732386934,10.57573695622));
#23276=CARTESIAN_POINT('Ctrl Pts',(1.29587368296139,6.52373126818002,10.567549347867));
#23277=CARTESIAN_POINT('Ctrl Pts',(1.32053929958603,6.50240198479123,10.5634256617298));
#23278=CARTESIAN_POINT('Ctrl Pts',(1.36872358970513,6.45864023142691,10.555148172375));
#23279=CARTESIAN_POINT('Ctrl Pts',(1.39224220757259,6.43620771243708,10.55099433322));
#23280=CARTESIAN_POINT('Ctrl Pts',(1.4610913387557,6.36726288378714,10.5385315822717));
#23281=CARTESIAN_POINT('Ctrl Pts',(1.50472392477513,6.31909997369742,10.5302199439827));
#23282=CARTESIAN_POINT('Ctrl Pts',(1.56672823513365,6.24354374806328,10.5179294711992));
#23283=CARTESIAN_POINT('Ctrl Pts',(1.58683239039956,6.21778889344791,10.5138597507829));
#23284=CARTESIAN_POINT('Ctrl Pts',(1.6161016816345,6.17832911805555,10.5078247606078));
#23285=CARTESIAN_POINT('Ctrl Pts',(1.62571843761662,6.1650255201114,10.5058229387712));
#23286=CARTESIAN_POINT('Ctrl Pts',(1.64464698003922,6.13814854085892,10.5018477476246));
#23287=CARTESIAN_POINT('Ctrl Pts',(1.65397617044284,6.12454850538974,10.499870634197));
#23288=CARTESIAN_POINT('Ctrl Pts',(1.68139072580193,6.08350424716808,10.4940115591526));
#23289=CARTESIAN_POINT('Ctrl Pts',(1.69891390415089,6.05581018704498,10.4902001605269));
#23290=CARTESIAN_POINT('Ctrl Pts',(1.73251350442475,5.99972016963036,10.4827841018083));
#23291=CARTESIAN_POINT('Ctrl Pts',(1.74858464332341,5.97133260773809,10.4791805630355));
#23292=CARTESIAN_POINT('Ctrl Pts',(1.79463799383422,5.88515133481207,10.4687193272885));
#23293=CARTESIAN_POINT('Ctrl Pts',(1.82246482243469,5.82634120558652,10.4622107555889));
#23294=CARTESIAN_POINT('Ctrl Pts',(1.87237421923056,5.70599712498802,10.4503149357833));
#23295=CARTESIAN_POINT('Ctrl Pts',(1.89445476493774,5.64445862053575,10.444927839113));
#23296=CARTESIAN_POINT('Ctrl Pts',(1.91836707708914,5.56578761925045,10.4390151642179));
#23297=CARTESIAN_POINT('Ctrl Pts',(1.92296315819647,5.54996232425224,10.4378740793336));
#23298=CARTESIAN_POINT('Ctrl Pts',(1.93178163491661,5.5181374274502,10.4356771459032));
#23299=CARTESIAN_POINT('Ctrl Pts',(1.93600517233787,5.50212653071398,10.4346209950434));
#23300=CARTESIAN_POINT('Ctrl Pts',(1.94804029604001,5.45409275014757,10.4316020966957));
#23301=CARTESIAN_POINT('Ctrl Pts',(1.95524117062808,5.42199718022814,10.4297829273177));
#23302=CARTESIAN_POINT('Ctrl Pts',(1.96802949678548,5.35764438713302,10.4265376735752));
#23303=CARTESIAN_POINT('Ctrl Pts',(1.97361668270375,5.32539019906802,10.4251116527113));
#23304=CARTESIAN_POINT('Ctrl Pts',(1.98319504135561,5.26072778293563,10.422659196293));
#23305=CARTESIAN_POINT('Ctrl Pts',(1.98718618879701,5.22831955259754,10.4216327573112));
#23306=CARTESIAN_POINT('Ctrl Pts',(1.99357860825591,5.16334951049017,10.4199856386474));
#23307=CARTESIAN_POINT('Ctrl Pts',(1.99597987869506,5.13078769863434,10.4193649556265));
#23308=CARTESIAN_POINT('Ctrl Pts',(1.99918721500645,5.06550989744515,10.4185353908046));
#23309=CARTESIAN_POINT('Ctrl Pts',(1.99999330286821,5.0327939101992,10.4183265055687));
#23310=CARTESIAN_POINT('Ctrl Pts',(1.99999329969225,5.,10.4183265058185));
#23311=CARTESIAN_POINT('Ctrl Pts',(2.,5.,10.4183332061262));
#23312=CARTESIAN_POINT('Ctrl Pts',(2.41562897926683,5.,10.833962185393));
#23313=CARTESIAN_POINT('Ctrl Pts',(3.59141650529373E-16,7.32295927629177,
-11.1000030851297));
#23314=CARTESIAN_POINT('Ctrl Pts',(-0.0395691838876551,7.32295990573061,
-11.1000032408218));
#23315=CARTESIAN_POINT('Ctrl Pts',(-0.0792480196814607,7.32202355274369,
-11.0997912002962));
#23316=CARTESIAN_POINT('Ctrl Pts',(-0.138851565118895,7.31919772571126,
-11.0991524396978));
#23317=CARTESIAN_POINT('Ctrl Pts',(-0.158753838675174,7.31801677199209,
-11.0988856072371));
#23318=CARTESIAN_POINT('Ctrl Pts',(-0.198581505665056,7.31517650523761,
-11.098244514889));
#23319=CARTESIAN_POINT('Ctrl Pts',(-0.218536420251613,7.31351371080974,
-11.0978694722481));
#23320=CARTESIAN_POINT('Ctrl Pts',(-0.278146117405925,7.30782774736753,
-11.0965886887918));
#23321=CARTESIAN_POINT('Ctrl Pts',(-0.317613541660884,7.30310818992191,
-11.0955274847949));
#23322=CARTESIAN_POINT('Ctrl Pts',(-0.39605519666046,7.29184182175108,-11.0930045053607));
#23323=CARTESIAN_POINT('Ctrl Pts',(-0.435022618201916,7.2852960959019,-11.0915429826038));
#23324=CARTESIAN_POINT('Ctrl Pts',(-0.551175423835523,7.26295715587163,
-11.0865811830642));
#23325=CARTESIAN_POINT('Ctrl Pts',(-0.627612884303839,7.24446796609068,
-11.0825036025914));
#23326=CARTESIAN_POINT('Ctrl Pts',(-0.740782815607558,7.21136052569271,
-11.0753211833526));
#23327=CARTESIAN_POINT('Ctrl Pts',(-0.778258017825594,7.19942761690082,
-11.0727493127705));
#23328=CARTESIAN_POINT('Ctrl Pts',(-0.852708576998866,7.17375101290638,
-11.0672648489048));
#23329=CARTESIAN_POINT('Ctrl Pts',(-0.889689399732524,7.16000413758078,
-11.0643515901889));
#23330=CARTESIAN_POINT('Ctrl Pts',(-0.963122271949541,7.13068279406864,
-11.0582018229929));
#23331=CARTESIAN_POINT('Ctrl Pts',(-0.999664283304993,7.11505987960465,
-11.0549556139893));
#23332=CARTESIAN_POINT('Ctrl Pts',(-1.07137816592919,7.08233580403699,-11.0482356814349));
#23333=CARTESIAN_POINT('Ctrl Pts',(-1.10671472204407,7.06517237057916,-11.0447487888929));
#23334=CARTESIAN_POINT('Ctrl Pts',(-1.17627149074728,7.02930781471142,-11.0375576578648));
#23335=CARTESIAN_POINT('Ctrl Pts',(-1.21050801027134,7.01060045520381,-11.0338520882294));
#23336=CARTESIAN_POINT('Ctrl Pts',(-1.27791136778758,6.97165130432156,-11.0262488851133));
#23337=CARTESIAN_POINT('Ctrl Pts',(-1.31107818901857,6.95140949202481,-11.022351230684));
#23338=CARTESIAN_POINT('Ctrl Pts',(-1.37634819184388,6.90939549569852,-11.0143914369154));
#23339=CARTESIAN_POINT('Ctrl Pts',(-1.40845137292374,6.88762331447492,-11.0103292771151));
#23340=CARTESIAN_POINT('Ctrl Pts',(-1.47159235053576,6.8425412193416,-11.0020680975225));
#23341=CARTESIAN_POINT('Ctrl Pts',(-1.50263016283063,6.81923133219222,-10.9978690567128));
#23342=CARTESIAN_POINT('Ctrl Pts',(-1.56363073599172,6.77105478122795,-10.9893621530921));
#23343=CARTESIAN_POINT('Ctrl Pts',(-1.59358047784877,6.74619913511913,-10.9850561672757));
#23344=CARTESIAN_POINT('Ctrl Pts',(-1.63772444238942,6.70769161663002,-10.9785315012905));
#23345=CARTESIAN_POINT('Ctrl Pts',(-1.65229673063601,6.69466048408886,-10.9763473205741));
#23346=CARTESIAN_POINT('Ctrl Pts',(-1.68100866985036,6.66834339584427,-10.9719867982326));
#23347=CARTESIAN_POINT('Ctrl Pts',(-1.69517895867899,6.65503220446354,-10.9698060775071));
#23348=CARTESIAN_POINT('Ctrl Pts',(-1.76501302384678,6.58778811663768,-10.9589227410546));
#23349=CARTESIAN_POINT('Ctrl Pts',(-1.81781525541685,6.53168602021943,-10.9502589641262));
#23350=CARTESIAN_POINT('Ctrl Pts',(-1.91736851011095,6.41498992816885,-10.9332668766608));
#23351=CARTESIAN_POINT('Ctrl Pts',(-1.96413203779847,6.35438957031199,-10.9249365463836));
#23352=CARTESIAN_POINT('Ctrl Pts',(-2.02973646447202,6.26007175633004,-10.9128704248536));
#23353=CARTESIAN_POINT('Ctrl Pts',(-2.05084657504034,6.2280620392678,-10.9089199119683));
#23354=CARTESIAN_POINT('Ctrl Pts',(-2.09152952892892,6.16288203805261,-10.9011930500009));
#23355=CARTESIAN_POINT('Ctrl Pts',(-2.11109336159131,6.1297281320993,-10.8974184538125));
#23356=CARTESIAN_POINT('Ctrl Pts',(-2.14868711090803,6.06216595808922,-10.8900683089525));
#23357=CARTESIAN_POINT('Ctrl Pts',(-2.16656540913263,6.02802490454898,-10.8865224179582));
#23358=CARTESIAN_POINT('Ctrl Pts',(-2.20043854820833,5.95918844731336,-10.8797263939069));
#23359=CARTESIAN_POINT('Ctrl Pts',(-2.21644946563092,5.92446397243587,-10.8764730840726));
#23360=CARTESIAN_POINT('Ctrl Pts',(-2.26173355722098,5.81939986438648,-10.867179507195));
#23361=CARTESIAN_POINT('Ctrl Pts',(-2.28827057824315,5.74815944124914,-10.861604149854));
#23362=CARTESIAN_POINT('Ctrl Pts',(-2.32262249161282,5.63950759674824,-10.8542913504755));
#23363=CARTESIAN_POINT('Ctrl Pts',(-2.33316279507002,5.6029910482451,-10.8520287182818));
#23364=CARTESIAN_POINT('Ctrl Pts',(-2.35240682804735,5.52935307013381,-10.8478734427179));
#23365=CARTESIAN_POINT('Ctrl Pts',(-2.3611106540472,5.4922316722176,-10.845980778159));
#23366=CARTESIAN_POINT('Ctrl Pts',(-2.37665232084687,5.41737336076027,-10.8425857820485));
#23367=CARTESIAN_POINT('Ctrl Pts',(-2.38349027560913,5.37963617118941,-10.8410834320379));
#23368=CARTESIAN_POINT('Ctrl Pts',(-2.39525550971482,5.30353201909676,-10.8384900627892));
#23369=CARTESIAN_POINT('Ctrl Pts',(-2.40013100120209,5.2655000511311,-10.837410515403));
#23370=CARTESIAN_POINT('Ctrl Pts',(-2.40791064220601,5.18947403914131,-10.8356846557461));
#23371=CARTESIAN_POINT('Ctrl Pts',(-2.41081468487305,5.1514802455297,-10.8350383575405));
#23372=CARTESIAN_POINT('Ctrl Pts',(-2.41467844117742,5.07553057246289,-10.8341779448215));
#23373=CARTESIAN_POINT('Ctrl Pts',(-2.41563806455839,5.03757469469925,-10.8339638311628));
#23374=CARTESIAN_POINT('Ctrl Pts',(-2.41561975408118,4.92376356609547,-10.833967947073));
#23375=CARTESIAN_POINT('Ctrl Pts',(-2.41174928755245,4.84795567679569,-10.8348331281171));
#23376=CARTESIAN_POINT('Ctrl Pts',(-2.40011491936355,4.7343846268852,-10.8374140583306));
#23377=CARTESIAN_POINT('Ctrl Pts',(-2.39525947699857,4.69653011768703,-10.8384891654576));
#23378=CARTESIAN_POINT('Ctrl Pts',(-2.38649876037944,4.63980636344301,-10.8404202936167));
#23379=CARTESIAN_POINT('Ctrl Pts',(-2.38332866809805,4.62089145846394,-10.8411178467378));
#23380=CARTESIAN_POINT('Ctrl Pts',(-2.37649388864143,4.58309623805945,-10.8426181569366));
#23381=CARTESIAN_POINT('Ctrl Pts',(-2.37282073446204,4.56417679276885,-10.843422759711));
#23382=CARTESIAN_POINT('Ctrl Pts',(-2.36109679154098,4.50769073244946,-10.8459838310384));
#23383=CARTESIAN_POINT('Ctrl Pts',(-2.35235033340462,4.47040395413937,-10.8478857353273));
#23384=CARTESIAN_POINT('Ctrl Pts',(-2.33301633666041,4.39647560359754,-10.8520602474027));
#23385=CARTESIAN_POINT('Ctrl Pts',(-2.32243189431414,4.35984750172526,-10.8543321744628));
#23386=CARTESIAN_POINT('Ctrl Pts',(-2.28796384475904,4.25095579577922,-10.8616689395862));
#23387=CARTESIAN_POINT('Ctrl Pts',(-2.26137136575613,4.17968274209439,-10.8672548790013));
#23388=CARTESIAN_POINT('Ctrl Pts',(-2.21608806072755,4.07473675640512,-10.8765467260252));
#23389=CARTESIAN_POINT('Ctrl Pts',(-2.2000930135488,4.04008256395551,-10.8797962235171));
#23390=CARTESIAN_POINT('Ctrl Pts',(-2.16628564461604,3.97143386483924,-10.8865780337264));
#23391=CARTESIAN_POINT('Ctrl Pts',(-2.14846743479671,3.93743084302305,-10.8901114717125));
#23392=CARTESIAN_POINT('Ctrl Pts',(-2.11100815043168,3.87012722042859,-10.897434898757));
#23393=CARTESIAN_POINT('Ctrl Pts',(-2.09129431600467,3.83672057611178,-10.9012383813503));
#23394=CARTESIAN_POINT('Ctrl Pts',(-2.05046094958217,3.77134095492018,-10.9089924865386));
#23395=CARTESIAN_POINT('Ctrl Pts',(-2.02926952283999,3.73923014273384,-10.9129573908145));
#23396=CARTESIAN_POINT('Ctrl Pts',(-1.98540346162804,3.67621926622253,-10.9210231443611));
#23397=CARTESIAN_POINT('Ctrl Pts',(-1.96272209651996,3.64530635015959,-10.92512534656));
#23398=CARTESIAN_POINT('Ctrl Pts',(-1.91587702393904,3.58465032601408,-10.9334375514149));
#23399=CARTESIAN_POINT('Ctrl Pts',(-1.89171329625648,3.5549072365286,-10.9376475756115));
#23400=CARTESIAN_POINT('Ctrl Pts',(-1.84190652454543,3.49658451455479,-10.9461451486341));
#23401=CARTESIAN_POINT('Ctrl Pts',(-1.81626348332508,3.46800488265077,-10.9504327184813));
#23402=CARTESIAN_POINT('Ctrl Pts',(-1.76349005078676,3.41201136675084,-10.9590552586289));
#23403=CARTESIAN_POINT('Ctrl Pts',(-1.7363596855068,3.38459746530546,-10.9633902505249));
#23404=CARTESIAN_POINT('Ctrl Pts',(-1.68059225573073,3.33094649266312,-10.972077285153));
#23405=CARTESIAN_POINT('Ctrl Pts',(-1.65195998582945,3.30471422081765,-10.976428573253));
#23406=CARTESIAN_POINT('Ctrl Pts',(-1.60784381620708,3.26624919219284,-10.9829473980705));
#23407=CARTESIAN_POINT('Ctrl Pts',(-1.59293142889825,3.25356637157806,-10.9851205633184));
#23408=CARTESIAN_POINT('Ctrl Pts',(-1.56287213526931,3.2286300328751,-10.9894373871103));
#23409=CARTESIAN_POINT('Ctrl Pts',(-1.54770701089334,3.21635854627108,-10.9915839288304));
#23410=CARTESIAN_POINT('Ctrl Pts',(-1.47124726535168,3.15602666933922,-11.0022410166242));
#23411=CARTESIAN_POINT('Ctrl Pts',(-1.40799822711262,3.11093266553086,-11.0105376568215));
#23412=CARTESIAN_POINT('Ctrl Pts',(-1.27743060091983,3.02697722307456,-11.0264485241274));
#23413=CARTESIAN_POINT('Ctrl Pts',(-1.21010900327941,2.98810844119082,-11.0340642433641));
#23414=CARTESIAN_POINT('Ctrl Pts',(-1.10603575631408,2.93449324692185,-11.0448165040961));
#23415=CARTESIAN_POINT('Ctrl Pts',(-1.07082872973356,2.91740410314997,-11.0482887604197));
#23416=CARTESIAN_POINT('Ctrl Pts',(-0.999365357715494,2.88481322043536,
-11.054982008906));
#23417=CARTESIAN_POINT('Ctrl Pts',(-0.963130129682714,2.8693200429042,-11.0582012189792));
#23418=CARTESIAN_POINT('Ctrl Pts',(-0.889500812844894,2.83992085997029,
-11.0643673298873));
#23419=CARTESIAN_POINT('Ctrl Pts',(-0.852281491609653,2.82609058473917,
-11.0672984223757));
#23420=CARTESIAN_POINT('Ctrl Pts',(-0.777480106558127,2.80031537803422,
-11.0728044734589));
#23421=CARTESIAN_POINT('Ctrl Pts',(-0.739808001792916,2.78833429109514,
-11.075387037792));
#23422=CARTESIAN_POINT('Ctrl Pts',(-0.626081142235231,2.75512486228593,
-11.0825926591987));
#23423=CARTESIAN_POINT('Ctrl Pts',(-0.549225020867577,2.73659502179654,
-11.0866800489708));
#23424=CARTESIAN_POINT('Ctrl Pts',(-0.432511795538508,2.714259073949,-11.0916421001459));
#23425=CARTESIAN_POINT('Ctrl Pts',(-0.39331219251049,2.7077195146796,-11.0931025310654));
#23426=CARTESIAN_POINT('Ctrl Pts',(-0.314496088528354,2.69649228340761,
-11.0956171788991));
#23427=CARTESIAN_POINT('Ctrl Pts',(-0.274695919596678,2.69178947522293,
-11.0966748018542));
#23428=CARTESIAN_POINT('Ctrl Pts',(-0.195299801987465,2.68432829145873,
-11.0983556871801));
#23429=CARTESIAN_POINT('Ctrl Pts',(-0.155652603752789,2.68155469534811,
-11.098982337027));
#23430=CARTESIAN_POINT('Ctrl Pts',(-0.0764579289352454,2.6778916390882,
-11.0998103951135));
#23431=CARTESIAN_POINT('Ctrl Pts',(-0.0369104896689312,2.67700143095427,
-11.1000119889358));
#23432=CARTESIAN_POINT('Ctrl Pts',(0.0815837784829221,2.67712330742632,
-11.0999843726987));
#23433=CARTESIAN_POINT('Ctrl Pts',(0.160382862315405,2.68092188458113,-11.0991228019287));
#23434=CARTESIAN_POINT('Ctrl Pts',(0.278286104013499,2.69219436339788,-11.0965837446232));
#23435=CARTESIAN_POINT('Ctrl Pts',(0.317537877518113,2.69688246104062,-11.0955295843832));
#23436=CARTESIAN_POINT('Ctrl Pts',(0.395941801212285,2.70814037681139,-11.0930084858397));
#23437=CARTESIAN_POINT('Ctrl Pts',(0.435094106484223,2.71471078980386,-11.0915413949138));
#23438=CARTESIAN_POINT('Ctrl Pts',(0.493746116159599,2.72600132427696,-11.0890336930226));
#23439=CARTESIAN_POINT('Ctrl Pts',(0.513309517811984,2.73001078199123,-11.0881451501855));
#23440=CARTESIAN_POINT('Ctrl Pts',(0.552256455133781,2.73847997335676,-11.086273564099));
#23441=CARTESIAN_POINT('Ctrl Pts',(0.571634753907634,2.74293742472352,-11.0852910185488));
#23442=CARTESIAN_POINT('Ctrl Pts',(0.629455063331992,2.75696591963619,-11.0822083735072));
#23443=CARTESIAN_POINT('Ctrl Pts',(0.667657542074438,2.76720614779721,-11.0799702944701));
#23444=CARTESIAN_POINT('Ctrl Pts',(0.781046169005456,2.80050386894502,-11.0727487414743));
#23445=CARTESIAN_POINT('Ctrl Pts',(0.855193468192384,2.82616680184042,-11.0672503698462));
#23446=CARTESIAN_POINT('Ctrl Pts',(0.964189026966947,2.86977153157994,-11.0581074024243));
#23447=CARTESIAN_POINT('Ctrl Pts',(1.00015468304478,2.88516068993715,-11.0549101944511));
#23448=CARTESIAN_POINT('Ctrl Pts',(1.07135197113703,2.91765546259803,-11.0482376006944));
#23449=CARTESIAN_POINT('Ctrl Pts',(1.1065836303793,2.93476100614121,-11.0447621885171));
#23450=CARTESIAN_POINT('Ctrl Pts',(1.17630609820376,2.97070906114556,-11.0375542330585));
#23451=CARTESIAN_POINT('Ctrl Pts',(1.2107826338078,2.98954328771685,-11.0338232927107));
#23452=CARTESIAN_POINT('Ctrl Pts',(1.27903955187267,3.02901587879235,-11.0261193965257));
#23453=CARTESIAN_POINT('Ctrl Pts',(1.31254945725883,3.04950014064211,-11.0221767713055));
#23454=CARTESIAN_POINT('Ctrl Pts',(1.37823901392251,3.09186099485949,-11.0141556229233));
#23455=CARTESIAN_POINT('Ctrl Pts',(1.41044151771734,3.11375084020812,-11.0100745081484));
#23456=CARTESIAN_POINT('Ctrl Pts',(1.47357760128402,3.15892606381394,-11.0018023721546));
#23457=CARTESIAN_POINT('Ctrl Pts',(1.50451216341957,3.1822121184455,-10.9976111942887));
#23458=CARTESIAN_POINT('Ctrl Pts',(1.59543396737852,3.2541520184694,-10.9849174124688));
#23459=CARTESIAN_POINT('Ctrl Pts',(1.65354585178342,3.3048853736236,-10.9762937510806));
#23460=CARTESIAN_POINT('Ctrl Pts',(1.73693817902585,3.38517496114059,-10.9632984167516));
#23461=CARTESIAN_POINT('Ctrl Pts',(1.76411205328141,3.41264540788295,-10.9589554791838));
#23462=CARTESIAN_POINT('Ctrl Pts',(1.81716937117498,3.46899272703761,-10.9502828043387));
#23463=CARTESIAN_POINT('Ctrl Pts',(1.84309667555061,3.49792107129187,-10.9459455511756));
#23464=CARTESIAN_POINT('Ctrl Pts',(1.89350371089981,3.55706432478315,-10.9373384473274));
#23465=CARTESIAN_POINT('Ctrl Pts',(1.91782002726333,3.58708091253443,-10.9330970558847));
#23466=CARTESIAN_POINT('Ctrl Pts',(1.96480545503627,3.64809681086166,-10.9247510204171));
#23467=CARTESIAN_POINT('Ctrl Pts',(1.98745910955116,3.67907795866426,-10.9206489900008));
#23468=CARTESIAN_POINT('Ctrl Pts',(2.05293600252221,3.77342700143773,-10.9085975966294));
#23469=CARTESIAN_POINT('Ctrl Pts',(2.09328053962265,3.83819748311837,-10.900902625416));
#23470=CARTESIAN_POINT('Ctrl Pts',(2.16737993193662,3.97149066954996,-10.8864120662151));
#23471=CARTESIAN_POINT('Ctrl Pts',(2.20113579376919,4.04002624499109,-10.8796157428706));
#23472=CARTESIAN_POINT('Ctrl Pts',(2.23910046262614,4.12808394712988,-10.8718244935691));
#23473=CARTESIAN_POINT('Ctrl Pts',(2.24648332267895,4.14582775641521,-10.8703010264556));
#23474=CARTESIAN_POINT('Ctrl Pts',(2.26081365706442,4.18153720245236,-10.8673296459906));
#23475=CARTESIAN_POINT('Ctrl Pts',(2.26777396396924,4.19954109715767,-10.865879022026));
#23476=CARTESIAN_POINT('Ctrl Pts',(2.28791485853621,4.25368668331467,-10.8616624914817));
#23477=CARTESIAN_POINT('Ctrl Pts',(2.30035376619681,4.28993814494949,-10.8590326047595));
#23478=CARTESIAN_POINT('Ctrl Pts',(2.32332083291499,4.36282874497073,-10.8541419345693));
#23479=CARTESIAN_POINT('Ctrl Pts',(2.33384408929083,4.39945372831524,-10.8518821742987));
#23480=CARTESIAN_POINT('Ctrl Pts',(2.35299205151236,4.4730596002693,-10.8477464746504));
#23481=CARTESIAN_POINT('Ctrl Pts',(2.36161668196543,4.51004050194072,-10.8458705231367));
#23482=CARTESIAN_POINT('Ctrl Pts',(2.38465480161393,4.62151562385937,-10.840837088678));
#23483=CARTESIAN_POINT('Ctrl Pts',(2.39623906502688,4.6965614004445,-10.8382739242991));
#23484=CARTESIAN_POINT('Ctrl Pts',(2.40787690299187,4.81014885074317,-10.8356921356679));
#23485=CARTESIAN_POINT('Ctrl Pts',(2.41079816467738,4.84822416052067,-10.8350420382505));
#23486=CARTESIAN_POINT('Ctrl Pts',(2.41371723344945,4.90556045584082,-10.8343919934576));
#23487=CARTESIAN_POINT('Ctrl Pts',(2.41444610176836,4.92472893436486,-10.8342295549678));
#23488=CARTESIAN_POINT('Ctrl Pts',(2.41541087362559,4.96315380364675,-10.8340145074147));
#23489=CARTESIAN_POINT('Ctrl Pts',(2.4156455512877,4.98241110455632,-10.8339621722294));
#23490=CARTESIAN_POINT('Ctrl Pts',(2.41560313911598,5.03999264903484,-10.833971630943));
#23491=CARTESIAN_POINT('Ctrl Pts',(2.4145875281457,5.07822847892658,-10.834198215873));
#23492=CARTESIAN_POINT('Ctrl Pts',(2.41061596210125,5.15440587986219,-10.835082583));
#23493=CARTESIAN_POINT('Ctrl Pts',(2.40766058078035,5.19234684080988,-10.8357402188351));
#23494=CARTESIAN_POINT('Ctrl Pts',(2.39592148041045,5.30573219765167,-10.8383441805306));
#23495=CARTESIAN_POINT('Ctrl Pts',(2.38427095852029,5.38073995810597,-10.8409216799096));
#23496=CARTESIAN_POINT('Ctrl Pts',(2.36107290737889,5.49238191222086,-10.8459889485252));
#23497=CARTESIAN_POINT('Ctrl Pts',(2.35238494926879,5.52945072166158,-10.8478782167291));
#23498=CARTESIAN_POINT('Ctrl Pts',(2.33307955313958,5.60329556878828,-10.8520466422376));
#23499=CARTESIAN_POINT('Ctrl Pts',(2.32246088539331,5.64007259006972,-10.8543260677788));
#23500=CARTESIAN_POINT('Ctrl Pts',(2.29926633375405,5.71332551677146,-10.8592630609384));
#23501=CARTESIAN_POINT('Ctrl Pts',(2.28665985543623,5.7498592815894,-10.8619268242372));
#23502=CARTESIAN_POINT('Ctrl Pts',(2.25978404179862,5.82174961553897,-10.8675499732185));
#23503=CARTESIAN_POINT('Ctrl Pts',(2.24546305066682,5.85727787033199,-10.8705204036662));
#23504=CARTESIAN_POINT('Ctrl Pts',(2.21511805933157,5.92741325183323,-10.8767444511339));
#23505=CARTESIAN_POINT('Ctrl Pts',(2.19908867693094,5.96203795192665,-10.8799992263874));
#23506=CARTESIAN_POINT('Ctrl Pts',(2.1653338515937,6.03041285824769,-10.8867673422212));
#23507=CARTESIAN_POINT('Ctrl Pts',(2.14760838564802,6.0641630512634,-10.8902807001735));
#23508=CARTESIAN_POINT('Ctrl Pts',(2.110466257554,6.13079395130041,-10.8975395078308));
#23509=CARTESIAN_POINT('Ctrl Pts',(2.09104959843572,6.16367465819078,-10.9012849744881));
#23510=CARTESIAN_POINT('Ctrl Pts',(2.05051737516466,6.2285652853405,-10.9089816490723));
#23511=CARTESIAN_POINT('Ctrl Pts',(2.02940184035635,6.26057521860074,-10.9129328744282));
#23512=CARTESIAN_POINT('Ctrl Pts',(1.98545129698501,6.32371657530621,-10.9210145348477));
#23513=CARTESIAN_POINT('Ctrl Pts',(1.96262998828763,6.35483019777428,-10.9251425458962));
#23514=CARTESIAN_POINT('Ctrl Pts',(1.91517913008013,6.41623574499544,-10.9335605156211));
#23515=CARTESIAN_POINT('Ctrl Pts',(1.89071033352914,6.44631744271524,-10.9378216781217));
#23516=CARTESIAN_POINT('Ctrl Pts',(1.8153924592825,6.53435906734782,-10.950662557146));
#23517=CARTESIAN_POINT('Ctrl Pts',(1.76248430705585,6.5903627060743,-10.9593285423635));
#23518=CARTESIAN_POINT('Ctrl Pts',(1.65143685751177,6.69700650572329,-10.9766108908935));
#23519=CARTESIAN_POINT('Ctrl Pts',(1.593287021374,6.74766692004806,-10.9852300851391));
#23520=CARTESIAN_POINT('Ctrl Pts',(1.47167902435032,6.84364147053686,-11.0021816610453));
#23521=CARTESIAN_POINT('Ctrl Pts',(1.40820021283237,6.88897017522776,-11.010517190463));
#23522=CARTESIAN_POINT('Ctrl Pts',(1.27579527666471,6.9740412210718,-11.0266436095859));
#23523=CARTESIAN_POINT('Ctrl Pts',(1.20797645046747,7.01307704737157,-11.0342982898015));
#23524=CARTESIAN_POINT('Ctrl Pts',(1.06908784663473,7.08445147588905,-11.048619592373));
#23525=CARTESIAN_POINT('Ctrl Pts',(0.998035979663791,7.11677742070683,-11.0552843505145));
#23526=CARTESIAN_POINT('Ctrl Pts',(0.852713243143896,7.17473256025119,-11.0674417000716));
#23527=CARTESIAN_POINT('Ctrl Pts',(0.778416648026101,7.20036362544414,-11.0729351492412));
#23528=CARTESIAN_POINT('Ctrl Pts',(0.664562228432768,7.23365210234308,-11.0801573497189));
#23529=CARTESIAN_POINT('Ctrl Pts',(0.626133503253441,7.24389773727957,-11.0823974328985));
#23530=CARTESIAN_POINT('Ctrl Pts',(0.548614559546499,7.26258443636509,-11.0865051926693));
#23531=CARTESIAN_POINT('Ctrl Pts',(0.509814499361565,7.2709566045556,-11.0883576190884));
#23532=CARTESIAN_POINT('Ctrl Pts',(0.431999673116113,7.28582934008303,-11.0916618070167));
#23533=CARTESIAN_POINT('Ctrl Pts',(0.393007691850147,7.29232444025252,-11.0931123766216));
#23534=CARTESIAN_POINT('Ctrl Pts',(0.314856544245277,7.30345579210369,-11.0956055483394));
#23535=CARTESIAN_POINT('Ctrl Pts',(0.275697371158881,7.30809196402797,-11.0966481564864));
#23536=CARTESIAN_POINT('Ctrl Pts',(0.157970235931856,7.3192272426051,-11.0991565661922));
#23537=CARTESIAN_POINT('Ctrl Pts',(0.0791383677753115,7.32295801741409,
-11.1000027737453));
#23538=CARTESIAN_POINT('Ctrl Pts',(3.59141650529373E-16,7.32295927629177,
-11.1000030851297));
#23539=CARTESIAN_POINT('Ctrl Pts',(4.03188655311423E-16,6.99999286992453,
-10.674155471012));
#23540=CARTESIAN_POINT('Ctrl Pts',(-0.0327607868253891,6.99999341185104,
-10.6741556207311));
#23541=CARTESIAN_POINT('Ctrl Pts',(-0.0656123585070314,6.9991872421877,
-10.6739517150638));
#23542=CARTESIAN_POINT('Ctrl Pts',(-0.114960332214575,6.99675429643007,
-10.6733374602853));
#23543=CARTESIAN_POINT('Ctrl Pts',(-0.131438158574352,6.99573753344068,
-10.6730808647556));
#23544=CARTESIAN_POINT('Ctrl Pts',(-0.164412953093731,6.99329215554895,
-10.6724643676842));
#23545=CARTESIAN_POINT('Ctrl Pts',(-0.180934362904284,6.99186054328014,
-10.6721037134189));
#23546=CARTESIAN_POINT('Ctrl Pts',(-0.230287429844603,6.98696511249956,
-10.670872066758));
#23547=CARTESIAN_POINT('Ctrl Pts',(-0.262963966116202,6.98290172605249,
-10.6698515754695));
#23548=CARTESIAN_POINT('Ctrl Pts',(-0.327908705561348,6.97320174713271,
-10.6674253892312));
#23549=CARTESIAN_POINT('Ctrl Pts',(-0.360171271143761,6.96756608870329,
-10.6660199372677));
#23550=CARTESIAN_POINT('Ctrl Pts',(-0.456338463152356,6.94833298322491,
-10.6612484953774));
#23551=CARTESIAN_POINT('Ctrl Pts',(-0.519623856019679,6.93241438830641,
-10.6573273498086));
#23552=CARTESIAN_POINT('Ctrl Pts',(-0.613321416348892,6.90390995199787,
-10.6504204814928));
#23553=CARTESIAN_POINT('Ctrl Pts',(-0.64434851851395,6.89363610314287,-10.6479472797978));
#23554=CARTESIAN_POINT('Ctrl Pts',(-0.705988882515448,6.87152937684899,
-10.6426732254099));
#23555=CARTESIAN_POINT('Ctrl Pts',(-0.736606669670444,6.85969376142734,
-10.6398717328137));
#23556=CARTESIAN_POINT('Ctrl Pts',(-0.797404453105115,6.83444903218893,
-10.6339578992176));
#23557=CARTESIAN_POINT('Ctrl Pts',(-0.827658932134272,6.82099820769395,
-10.6308362298514));
#23558=CARTESIAN_POINT('Ctrl Pts',(-0.887033500681286,6.7928238361157,-10.6243741050852));
#23559=CARTESIAN_POINT('Ctrl Pts',(-0.916289938854812,6.77804667454909,
-10.6210209859178));
#23560=CARTESIAN_POINT('Ctrl Pts',(-0.973878553221769,6.74716845091829,
-10.6141057400374));
#23561=CARTESIAN_POINT('Ctrl Pts',(-1.00222423052815,6.73106201891487,-10.6105423332443));
#23562=CARTESIAN_POINT('Ctrl Pts',(-1.0580299563462,6.69752805865601,-10.603230824273));
#23563=CARTESIAN_POINT('Ctrl Pts',(-1.0854899909806,6.6801005123873,-10.5994827019498));
#23564=CARTESIAN_POINT('Ctrl Pts',(-1.13952943376257,6.64392781924231,-10.5918282827977));
#23565=CARTESIAN_POINT('Ctrl Pts',(-1.16610884148417,6.62518267478179,-10.5879219662928));
#23566=CARTESIAN_POINT('Ctrl Pts',(-1.2183855857643,6.58636844771034,-10.5799777238751));
#23567=CARTESIAN_POINT('Ctrl Pts',(-1.24408293537336,6.56629938813905,-10.5759397777512));
#23568=CARTESIAN_POINT('Ctrl Pts',(-1.2945875598611,6.52482093459518,-10.5677592384192));
#23569=CARTESIAN_POINT('Ctrl Pts',(-1.31938405582187,6.50342102651133,-10.5636184501953));
#23570=CARTESIAN_POINT('Ctrl Pts',(-1.35593247228738,6.47026729747152,-10.5573441006669));
#23571=CARTESIAN_POINT('Ctrl Pts',(-1.3679974072164,6.4590479134576,-10.5552437152558));
#23572=CARTESIAN_POINT('Ctrl Pts',(-1.39176908071372,6.43638975092178,-10.5510504827809));
#23573=CARTESIAN_POINT('Ctrl Pts',(-1.40350118549718,6.42492924529715,-10.5489534246192));
#23574=CARTESIAN_POINT('Ctrl Pts',(-1.46131938383472,6.36703425868757,-10.5384876234438));
#23575=CARTESIAN_POINT('Ctrl Pts',(-1.50503629892909,6.31873216662301,-10.5301562291917));
#23576=CARTESIAN_POINT('Ctrl Pts',(-1.58746011044886,6.21826060242907,-10.5138160370322));
#23577=CARTESIAN_POINT('Ctrl Pts',(-1.6261773598651,6.16608565262814,-10.5058052968709));
#23578=CARTESIAN_POINT('Ctrl Pts',(-1.68049368448563,6.08488106269207,-10.4942020877408));
#23579=CARTESIAN_POINT('Ctrl Pts',(-1.6979715236584,6.05732173070268,-10.4904031348571));
#23580=CARTESIAN_POINT('Ctrl Pts',(-1.73165444174784,6.00120385596309,-10.4829727111617));
#23581=CARTESIAN_POINT('Ctrl Pts',(-1.74785206040866,5.97265941431339,-10.4793429259945));
#23582=CARTESIAN_POINT('Ctrl Pts',(-1.7789773120897,5.91449056577787,-10.4722747667905));
#23583=CARTESIAN_POINT('Ctrl Pts',(-1.79377941461961,5.88509622195569,-10.468864912625));
#23584=CARTESIAN_POINT('Ctrl Pts',(-1.82182423584976,5.82583025674177,-10.4623296155848));
#23585=CARTESIAN_POINT('Ctrl Pts',(-1.83508026493665,5.79593360600127,-10.4592011178087));
#23586=CARTESIAN_POINT('Ctrl Pts',(-1.87257263463879,5.70547680414255,-10.4502640856555));
#23587=CARTESIAN_POINT('Ctrl Pts',(-1.89454361314491,5.64414110197029,-10.4449026248875));
#23588=CARTESIAN_POINT('Ctrl Pts',(-1.92298482927188,5.55059537496581,-10.4378703784192));
#23589=CARTESIAN_POINT('Ctrl Pts',(-1.93171153527669,5.51915580674477,-10.4356945512933));
#23590=CARTESIAN_POINT('Ctrl Pts',(-1.94764437998263,5.45575588721916,-10.4316986913775));
#23591=CARTESIAN_POINT('Ctrl Pts',(-1.95485059856305,5.42379556319981,-10.4298786382116));
#23592=CARTESIAN_POINT('Ctrl Pts',(-1.96771811775107,5.35934497609858,-10.4266138899021));
#23593=CARTESIAN_POINT('Ctrl Pts',(-1.9733795127124,5.32685447536398,-10.4251691770077));
#23594=CARTESIAN_POINT('Ctrl Pts',(-1.98312038398174,5.26133125973539,-10.4226753014347));
#23595=CARTESIAN_POINT('Ctrl Pts',(-1.98715698321348,5.22858696432873,-10.4216371704946));
#23596=CARTESIAN_POINT('Ctrl Pts',(-1.99359803494776,5.16313102480355,-10.4199775228208));
#23597=CARTESIAN_POINT('Ctrl Pts',(-1.99600239898559,5.13041959628215,-10.4193560196127));
#23598=CARTESIAN_POINT('Ctrl Pts',(-1.9992013453422,5.06502938210275,-10.4185286163173));
#23599=CARTESIAN_POINT('Ctrl Pts',(-1.99999585293441,5.03235059790058,-10.4183227170519));
#23600=CARTESIAN_POINT('Ctrl Pts',(-1.99998069301495,4.93436289400731,-10.4183266750566));
#23601=CARTESIAN_POINT('Ctrl Pts',(-1.99677619101608,4.86909475106813,-10.4191586637422));
#23602=CARTESIAN_POINT('Ctrl Pts',(-1.98714366846619,4.77131374717008,-10.4216405774991));
#23603=CARTESIAN_POINT('Ctrl Pts',(-1.98312366864227,4.7387222380274,-10.422674438529));
#23604=CARTESIAN_POINT('Ctrl Pts',(-1.97587034821981,4.68988491866461,-10.4245314796529));
#23605=CARTESIAN_POINT('Ctrl Pts',(-1.97324571189318,4.67359979671702,-10.4252022714002));
#23606=CARTESIAN_POINT('Ctrl Pts',(-1.96758694588452,4.64105933331006,-10.4266450227394));
#23607=CARTESIAN_POINT('Ctrl Pts',(-1.96454580605742,4.62477030230104,-10.4274187572186));
#23608=CARTESIAN_POINT('Ctrl Pts',(-1.95483912128284,4.57613762972611,-10.4298815739684));
#23609=CARTESIAN_POINT('Ctrl Pts',(-1.94759760598414,4.5440349185319,-10.4317105123853));
#23610=CARTESIAN_POINT('Ctrl Pts',(-1.93159027695736,4.480384997727,-10.4357248708109));
#23611=CARTESIAN_POINT('Ctrl Pts',(-1.92282702673824,4.44884938566002,-10.437909636209));
#23612=CARTESIAN_POINT('Ctrl Pts',(-1.89428965717975,4.35509714570243,-10.444964928985));
#23613=CARTESIAN_POINT('Ctrl Pts',(-1.87227276296581,4.29373334968308,-10.4503365658497));
#23614=CARTESIAN_POINT('Ctrl Pts',(-1.83478104448698,4.20337824735948,-10.4592719345143));
#23615=CARTESIAN_POINT('Ctrl Pts',(-1.8215381549603,4.17354210751817,-10.4623967662073));
#23616=CARTESIAN_POINT('Ctrl Pts',(-1.79354778725739,4.11443779597759,-10.4689183947143));
#23617=CARTESIAN_POINT('Ctrl Pts',(-1.77879543413435,4.08516229300892,-10.4723162736268));
#23618=CARTESIAN_POINT('Ctrl Pts',(-1.74778151094684,4.02721604888781,-10.4793587400345));
#23619=CARTESIAN_POINT('Ctrl Pts',(-1.73145970029198,3.99845400767373,-10.4830163033902));
#23620=CARTESIAN_POINT('Ctrl Pts',(-1.69765225011823,3.94216426658589,-10.4904729251302));
#23621=CARTESIAN_POINT('Ctrl Pts',(-1.68010708628575,3.91451789496137,-10.4942857172838));
#23622=CARTESIAN_POINT('Ctrl Pts',(-1.64378875623639,3.86026756649618,-10.5020420311054));
#23623=CARTESIAN_POINT('Ctrl Pts',(-1.62501001747555,3.83365254472388,-10.5059868537968));
#23624=CARTESIAN_POINT('Ctrl Pts',(-1.58622525403486,3.78142966804803,-10.513980163911));
#23625=CARTESIAN_POINT('Ctrl Pts',(-1.56621921262261,3.75582182915573,-10.5180286720479));
#23626=CARTESIAN_POINT('Ctrl Pts',(-1.52498234923167,3.70560785024849,-10.526200238747));
#23627=CARTESIAN_POINT('Ctrl Pts',(-1.50375152957793,3.68100171073647,-10.5303233175237));
#23628=CARTESIAN_POINT('Ctrl Pts',(-1.46005845826469,3.63279310298997,-10.5386150570291));
#23629=CARTESIAN_POINT('Ctrl Pts',(-1.43759622816299,3.60919061973207,-10.5427837385248));
#23630=CARTESIAN_POINT('Ctrl Pts',(-1.39142431610491,3.56299886603047,-10.5511374982031));
#23631=CARTESIAN_POINT('Ctrl Pts',(-1.36771860377042,3.54041372767345,-10.5553218507049));
#23632=CARTESIAN_POINT('Ctrl Pts',(-1.33119319974296,3.5072965810337,-10.5615905831599));
#23633=CARTESIAN_POINT('Ctrl Pts',(-1.31884668425598,3.49637708233266,-10.563680375707));
#23634=CARTESIAN_POINT('Ctrl Pts',(-1.29395948634249,3.47490770053292,-10.5678315861114));
#23635=CARTESIAN_POINT('Ctrl Pts',(-1.28140372051583,3.46434234712297,-10.5698957765327));
#23636=CARTESIAN_POINT('Ctrl Pts',(-1.21809987701117,3.41239855072201,-10.580144008998));
#23637=CARTESIAN_POINT('Ctrl Pts',(-1.16573366535366,3.37357407066731,-10.5881223515868));
#23638=CARTESIAN_POINT('Ctrl Pts',(-1.05763191172308,3.30129114775118,-10.6034228042084));
#23639=CARTESIAN_POINT('Ctrl Pts',(-1.00189387792299,3.26782638260352,-10.6107463491238));
#23640=CARTESIAN_POINT('Ctrl Pts',(-0.915727798083462,3.2216654329248,-10.6210861032517));
#23641=CARTESIAN_POINT('Ctrl Pts',(-0.886578602188769,3.20695223237699,
-10.624425147714));
#23642=CARTESIAN_POINT('Ctrl Pts',(-0.827411440613592,3.17889253554151,
-10.6308616121367));
#23643=CARTESIAN_POINT('Ctrl Pts',(-0.797410958811738,3.16555341035283,
-10.6339573183767));
#23644=CARTESIAN_POINT('Ctrl Pts',(-0.73645053163076,3.14024166388806,-10.6398868686641));
#23645=CARTESIAN_POINT('Ctrl Pts',(-0.705635282768996,3.12833424384263,
-10.6427055108466));
#23646=CARTESIAN_POINT('Ctrl Pts',(-0.643704457082796,3.10614262380134,
-10.6480003242663));
#23647=CARTESIAN_POINT('Ctrl Pts',(-0.612514332036124,3.09582729511847,
-10.6504838094504));
#23648=CARTESIAN_POINT('Ctrl Pts',(-0.518355670264217,3.06723505008393,
-10.6574129897912));
#23649=CARTESIAN_POINT('Ctrl Pts',(-0.454723652597518,3.05128145621922,
-10.661343568329));
#23650=CARTESIAN_POINT('Ctrl Pts',(-0.358092468449763,3.03205092691298,
-10.666115252201));
#23651=CARTESIAN_POINT('Ctrl Pts',(-0.325637671252416,3.02642057770976,
-10.6675196542151));
#23652=CARTESIAN_POINT('Ctrl Pts',(-0.260382911681688,3.01675429439487,
-10.6699378284918));
#23653=CARTESIAN_POINT('Ctrl Pts',(-0.227430883820392,3.01270532852036,
-10.6709548761238));
#23654=CARTESIAN_POINT('Ctrl Pts',(-0.161695909574891,3.00628149040917,
-10.6725712748905));
#23655=CARTESIAN_POINT('Ctrl Pts',(-0.128870531795076,3.00389351378737,
-10.6731738835421));
#23656=CARTESIAN_POINT('Ctrl Pts',(-0.0633023394679634,3.00073974072009,
-10.6739701734787));
#23657=CARTESIAN_POINT('Ctrl Pts',(-0.0305595558175949,2.99997330028406,
-10.6741640332268));
#23658=CARTESIAN_POINT('Ctrl Pts',(0.067546219373333,3.00007823198808,-10.6741374764767));
#23659=CARTESIAN_POINT('Ctrl Pts',(0.132786887330565,3.0033486841664,-10.6733089595586));
#23660=CARTESIAN_POINT('Ctrl Pts',(0.230403329920755,3.01305392415495,-10.6708673122705));
#23661=CARTESIAN_POINT('Ctrl Pts',(0.262901320981579,3.0170902247284,-10.6698535945079));
#23662=CARTESIAN_POINT('Ctrl Pts',(0.327814821287288,3.0267829264048,-10.6674292170005));
#23663=CARTESIAN_POINT('Ctrl Pts',(0.360230458929732,3.0324398396669,-10.6660184104888));
#23664=CARTESIAN_POINT('Ctrl Pts',(0.408790621082765,3.04216062499209,-10.663606915676));
#23665=CARTESIAN_POINT('Ctrl Pts',(0.42498788289436,3.04561263851753,-10.6627524614643));
#23666=CARTESIAN_POINT('Ctrl Pts',(0.45723348883632,3.0529043385994,-10.6609526781029));
#23667=CARTESIAN_POINT('Ctrl Pts',(0.473277497147183,3.05674206018251,-10.6600078275582));
#23668=CARTESIAN_POINT('Ctrl Pts',(0.521149063986236,3.06882014096848,-10.6570434470816));
#23669=CARTESIAN_POINT('Ctrl Pts',(0.552778305210063,3.07763664649945,-10.6548912311395));
#23670=CARTESIAN_POINT('Ctrl Pts',(0.646656931716427,3.10630490838491,-10.6479467304191));
#23671=CARTESIAN_POINT('Ctrl Pts',(0.708046215587488,3.12839986430357,-10.6426593018352));
#23672=CARTESIAN_POINT('Ctrl Pts',(0.798287658930455,3.16594212751282,-10.6338671010601));
#23673=CARTESIAN_POINT('Ctrl Pts',(0.828064952167477,3.17919169555405,-10.6307925528174));
#23674=CARTESIAN_POINT('Ctrl Pts',(0.887011813046133,3.20716864473898,-10.6243759507131));
#23675=CARTESIAN_POINT('Ctrl Pts',(0.916181403230322,3.22189596496015,-10.6210338714703));
#23676=CARTESIAN_POINT('Ctrl Pts',(0.973907206011464,3.25284607864923,-10.6141024466226));
#23677=CARTESIAN_POINT('Ctrl Pts',(1.0024516014833,3.2690617390947,-10.6105146424553));
#23678=CARTESIAN_POINT('Ctrl Pts',(1.05896402156259,3.3030463644449,-10.6031063034683));
#23679=CARTESIAN_POINT('Ctrl Pts',(1.08670810822353,3.3206826519439,-10.5993149356424));
#23680=CARTESIAN_POINT('Ctrl Pts',(1.14109491510325,3.35715397852438,-10.5916015157244));
#23681=CARTESIAN_POINT('Ctrl Pts',(1.16775655576403,3.37600042799412,-10.5876769714456));
#23682=CARTESIAN_POINT('Ctrl Pts',(1.22002924808351,3.41489483567103,-10.579722192965));
#23683=CARTESIAN_POINT('Ctrl Pts',(1.24564111307727,3.43494337621453,-10.575691808126));
#23684=CARTESIAN_POINT('Ctrl Pts',(1.3209186281685,3.4968813053809,-10.5634850186665));
#23685=CARTESIAN_POINT('Ctrl Pts',(1.36903160068738,3.54056108470851,-10.5551922009365));
#23686=CARTESIAN_POINT('Ctrl Pts',(1.43807518428478,3.60968782498416,-10.542695427921));
#23687=CARTESIAN_POINT('Ctrl Pts',(1.46057343707218,3.63333899191555,-10.5385191055863));
#23688=CARTESIAN_POINT('Ctrl Pts',(1.50450154754197,3.68185221283114,-10.5301791547831));
#23689=CARTESIAN_POINT('Ctrl Pts',(1.52596771914682,3.70675858240798,-10.526008298773));
#23690=CARTESIAN_POINT('Ctrl Pts',(1.56770156294414,3.75767901243609,-10.5177314033589));
#23691=CARTESIAN_POINT('Ctrl Pts',(1.58783393815349,3.78352232449705,-10.5136527313689));
#23692=CARTESIAN_POINT('Ctrl Pts',(1.62673490683457,3.83605504121403,-10.5056268885413));
#23693=CARTESIAN_POINT('Ctrl Pts',(1.64549070297335,3.86272880830937,-10.501682231042));
#23694=CARTESIAN_POINT('Ctrl Pts',(1.69970143773757,3.94396028522575,-10.49009318503));
#23695=CARTESIAN_POINT('Ctrl Pts',(1.73310416808659,3.99972557688104,-10.4826934286111));
#23696=CARTESIAN_POINT('Ctrl Pts',(1.79445378809172,4.11448670299691,-10.4687587944868));
#23697=CARTESIAN_POINT('Ctrl Pts',(1.8224015111697,4.17349361871624,-10.462223209635));
#23698=CARTESIAN_POINT('Ctrl Pts',(1.85383386081593,4.24930845464478,-10.4547308688031));
#23699=CARTESIAN_POINT('Ctrl Pts',(1.85994640296646,4.26458530104584,-10.4532658489556));
#23700=CARTESIAN_POINT('Ctrl Pts',(1.87181101536952,4.29532998012479,-10.4504084644303));
#23701=CARTESIAN_POINT('Ctrl Pts',(1.87757371018256,4.31083075166611,-10.4490134931308));
#23702=CARTESIAN_POINT('Ctrl Pts',(1.89424909967874,4.35744835162015,-10.4449587282598));
#23703=CARTESIAN_POINT('Ctrl Pts',(1.90454773013222,4.3886596886135,-10.442429736193));
#23704=CARTESIAN_POINT('Ctrl Pts',(1.92356301179397,4.45141613975527,-10.4377266948003));
#23705=CARTESIAN_POINT('Ctrl Pts',(1.93227560389121,4.4829490668702,-10.4355536294173));
#23706=CARTESIAN_POINT('Ctrl Pts',(1.94812890807492,4.54632134403188,-10.4315765943941));
#23707=CARTESIAN_POINT('Ctrl Pts',(1.95526955774118,4.57816070532523,-10.4297726130834));
#23708=CARTESIAN_POINT('Ctrl Pts',(1.97434366674437,4.67413718295142,-10.424932284522));
#23709=CARTESIAN_POINT('Ctrl Pts',(1.98393470570248,4.7387491714715,-10.4224674550198));
#23710=CARTESIAN_POINT('Ctrl Pts',(1.99357010100791,4.836544295573,-10.4199847157782));
#23711=CARTESIAN_POINT('Ctrl Pts',(1.99598872130629,4.86932590687989,-10.4193595591137));
#23712=CARTESIAN_POINT('Ctrl Pts',(1.99840552601066,4.91869060431424,-10.4187344530547));
#23713=CARTESIAN_POINT('Ctrl Pts',(1.99900898297575,4.93519404488994,-10.4185782464589));
#23714=CARTESIAN_POINT('Ctrl Pts',(1.99980775318135,4.96827661563313,-10.4183714491277));
#23715=CARTESIAN_POINT('Ctrl Pts',(2.00000205147375,4.98485652941228,-10.4183211217629));
#23716=CARTESIAN_POINT('Ctrl Pts',(1.99996693687244,5.03443237844717,-10.4183302175963));
#23717=CARTESIAN_POINT('Ctrl Pts',(1.99912607508997,5.06735219238454,-10.4185481096773));
#23718=CARTESIAN_POINT('Ctrl Pts',(1.99583786907306,5.13293847289988,-10.4193985483784));
#23719=CARTESIAN_POINT('Ctrl Pts',(1.99339099987005,5.16560441420555,-10.420030954252));
#23720=CARTESIAN_POINT('Ctrl Pts',(1.98367176568468,5.26322554237064,-10.4225350158964));
#23721=CARTESIAN_POINT('Ctrl Pts',(1.97402586888932,5.32780480023109,-10.4250136304415));
#23722=CARTESIAN_POINT('Ctrl Pts',(1.9548193467042,5.42392491498701,-10.4298864951246));
#23723=CARTESIAN_POINT('Ctrl Pts',(1.94762626573488,5.45583996202888,-10.4317032822354));
#23724=CARTESIAN_POINT('Ctrl Pts',(1.93164261621215,5.51941798909179,-10.4357117876031));
#23725=CARTESIAN_POINT('Ctrl Pts',(1.92285102952203,5.55108181595763,-10.4379037638056));
#23726=CARTESIAN_POINT('Ctrl Pts',(1.90364740470372,5.61415021866191,-10.4426513510036));
#23727=CARTESIAN_POINT('Ctrl Pts',(1.89321003632208,5.6456046095741,-10.4452129199845));
#23728=CARTESIAN_POINT('Ctrl Pts',(1.87095855891445,5.70749986395087,-10.4506203388836));
#23729=CARTESIAN_POINT('Ctrl Pts',(1.85910168213551,5.73808854322452,-10.4534768098387));
#23730=CARTESIAN_POINT('Ctrl Pts',(1.8339779445532,5.79847284025612,-10.4594620739706));
#23731=CARTESIAN_POINT('Ctrl Pts',(1.82070662763005,5.82828358813145,-10.4625919809456));
#23732=CARTESIAN_POINT('Ctrl Pts',(1.79275976270791,5.88715217292303,-10.469100440457));
#23733=CARTESIAN_POINT('Ctrl Pts',(1.77808419565885,5.91620999846434,-10.4724790096989));
#23734=CARTESIAN_POINT('Ctrl Pts',(1.74733285784584,5.9735770502033,-10.479459335819));
#23735=CARTESIAN_POINT('Ctrl Pts',(1.73125708959058,6.00188627628834,-10.4830611089991));
#23736=CARTESIAN_POINT('Ctrl Pts',(1.69769896693899,6.05775500930874,-10.4904625034394));
#23737=CARTESIAN_POINT('Ctrl Pts',(1.680216636838,6.08531452743744,-10.4942621414599));
#23738=CARTESIAN_POINT('Ctrl Pts',(1.6438283608928,6.13967719513339,-10.5020337518928));
#23739=CARTESIAN_POINT('Ctrl Pts',(1.62493375767266,6.16646501863456,-10.5060033932866));
#23740=CARTESIAN_POINT('Ctrl Pts',(1.58564744196769,6.21933321045759,-10.5140984106397));
#23741=CARTESIAN_POINT('Ctrl Pts',(1.56538882278599,6.24523258009862,-10.5181960951784));
#23742=CARTESIAN_POINT('Ctrl Pts',(1.50303037664793,6.32103357381821,-10.5305443385106));
#23743=CARTESIAN_POINT('Ctrl Pts',(1.45922576593362,6.36925089699378,-10.5388778563317));
#23744=CARTESIAN_POINT('Ctrl Pts',(1.36728548654099,6.4610677622726,-10.5554971737949));
#23745=CARTESIAN_POINT('Ctrl Pts',(1.31914109238269,6.50468474190315,-10.5637856957625));
#23746=CARTESIAN_POINT('Ctrl Pts',(1.21845734621205,6.58731572843475,-10.5800869305743));
#23747=CARTESIAN_POINT('Ctrl Pts',(1.16590089678122,6.62634227836551,-10.5881026704127));
#23748=CARTESIAN_POINT('Ctrl Pts',(1.05627796645429,6.69958569974766,-10.6036104052836));
#23749=CARTESIAN_POINT('Ctrl Pts',(1.00012825879239,6.73319428473922,-10.610971416454));
#23750=CARTESIAN_POINT('Ctrl Pts',(0.885137260859031,6.79464536121258,-10.6247432874189));
#23751=CARTESIAN_POINT('Ctrl Pts',(0.826310799492401,6.82247695507946,-10.6311523545183));
#23752=CARTESIAN_POINT('Ctrl Pts',(0.705992745787938,6.8723744573944,-10.6428432917456));
#23753=CARTESIAN_POINT('Ctrl Pts',(0.644479854326622,6.89444197624564,-10.648125986718));
#23754=CARTESIAN_POINT('Ctrl Pts',(0.550215580868819,6.92310227913939,-10.6550711100818));
#23755=CARTESIAN_POINT('Ctrl Pts',(0.518399021882904,6.93192343972681,-10.6572252532775));
#23756=CARTESIAN_POINT('Ctrl Pts',(0.454218229150574,6.94801208377446,-10.6611754203266));
#23757=CARTESIAN_POINT('Ctrl Pts',(0.422094228207732,6.95522025003796,-10.6629567790744));
#23758=CARTESIAN_POINT('Ctrl Pts',(0.357668463408306,6.96802519471123,-10.6661342030247));
#23759=CARTESIAN_POINT('Ctrl Pts',(0.325385563923601,6.97361726606649,-10.6675291220501));
#23760=CARTESIAN_POINT('Ctrl Pts',(0.260681346265714,6.98320100029813,-10.6699266441343));
#23761=CARTESIAN_POINT('Ctrl Pts',(0.228260022506622,6.98719259450597,-10.6709292529959));
#23762=CARTESIAN_POINT('Ctrl Pts',(0.130789384959454,6.99677970952189,-10.6733414284682));
#23763=CARTESIAN_POINT('Ctrl Pts',(0.0655215736507795,6.99999178607152,
-10.6741551715738));
#23764=CARTESIAN_POINT('Ctrl Pts',(4.03188655311423E-16,6.99999286992453,
-10.674155471012));
#23765=CARTESIAN_POINT('Ctrl Pts',(5.66553889764798E-16,7.,-10.6741648723787));
#23766=CARTESIAN_POINT('Ctrl Pts',(3.59143153197828E-16,7.32295693650353,
-11.1));
#23767=CARTESIAN_POINT('Origin',(0.,274.500012,0.));
#23768=CARTESIAN_POINT('',(-1.12667505521557E-15,274.500012,-9.2));
#23769=CARTESIAN_POINT('Origin',(0.,0.,0.));
#23770=CARTESIAN_POINT('',(-1.18790739517294E-15,0.,9.70000000000007));
#23771=CARTESIAN_POINT('Origin',(0.,275.,0.));
#23772=CARTESIAN_POINT('',(-1.2981256070962E-15,275.,10.6));
#23773=CARTESIAN_POINT('Origin',(0.,0.499999999999945,0.));
#23774=CARTESIAN_POINT('',(-1.35935794705356E-15,0.499999999999945,-11.1));
#32965=UNCERTAINTY_MEASURE_WITH_UNIT(LENGTH_MEASURE(0.01),#33017,
'DISTANCE_ACCURACY_VALUE',
'Maximum model space distance between geometric entities at asserted c
onnectivities');
#32984=UNCERTAINTY_MEASURE_WITH_UNIT(LENGTH_MEASURE(0.01),#33017,
'DISTANCE_ACCURACY_VALUE',
'Maximum model space distance between geometric entities at asserted c
onnectivities');
#32997=(
GEOMETRIC_REPRESENTATION_CONTEXT(3)
GLOBAL_UNCERTAINTY_ASSIGNED_CONTEXT((#32965))
GLOBAL_UNIT_ASSIGNED_CONTEXT((#33017,#33019,#33020))
REPRESENTATION_CONTEXT('','3D')
);
#33016=(
GEOMETRIC_REPRESENTATION_CONTEXT(3)
GLOBAL_UNCERTAINTY_ASSIGNED_CONTEXT((#32984))
GLOBAL_UNIT_ASSIGNED_CONTEXT((#33017,#33019,#33020))
REPRESENTATION_CONTEXT('','3D')
);
#33017=(
LENGTH_UNIT()
NAMED_UNIT(*)
SI_UNIT(.MILLI.,.METRE.)
);
#33019=(
NAMED_UNIT(*)
PLANE_ANGLE_UNIT()
SI_UNIT($,.RADIAN.)
);
#33020=(
NAMED_UNIT(*)
SI_UNIT($,.STERADIAN.)
SOLID_ANGLE_UNIT()
);
#33033=SHAPE_DEFINITION_REPRESENTATION(#33072,#33136);
#33072=PRODUCT_DEFINITION_SHAPE('',$,#33168);
#33136=SHAPE_REPRESENTATION('',(#10704),#32997);
#33155=PRODUCT_DEFINITION_CONTEXT('part definition',#33250,'design');
#33168=PRODUCT_DEFINITION(
'P_Torque Wrench_Barrel_PRT-TQ-1012-02_M_Rev01','PRT-TQ-1012-02',#33199,
#33155);
#33199=PRODUCT_DEFINITION_FORMATION('',$,#33264);
#33250=APPLICATION_CONTEXT(
'Core Data for Automotive Mechanical Design Process');
#33251=PRODUCT_CONTEXT('part definition',#33250,'mechanical');
#33264=PRODUCT('P_Torque Wrench_Barrel_PRT-TQ-1012-02_M_Rev01',
'PRT-TQ-1012-02',$,(#33251));
#33284=PRESENTATION_STYLE_ASSIGNMENT((#33291));
#33291=SURFACE_STYLE_USAGE(.BOTH.,#33298);
#33298=SURFACE_SIDE_STYLE('',(#33305));
#33305=SURFACE_STYLE_FILL_AREA(#33312);
#33312=FILL_AREA_STYLE('Opaque(186,91,6)',(#33319));
#33319=FILL_AREA_STYLE_COLOUR('Opaque(186,91,6)',#33326);
#33326=COLOUR_RGB('Opaque(186,91,6)', 0.09019608, 0.27058824, 0.51372549);
ENDSEC;
END-ISO-10303-21;
